ISO-10303-21;
HEADER;
/* Generated by software containing ST-Developer
 * from STEP Tools, Inc. (www.steptools.com) 
 */

FILE_DESCRIPTION(
/* description */ ('STEP AP214'),
/* implementation_level */ '2;1');

FILE_NAME(
/* name */ 'PRT-TQ-1012-01.step',
/* time_stamp */ '2026-10-07T12:49:37-07:00',
/* author */ (''),
/* organization */ (''),
/* preprocessor_version */ 'ST-DEVELOPER v20.2',
/* originating_system */ 'Autodesk Translation Framework v15.15.0.0',
/* authorisation */ '');

FILE_SCHEMA (('AUTOMOTIVE_DESIGN { 1 0 10303 214 3 1 1 }'));
ENDSEC;

DATA;
#10=MECHANICAL_DESIGN_GEOMETRIC_PRESENTATION_REPRESENTATION('',(#287),#33016);
#233=SHAPE_REPRESENTATION_RELATIONSHIP('SRR','None',#33125,#260);
#260=ADVANCED_BREP_SHAPE_REPRESENTATION('',(#318),#32986);
#287=STYLED_ITEM('',(#33284),#318);
#318=MANIFOLD_SOLID_BREP('Body1',#9942);
#345=CONICAL_SURFACE('',#10507,8.35,0.0195779178250561);
#384=TOROIDAL_SURFACE('',#10492,24.,1.);
#385=TOROIDAL_SURFACE('',#10497,24.,1.);
#386=TOROIDAL_SURFACE('',#10509,10.7,2.35);
#406=ELLIPSE('',#10481,60.7873002660044,48.913538415008);
#407=ELLIPSE('',#10482,61.4826185628427,49.2667804806539);
#408=ELLIPSE('',#10484,60.7873001110675,48.9135383360532);
#409=ELLIPSE('',#10485,61.4826190218256,49.2667807119994);
#416=(
BOUNDED_SURFACE()
B_SPLINE_SURFACE(3,2,((#16054,#16055,#16056),(#16057,#16058,#16059),(#16060,
#16061,#16062),(#16063,#16064,#16065),(#16066,#16067,#16068),(#16069,#16070,
#16071),(#16072,#16073,#16074),(#16075,#16076,#16077),(#16078,#16079,#16080),
(#16081,#16082,#16083),(#16084,#16085,#16086),(#16087,#16088,#16089),(#16090,
#16091,#16092),(#16093,#16094,#16095),(#16096,#16097,#16098),(#16099,#16100,
#16101),(#16102,#16103,#16104),(#16105,#16106,#16107),(#16108,#16109,#16110),
(#16111,#16112,#16113),(#16114,#16115,#16116),(#16117,#16118,#16119),(#16120,
#16121,#16122),(#16123,#16124,#16125),(#16126,#16127,#16128),(#16129,#16130,
#16131),(#16132,#16133,#16134),(#16135,#16136,#16137),(#16138,#16139,#16140),
(#16141,#16142,#16143),(#16144,#16145,#16146),(#16147,#16148,#16149),(#16150,
#16151,#16152),(#16153,#16154,#16155),(#16156,#16157,#16158),(#16159,#16160,
#16161)),.UNSPECIFIED.,.F.,.F.,.F.)
B_SPLINE_SURFACE_WITH_KNOTS((4,2,2,2,2,2,2,2,2,2,2,2,2,2,2,2,2,4),(3,3),
(-4.50555258903737E-5,0.00452987415304152,0.00910480383197342,0.0136797335109053,
0.0159671983503713,0.0182546631898372,0.027404522547701,0.0319794522266329,
0.0342669170660989,0.0365543819055648,0.0457042412634286,0.0502791709423605,
0.0525666357818265,0.0548541006212924,0.0640039599791562,0.0662914248186222,
0.0685788896580881,0.0731634999929292),(0.00648189094804022,1.),
 .UNSPECIFIED.)
GEOMETRIC_REPRESENTATION_ITEM()
RATIONAL_B_SPLINE_SURFACE(((1.,1.,1.),(0.999999993904585,0.999999529811955,
1.),(0.999994327863884,0.999562462855218,1.),(0.999974289583845,0.998016750330974,
1.),(0.999959924932785,0.996908690107867,1.),(0.999924657184913,0.994188207138111,
1.),(0.999903750698009,0.992575522886546,1.),(0.999868762611196,0.989876612407046,
1.),(0.999856492038748,0.988930085186398,1.),(0.999830915534174,0.986957165186696,
1.),(0.999817574138465,0.985928036818482,1.),(0.999749334292439,0.980664152670038,
1.),(0.999689814480974,0.976072914407798,1.),(0.999600229749444,0.969162528823739,
1.),(0.999570279370106,0.966852216942669,1.),(0.999525883242204,0.96342758914054,
1.),(0.999511171834468,0.962292780806495,1.),(0.999482026548572,0.960044572210512,
1.),(0.999467654311881,0.958935926847064,1.),(0.999397542938765,0.953527676872053,
1.),(0.999346550374578,0.949594213273523,1.),(0.999280801890057,0.944522507728965,
1.),(0.999260669064275,0.942969502136649,1.),(0.999233527235783,0.940875836205731,
1.),(0.999225015439781,0.940219253422205,1.),(0.999209261308267,0.939004011478145,
1.),(0.999201991019664,0.938443196072482,1.),(0.99916868183243,0.935873792521809,
1.),(0.999151750490558,0.934567742944055,1.),(0.999143044500685,0.933896180436781,
1.),(0.999141927129791,0.933809988698688,1.),(0.999140956782754,0.933735138084517,
1.),(0.999141099903996,0.933746178168636,1.),(0.999143353447026,0.933920011934732,
1.),(0.999147295336228,0.93422408132076,1.),(0.999153508906997,0.934703383643111,
1.)))
REPRESENTATION_ITEM('')
SURFACE()
);
#417=(
BOUNDED_SURFACE()
B_SPLINE_SURFACE(3,2,((#16188,#16189,#16190),(#16191,#16192,#16193),(#16194,
#16195,#16196),(#16197,#16198,#16199),(#16200,#16201,#16202),(#16203,#16204,
#16205),(#16206,#16207,#16208),(#16209,#16210,#16211),(#16212,#16213,#16214),
(#16215,#16216,#16217),(#16218,#16219,#16220),(#16221,#16222,#16223),(#16224,
#16225,#16226),(#16227,#16228,#16229)),.UNSPECIFIED.,.F.,.F.,.F.)
B_SPLINE_SURFACE_WITH_KNOTS((4,2,2,2,2,2,4),(3,3),(-3.46944695195361E-18,
0.00544424253398455,0.0108884850679691,0.0122495457014652,0.0136106063349614,
0.0163327276019537,0.0217769701359382),(0.,1.),.UNSPECIFIED.)
GEOMETRIC_REPRESENTATION_ITEM()
RATIONAL_B_SPLINE_SURFACE(((1.,0.934274323097636,1.),(1.,0.937315053619643,
1.),(1.,0.939640795315729,1.),(1.,0.942781933275843,1.),(1.,0.943598076957802,
1.),(1.,0.943602884890644,1.),(1.,0.943552641913045,1.),(1.,0.943351495816259,
1.),(1.,0.943200678675229,1.),(1.,0.942600625954464,1.),(1.,0.942003873396426,
1.),(1.,0.939645364712022,1.),(1.,0.937315936924793,1.),(1.,0.934274323097636,
1.)))
REPRESENTATION_ITEM('')
SURFACE()
);
#418=(
BOUNDED_SURFACE()
B_SPLINE_SURFACE(3,2,((#16234,#16235,#16236),(#16237,#16238,#16239),(#16240,
#16241,#16242),(#16243,#16244,#16245),(#16246,#16247,#16248),(#16249,#16250,
#16251),(#16252,#16253,#16254),(#16255,#16256,#16257),(#16258,#16259,#16260),
(#16261,#16262,#16263),(#16264,#16265,#16266),(#16267,#16268,#16269),(#16270,
#16271,#16272),(#16273,#16274,#16275),(#16276,#16277,#16278),(#16279,#16280,
#16281),(#16282,#16283,#16284),(#16285,#16286,#16287),(#16288,#16289,#16290),
(#16291,#16292,#16293),(#16294,#16295,#16296),(#16297,#16298,#16299),(#16300,
#16301,#16302),(#16303,#16304,#16305),(#16306,#16307,#16308),(#16309,#16310,
#16311),(#16312,#16313,#16314),(#16315,#16316,#16317),(#16318,#16319,#16320),
(#16321,#16322,#16323),(#16324,#16325,#16326),(#16327,#16328,#16329),(#16330,
#16331,#16332),(#16333,#16334,#16335),(#16336,#16337,#16338),(#16339,#16340,
#16341)),.UNSPECIFIED.,.F.,.F.,.F.)
B_SPLINE_SURFACE_WITH_KNOTS((4,2,2,2,2,2,2,2,2,2,2,2,2,2,2,2,2,4),(3,3),
(-4.50555258903737E-5,0.00452987415304152,0.00910480383197342,0.0136797335109053,
0.0159671983503713,0.0182546631898372,0.027404522547701,0.0319794522266329,
0.0342669170660989,0.0365543819055648,0.0457042412634286,0.0502791709423605,
0.0525666357818265,0.0548541006212924,0.0640039599791562,0.0662914248186222,
0.0685788896580881,0.0732274786700752),(0.,0.993439831725527),
 .UNSPECIFIED.)
GEOMETRIC_REPRESENTATION_ITEM()
RATIONAL_B_SPLINE_SURFACE(((1.,1.,1.),(1.,0.999999529849,0.999999993831461),
(1.,0.999562497327904,0.999994259817701),(1.,0.998016906587292,0.999973981147017),
(1.,0.996908933666058,0.999959444169404),(1.,0.994188665037773,0.999923753329497),
(1.,0.992576107846411,0.999902596036442),(1.,0.989877410008729,0.999867188212567),
(1.,0.988930957363088,0.999854770435329),(1.,0.98695819280585,0.999828887100406),
(1.,0.985929145520624,0.999815385653699),(1.,0.980665676103199,0.999746327163528),
(1.,0.976074799575539,0.99968609331843),(1.,0.969164958447091,0.999595433877325),
(1.,0.966854828590923,0.99956512419614),(1.,0.963430470608444,0.999520195466946),
(1.,0.962295751683703,0.999505307572765),(1.,0.960047720219627,0.999475812643384),
(1.,0.958939162204112,0.999461267989136),(1.,0.95353133833463,0.999390315519971),
(1.,0.949598184645746,0.999338711219874),(1.,0.944526878690836,0.999272173979003),
(1.,0.942973995456758,0.999251799628351),(1.,0.940880494481636,0.999224332190992),
(1.,0.940223963428969,0.999215718282626),(1.,0.939008817231418,0.999199775155558),
(1.,0.938448046011292,0.999192417648423),(1.,0.935878844898842,0.999158708865166),
(1.,0.934572898222151,0.999141574405253),(1.,0.933901388625957,0.999132763973354),
(1.,0.933815203678699,0.999131633197841),(1.,0.933740358961945,0.999130651209968),
(1.,0.933751398176195,0.999130796048175),(1.,0.933926836502455,0.999133097858059),
(1.,0.934237786269865,0.999137177623657),(1.,0.934728695117105,0.999143618512948)))
REPRESENTATION_ITEM('')
SURFACE()
);
#419=(
BOUNDED_SURFACE()
B_SPLINE_SURFACE(3,2,((#16362,#16363,#16364),(#16365,#16366,#16367),(#16368,
#16369,#16370),(#16371,#16372,#16373),(#16374,#16375,#16376),(#16377,#16378,
#16379),(#16380,#16381,#16382),(#16383,#16384,#16385),(#16386,#16387,#16388),
(#16389,#16390,#16391),(#16392,#16393,#16394),(#16395,#16396,#16397),(#16398,
#16399,#16400),(#16401,#16402,#16403),(#16404,#16405,#16406),(#16407,#16408,
#16409),(#16410,#16411,#16412),(#16413,#16414,#16415),(#16416,#16417,#16418),
(#16419,#16420,#16421),(#16422,#16423,#16424),(#16425,#16426,#16427),(#16428,
#16429,#16430),(#16431,#16432,#16433),(#16434,#16435,#16436),(#16437,#16438,
#16439),(#16440,#16441,#16442),(#16443,#16444,#16445),(#16446,#16447,#16448),
(#16449,#16450,#16451),(#16452,#16453,#16454),(#16455,#16456,#16457),(#16458,
#16459,#16460),(#16461,#16462,#16463),(#16464,#16465,#16466),(#16467,#16468,
#16469)),.UNSPECIFIED.,.F.,.F.,.F.)
B_SPLINE_SURFACE_WITH_KNOTS((4,2,2,2,2,2,2,2,2,2,2,2,2,2,2,2,2,4),(3,3),
(-4.50555258903755E-5,0.00452987415304115,0.00910480383197267,0.0136797335109042,
0.01596719835037,0.0182546631898357,0.0274045225476988,0.0319794522266303,
0.034266917066096,0.0365543819055618,0.0457042412634248,0.0502791709423564,
0.0525666357818221,0.0548541006212879,0.0640039599791509,0.0662914248186167,
0.0685788896580825,0.0732274786569346),(0.,0.993439832057625),
 .UNSPECIFIED.)
GEOMETRIC_REPRESENTATION_ITEM()
RATIONAL_B_SPLINE_SURFACE(((1.,1.,1.),(1.,0.999999529849,0.999999993831461),
(1.,0.999562497327757,0.99999425981799),(1.,0.998016906586629,0.999973981148326),
(1.,0.996908933665109,0.999959444171444),(1.,0.994188665035747,0.99992375333333),
(1.,0.992576107844015,0.999902596041341),(1.,0.989877410005303,0.999867188219246),
(1.,0.988930957359389,0.999854770442633),(1.,0.986958192801492,0.999828887109012),
(1.,0.985929145515922,0.999815385662983),(1.,0.980665676096738,0.999746327176285),
(1.,0.976074799567374,0.999686093334214),(1.,0.969164958436868,0.999595433897671),
(1.,0.96685482857993,0.999565124218011),(1.,0.963430470596179,0.999520195491075),
(1.,0.962295751671145,0.999505307597643),(1.,0.960047720206233,0.999475812669744),
(1.,0.958939162190388,0.999461268016229),(1.,0.953531338319099,0.999390315550632),
(1.,0.949598184628729,0.999338711253128),(1.,0.944526878672376,0.999272174015606),
(1.,0.942973995437611,0.999251799665976),(1.,0.940880494461918,0.99922433223),
(1.,0.940223963408945,0.999215718322066),(1.,0.939008817211073,0.999199775195801),
(1.,0.938448045990673,0.999192417689035),(1.,0.935878844877576,0.999158708907476),
(1.,0.934572898200279,0.999141574448422),(1.,0.933901388603861,0.999132764016967),
(1.,0.933815203656616,0.999131633241511),(1.,0.933740358939752,0.999130651253686),
(1.,0.933751398154091,0.999130796091887),(1.,0.933926836479949,0.999133097901649),
(1.,0.934237786246193,0.999137177667025),(1.,0.934728695091121,0.999143618555959)))
REPRESENTATION_ITEM('')
SURFACE()
);
#420=(
BOUNDED_SURFACE()
B_SPLINE_SURFACE(3,2,((#16492,#16493,#16494),(#16495,#16496,#16497),(#16498,
#16499,#16500),(#16501,#16502,#16503),(#16504,#16505,#16506),(#16507,#16508,
#16509),(#16510,#16511,#16512),(#16513,#16514,#16515),(#16516,#16517,#16518),
(#16519,#16520,#16521),(#16522,#16523,#16524),(#16525,#16526,#16527),(#16528,
#16529,#16530),(#16531,#16532,#16533)),.UNSPECIFIED.,.F.,.F.,.F.)
B_SPLINE_SURFACE_WITH_KNOTS((4,2,2,2,2,2,4),(3,3),(-1.38777878078145E-17,
0.00544424253398438,0.0108884850679688,0.0122495457014649,0.013610606334961,
0.0163327276019532,0.0217769701359376),(0.,1.),.UNSPECIFIED.)
GEOMETRIC_REPRESENTATION_ITEM()
RATIONAL_B_SPLINE_SURFACE(((1.,0.934274323097636,1.),(1.,0.937315053619719,
1.),(1.,0.939640795315628,1.),(1.,0.942781933275944,1.),(1.,0.943598076957802,
1.),(1.,0.943602884890644,1.),(1.,0.943552641913071,1.),(1.,0.943351495816233,
1.),(1.,0.943200678675229,1.),(1.,0.942600625954464,1.),(1.,0.942003873396376,
1.),(1.,0.939645364712124,1.),(1.,0.937315936924713,1.),(1.,0.934274323097642,
1.)))
REPRESENTATION_ITEM('')
SURFACE()
);
#421=(
BOUNDED_SURFACE()
B_SPLINE_SURFACE(3,2,((#16538,#16539,#16540),(#16541,#16542,#16543),(#16544,
#16545,#16546),(#16547,#16548,#16549),(#16550,#16551,#16552),(#16553,#16554,
#16555),(#16556,#16557,#16558),(#16559,#16560,#16561),(#16562,#16563,#16564),
(#16565,#16566,#16567),(#16568,#16569,#16570),(#16571,#16572,#16573),(#16574,
#16575,#16576),(#16577,#16578,#16579),(#16580,#16581,#16582),(#16583,#16584,
#16585),(#16586,#16587,#16588),(#16589,#16590,#16591),(#16592,#16593,#16594),
(#16595,#16596,#16597),(#16598,#16599,#16600),(#16601,#16602,#16603),(#16604,
#16605,#16606),(#16607,#16608,#16609),(#16610,#16611,#16612),(#16613,#16614,
#16615),(#16616,#16617,#16618),(#16619,#16620,#16621),(#16622,#16623,#16624),
(#16625,#16626,#16627),(#16628,#16629,#16630),(#16631,#16632,#16633),(#16634,
#16635,#16636),(#16637,#16638,#16639),(#16640,#16641,#16642),(#16643,#16644,
#16645)),.UNSPECIFIED.,.F.,.F.,.F.)
B_SPLINE_SURFACE_WITH_KNOTS((4,2,2,2,2,2,2,2,2,2,2,2,2,2,2,2,2,4),(3,3),
(-4.50555258903699E-5,0.00452987415304452,0.00910480383197942,0.0136797335109143,
0.0159671983503818,0.0182546631898492,0.027404522547719,0.0319794522266539,
0.0342669170661213,0.0365543819055888,0.0457042412634586,0.0502791709423935,
0.0525666357818609,0.0548541006213284,0.0640039599791982,0.0662914248186656,
0.0685788896581331,0.0731634999929532),(0.00648190587163059,1.),
 .UNSPECIFIED.)
GEOMETRIC_REPRESENTATION_ITEM()
RATIONAL_B_SPLINE_SURFACE(((1.,1.,1.),(0.999999993904571,0.999999529811961,
1.),(0.99999432785091,0.99956246286179,1.),(0.999974289525037,0.998016750360764,
1.),(0.99995992484112,0.996908690154303,1.),(0.999924657012579,0.994188207225404,
1.),(0.999903750477856,0.992575522998147,1.),(0.999868762311012,0.989876612559059,
1.),(0.999856491710498,0.98893008535267,1.),(0.999830915147422,0.986957165382596,
1.),(0.999817573721197,0.985928037029841,1.),(0.999749333719083,0.98066415296048,
1.),(0.999689813771477,0.976072914767201,1.),(0.999600228835038,0.969162529286938,
1.),(0.999570278387192,0.966852217440492,1.),(0.999525882157743,0.963427589689905,
1.),(0.999511170716356,0.962292781372864,1.),(0.999482025363796,0.960044572810649,
1.),(0.99946765309423,0.958935927463858,1.),(0.999397541560747,0.953527677570119,
1.),(0.999346548879922,0.949594214030664,1.),(0.999280800245013,0.944522508562285,
1.),(0.999260667373182,0.942969502993375,1.),(0.999233525482606,0.940875837093776,
1.),(0.999225013667134,0.940219254320119,1.),(0.999209259499587,0.939004012394397,
1.),(0.999201989194353,0.938443196997076,1.),(0.999168679930933,0.935873793485225,
1.),(0.999151748550332,0.93456774392691,1.),(0.999143042540544,0.933896181429722,
1.),(0.999141925167095,0.933809989692925,1.),(0.999140954817838,0.933735139079878,
1.),(0.999141097939409,0.933746179163875,1.),(0.999143351487591,0.933920012927231,
1.),(0.999147293385812,0.934224082308839,1.),(0.999153506970792,0.93470338462392,
1.)))
REPRESENTATION_ITEM('')
SURFACE()
);
#422=(
BOUNDED_SURFACE()
B_SPLINE_SURFACE(3,2,((#16675,#16676,#16677),(#16678,#16679,#16680),(#16681,
#16682,#16683),(#16684,#16685,#16686),(#16687,#16688,#16689),(#16690,#16691,
#16692),(#16693,#16694,#16695),(#16696,#16697,#16698),(#16699,#16700,#16701),
(#16702,#16703,#16704),(#16705,#16706,#16707),(#16708,#16709,#16710),(#16711,
#16712,#16713),(#16714,#16715,#16716),(#16717,#16718,#16719),(#16720,#16721,
#16722),(#16723,#16724,#16725),(#16726,#16727,#16728),(#16729,#16730,#16731),
(#16732,#16733,#16734)),.UNSPECIFIED.,.F.,.F.,.F.)
B_SPLINE_SURFACE_WITH_KNOTS((4,2,2,2,2,2,2,2,2,4),(3,3),(-1.21430643318376E-17,
0.000286716408612401,0.000573432817224815,0.00114686563444964,0.00229373126889929,
0.0045874625377986,0.00688119380669791,0.00917492507559722,0.0137623876133958,
0.0183498501511944),(0.,1.),.UNSPECIFIED.)
GEOMETRIC_REPRESENTATION_ITEM()
RATIONAL_B_SPLINE_SURFACE(((1.,0.715678085420542,1.),(1.,0.732713574734388,
1.),(1.,0.751287941176003,1.),(1.,0.783048929818799,1.),(1.,0.796213241095476,
1.),(1.,0.829148860260418,1.),(1.,0.843569652884034,1.),(1.,0.879829452120598,
1.),(1.,0.894194157570232,1.),(1.,0.930380052244755,1.),(1.,0.943334851348775,
1.),(1.,0.964070509897579,1.),(1.,0.97097877739709,1.),(1.,0.98166631964498,
1.),(1.,0.985389932826228,1.),(1.,0.994077955423915,1.),(1.,0.996586035113217,
1.),(1.,0.999617313053908,1.),(1.,0.999976096727813,1.),(1.,1.,1.)))
REPRESENTATION_ITEM('')
SURFACE()
);
#423=(
BOUNDED_SURFACE()
B_SPLINE_SURFACE(3,2,((#16736,#16737,#16738),(#16739,#16740,#16741),(#16742,
#16743,#16744),(#16745,#16746,#16747)),.UNSPECIFIED.,.F.,.F.,.F.)
B_SPLINE_SURFACE_WITH_KNOTS((4,4),(3,3),(0.,0.00310259288126481),(0.,1.),
 .UNSPECIFIED.)
GEOMETRIC_REPRESENTATION_ITEM()
RATIONAL_B_SPLINE_SURFACE(((1.,0.707106781186544,1.),(1.,0.709735448065174,
1.),(1.,0.712575844075049,1.),(1.,0.715678085420518,1.)))
REPRESENTATION_ITEM('')
SURFACE()
);
#424=(
BOUNDED_SURFACE()
B_SPLINE_SURFACE(3,2,((#16751,#16752,#16753),(#16754,#16755,#16756),(#16757,
#16758,#16759),(#16760,#16761,#16762)),.UNSPECIFIED.,.F.,.F.,.F.)
B_SPLINE_SURFACE_WITH_KNOTS((4,4),(3,3),(-1.73472347597681E-18,0.00310259288126371),
(0.,1.),.UNSPECIFIED.)
GEOMETRIC_REPRESENTATION_ITEM()
RATIONAL_B_SPLINE_SURFACE(((1.,0.715678085420547,1.),(1.,0.712575844075018,
1.),(1.,0.709735448065194,1.),(1.,0.707106781186547,1.)))
REPRESENTATION_ITEM('')
SURFACE()
);
#425=(
BOUNDED_SURFACE()
B_SPLINE_SURFACE(3,2,((#16764,#16765,#16766),(#16767,#16768,#16769),(#16770,
#16771,#16772),(#16773,#16774,#16775),(#16776,#16777,#16778),(#16779,#16780,
#16781),(#16782,#16783,#16784),(#16785,#16786,#16787),(#16788,#16789,#16790),
(#16791,#16792,#16793),(#16794,#16795,#16796),(#16797,#16798,#16799),(#16800,
#16801,#16802),(#16803,#16804,#16805),(#16806,#16807,#16808),(#16809,#16810,
#16811),(#16812,#16813,#16814),(#16815,#16816,#16817),(#16818,#16819,#16820),
(#16821,#16822,#16823),(#16824,#16825,#16826),(#16827,#16828,#16829)),
 .UNSPECIFIED.,.F.,.F.,.F.)
B_SPLINE_SURFACE_WITH_KNOTS((4,2,2,2,2,2,2,2,2,2,4),(3,3),(-4.45822180120765E-5,
0.00456146106532619,0.00686448270699533,0.00916750434866446,0.0114705259903336,
0.0137735476320027,0.0160765692736719,0.0172280800945064,0.0178038355049237,
0.0180917132101324,0.018655949664608),(0.,1.00027635874927),
 .UNSPECIFIED.)
GEOMETRIC_REPRESENTATION_ITEM()
RATIONAL_B_SPLINE_SURFACE(((1.,1.,1.),(1.,0.999975269355394,1.00000001366906),
(1.,0.999616856262281,1.00000021177025),(1.,0.997367139234066,1.00000145522822),
(1.,0.996329945283138,1.00000202850346),(1.,0.993242400650488,1.00000373504341),
(1.,0.991218555061358,1.00000485365828),(1.,0.985482929988757,1.00000802383862),
(1.,0.981797060269541,1.00001006108331),(1.,0.971222431433512,1.00001590586571),
(1.,0.964447640919971,1.00001965041098),(1.,0.943699466562788,1.00003111829001),
(1.,0.930712139865289,1.00003829661273),(1.,0.89444331730149,1.00005834302561),
(1.,0.880044194752108,1.00006630167261),(1.,0.843708864884983,1.00008638484524),
(1.,0.82925954511809,1.00009437123712),(1.,0.796263056814172,1.0001126089736),
(1.,0.783074395977812,1.00011989857722),(1.,0.735984363806146,1.00014592606201),
(1.,0.694442358121852,1.00016888705548),(1.,0.674552380648109,1.00017988059407)))
REPRESENTATION_ITEM('')
SURFACE()
);
#426=(
BOUNDED_SURFACE()
B_SPLINE_SURFACE(3,2,((#16830,#16831,#16832),(#16833,#16834,#16835),(#16836,
#16837,#16838),(#16839,#16840,#16841),(#16842,#16843,#16844),(#16845,#16846,
#16847),(#16848,#16849,#16850),(#16851,#16852,#16853),(#16854,#16855,#16856),
(#16857,#16858,#16859),(#16860,#16861,#16862),(#16863,#16864,#16865),(#16866,
#16867,#16868),(#16869,#16870,#16871),(#16872,#16873,#16874),(#16875,#16876,
#16877),(#16878,#16879,#16880),(#16881,#16882,#16883),(#16884,#16885,#16886),
(#16887,#16888,#16889),(#16890,#16891,#16892),(#16893,#16894,#16895)),
 .UNSPECIFIED.,.F.,.F.,.F.)
B_SPLINE_SURFACE_WITH_KNOTS((4,2,2,2,2,2,2,2,2,2,4),(3,3),(-4.45822180121706E-5,
0.00228108920328879,0.00460676062458975,0.00925810346719167,0.0115837748884926,
0.0139094463097936,0.0162351177310945,0.017397953441745,0.0179793712970703,
0.0182700802247329,0.0185607891523955),(0.,1.),.UNSPECIFIED.)
GEOMETRIC_REPRESENTATION_ITEM()
RATIONAL_B_SPLINE_SURFACE(((1.,1.,1.),(1.,0.999998791721631,1.),(1.,0.999892445298426,
1.),(1.,0.999316761910651,1.),(1.,0.998852418425575,1.),(1.,0.996589788033769,
1.),(1.,0.994126671587873,1.),(1.,0.985446396309632,1.),(1.,0.981713646123456,
1.),(1.,0.971107052837317,1.),(1.,0.96432827074271,1.),(1.,0.943870035476799,
1.),(1.,0.931100277618097,1.),(1.,0.894796160803365,1.),(1.,0.88026171681454,
1.),(1.,0.843728071613052,1.),(1.,0.829200458708476,1.),(1.,0.796111926064673,
1.),(1.,0.782895634776705,1.),(1.,0.751122556026189,1.),(1.,0.732604759639831,
1.),(1.,0.715678085420547,1.)))
REPRESENTATION_ITEM('')
SURFACE()
);
#427=(
BOUNDED_SURFACE()
B_SPLINE_SURFACE(3,2,((#16897,#16898,#16899),(#16900,#16901,#16902),(#16903,
#16904,#16905),(#16906,#16907,#16908)),.UNSPECIFIED.,.F.,.F.,.F.)
B_SPLINE_SURFACE_WITH_KNOTS((4,4),(3,3),(0.,0.00310259288127954),(0.,1.),
 .UNSPECIFIED.)
GEOMETRIC_REPRESENTATION_ITEM()
RATIONAL_B_SPLINE_SURFACE(((1.,0.715678085420547,1.),(1.,0.712575844075105,
1.),(1.,0.709735448065179,1.),(1.,0.707106781186548,1.)))
REPRESENTATION_ITEM('')
SURFACE()
);
#428=(
BOUNDED_SURFACE()
B_SPLINE_SURFACE(3,2,((#16912,#16913,#16914),(#16915,#16916,#16917),(#16918,
#16919,#16920),(#16921,#16922,#16923)),.UNSPECIFIED.,.F.,.F.,.F.)
B_SPLINE_SURFACE_WITH_KNOTS((4,4),(3,3),(0.,0.00310259288126651),(0.,1.),
 .UNSPECIFIED.)
GEOMETRIC_REPRESENTATION_ITEM()
RATIONAL_B_SPLINE_SURFACE(((1.,0.70710678118654,1.),(1.,0.709735448065188,
1.),(1.,0.712575844075016,1.),(1.,0.715678085420547,1.)))
REPRESENTATION_ITEM('')
SURFACE()
);
#429=(
BOUNDED_SURFACE()
B_SPLINE_SURFACE(3,2,((#16925,#16926,#16927),(#16928,#16929,#16930),(#16931,
#16932,#16933),(#16934,#16935,#16936),(#16937,#16938,#16939),(#16940,#16941,
#16942),(#16943,#16944,#16945),(#16946,#16947,#16948),(#16949,#16950,#16951),
(#16952,#16953,#16954),(#16955,#16956,#16957),(#16958,#16959,#16960),(#16961,
#16962,#16963),(#16964,#16965,#16966),(#16967,#16968,#16969),(#16970,#16971,
#16972),(#16973,#16974,#16975),(#16976,#16977,#16978),(#16979,#16980,#16981),
(#16982,#16983,#16984)),.UNSPECIFIED.,.F.,.F.,.F.)
B_SPLINE_SURFACE_WITH_KNOTS((4,2,2,2,2,2,2,2,2,4),(3,3),(0.,0.000286716408612405,
0.00057343281722481,0.00114686563444962,0.00229373126889924,0.00458746253779848,
0.00688119380669772,0.00917492507559696,0.0137623876133954,0.0183498501511939),
(0.,1.),.UNSPECIFIED.)
GEOMETRIC_REPRESENTATION_ITEM()
RATIONAL_B_SPLINE_SURFACE(((1.,0.715678085420547,1.),(1.,0.732713574734547,
1.),(1.,0.751287941176143,1.),(1.,0.783048929818852,1.),(1.,0.796213241095647,
1.),(1.,0.829148860260267,1.),(1.,0.843569652884057,1.),(1.,0.879829452120653,
1.),(1.,0.894194157570376,1.),(1.,0.930380052244515,1.),(1.,0.943334851348824,
1.),(1.,0.964070509897542,1.),(1.,0.970978777396964,1.),(1.,0.981666319645111,
1.),(1.,0.985389932826229,1.),(1.,0.994077955423916,1.),(1.,0.996586035113046,
1.),(1.,0.99961731305408,1.),(1.,0.999976096727683,1.),(1.,1.,1.)))
REPRESENTATION_ITEM('')
SURFACE()
);
#430=(
BOUNDED_SURFACE()
B_SPLINE_SURFACE(2,2,((#16994,#16995,#16996,#16997,#16998,#16999,#17000,
#17001,#17002),(#17003,#17004,#17005,#17006,#17007,#17008,#17009,#17010,
#17011),(#17012,#17013,#17014,#17015,#17016,#17017,#17018,#17019,#17020)),
 .UNSPECIFIED.,.F.,.T.,.F.)
B_SPLINE_SURFACE_WITH_KNOTS((3,3),(3,2,2,2,3),(-0.442628884695582,0.442628884695581),
(-3.14159265358979,-1.5707963267949,0.,1.5707963267949,3.14159265358979),
 .UNSPECIFIED.)
GEOMETRIC_REPRESENTATION_ITEM()
RATIONAL_B_SPLINE_SURFACE(((1.,0.707106781186548,1.,0.707106781186548,1.,
0.707106781186548,1.,0.707106781186548,1.),(0.903628792385486,0.638962046771188,
0.903628792385486,0.638962046771188,0.903628792385486,0.638962046771188,
0.903628792385486,0.638962046771188,0.903628792385486),(1.,0.707106781186548,
1.,0.707106781186548,1.,0.707106781186548,1.,0.707106781186548,1.)))
REPRESENTATION_ITEM('')
SURFACE()
);
#474=FACE_BOUND('',#1698,.T.);
#475=FACE_BOUND('',#1700,.T.);
#476=FACE_BOUND('',#1710,.T.);
#477=FACE_BOUND('',#1722,.T.);
#478=FACE_BOUND('',#1725,.T.);
#479=FACE_BOUND('',#1726,.T.);
#480=FACE_BOUND('',#1731,.T.);
#554=B_SPLINE_CURVE_WITH_KNOTS('',3,(#14640,#14641,#14642,#14643,#14644,
#14645,#14646,#14647,#14648,#14649,#14650,#14651,#14652,#14653,#14654,#14655,
#14656,#14657,#14658,#14659,#14660,#14661,#14662,#14663,#14664,#14665,#14666,
#14667,#14668,#14669,#14670,#14671,#14672,#14673),.UNSPECIFIED.,.F.,.F.,
(4,3,3,3,3,3,3,3,3,3,3,4),(0.0010057065754485,0.00361866511599219,0.00531965656119927,
0.00803958816950913,0.010759519777819,0.0107707078352687,0.011882063272691,
0.0121325673456277,0.01349922673087,0.0162115567860829,0.0188836740964046,
0.0205357090950889),.UNSPECIFIED.);
#555=B_SPLINE_CURVE_WITH_KNOTS('',3,(#14677,#14678,#14679,#14680,#14681,
#14682,#14683,#14684,#14685,#14686,#14687,#14688,#14689,#14690,#14691,#14692,
#14693,#14694,#14695,#14696,#14697,#14698,#14699,#14700,#14701,#14702,#14703,
#14704,#14705,#14706,#14707,#14708,#14709,#14710),.UNSPECIFIED.,.F.,.F.,
(4,3,3,3,3,3,3,3,3,3,3,4),(0.00100601928210048,0.00367908692095566,0.00533170946801007,
0.00804500415847367,0.00941214959364056,0.0105239002825655,0.0107744934468549,
0.0107856854833192,0.013506584430358,0.0162274833773967,0.0188413712147584,
0.0205429676116094),.UNSPECIFIED.);
#556=B_SPLINE_CURVE_WITH_KNOTS('',3,(#14715,#14716,#14717,#14718),
 .UNSPECIFIED.,.F.,.F.,(4,4),(0.,0.00310259288128586),.UNSPECIFIED.);
#557=B_SPLINE_CURVE_WITH_KNOTS('',3,(#14720,#14721,#14722,#14723,#14724,
#14725,#14726,#14727,#14728,#14729,#14730,#14731,#14732,#14733,#14734,#14735,
#14736,#14737,#14738,#14739,#14740,#14741,#14742,#14743,#14744,#14745,#14746,
#14747,#14748,#14749,#14750,#14751,#14752,#14753,#14754,#14755,#14756,#14757,
#14758,#14759,#14760,#14761,#14762,#14763,#14764,#14765,#14766,#14767,#14768,
#14769,#14770,#14771,#14772,#14773,#14774,#14775,#14776,#14777,#14778,#14779,
#14780,#14781,#14782,#14783,#14784,#14785,#14786,#14787,#14788,#14789,#14790,
#14791,#14792,#14793,#14794,#14795,#14796,#14797,#14798),.UNSPECIFIED.,
 .F.,.F.,(4,3,3,3,3,3,3,3,3,3,3,3,3,3,3,3,3,3,3,3,3,3,3,3,3,3,4),(0.,0.00029089201195018,
0.00058177691126932,0.00116064017748705,0.001163542589709,0.00232128035497411,
0.00232708521749185,0.00464256070994822,0.00465417035496075,0.00696384106492234,
0.00698125566896419,0.00813318854443032,0.00928512141989645,0.00930822641010844,
0.0103189114251322,0.0113354153193445,0.0116064017748706,0.0127670419523576,
0.0139276821298447,0.0139287558918501,0.0148713512522913,0.0158107627881495,
0.0162438817323399,0.0162489624848188,0.0180760281528238,0.0183987634801277,
0.0185702428397929),.UNSPECIFIED.);
#558=B_SPLINE_CURVE_WITH_KNOTS('',3,(#14800,#14801,#14802,#14803,#14804,
#14805,#14806,#14807,#14808,#14809,#14810,#14811,#14812,#14813,#14814,#14815,
#14816,#14817,#14818,#14819,#14820,#14821,#14822,#14823,#14824,#14825,#14826,
#14827,#14828,#14829,#14830,#14831,#14832,#14833,#14834,#14835,#14836,#14837,
#14838,#14839,#14840,#14841,#14842,#14843,#14844,#14845,#14846,#14847,#14848,
#14849,#14850,#14851,#14852,#14853,#14854,#14855,#14856,#14857,#14858,#14859,
#14860,#14861,#14862,#14863),.UNSPECIFIED.,.F.,.F.,(4,3,3,3,3,3,3,3,3,3,
3,3,3,3,3,3,3,3,3,3,3,4),(-4.46439725195681E-5,0.00185117245303053,0.00227381448108523,
0.00415828625857787,0.00459227293469002,0.00459331693554309,0.00665251407402816,
0.00868942277861947,0.00922918984189961,0.00923169636203958,0.0115471745933297,
0.0115476482955044,0.0128084107178559,0.0138639458401943,0.0138661067491092,
0.016183484747819,0.016184565202714,0.0173432542021003,0.0173437944295164,
0.0179231270235531,0.0182130679058979,0.0185030236563188),.UNSPECIFIED.);
#559=B_SPLINE_CURVE_WITH_KNOTS('',3,(#14865,#14866,#14867,#14868),
 .UNSPECIFIED.,.F.,.F.,(4,4),(0.,0.00310259288126633),.UNSPECIFIED.);
#560=B_SPLINE_CURVE_WITH_KNOTS('',3,(#14875,#14876,#14877,#14878),
 .UNSPECIFIED.,.F.,.F.,(4,4),(0.,0.00310259288126371),.UNSPECIFIED.);
#561=B_SPLINE_CURVE_WITH_KNOTS('',3,(#14880,#14881,#14882,#14883,#14884,
#14885,#14886,#14887,#14888,#14889,#14890,#14891,#14892,#14893,#14894,#14895,
#14896,#14897,#14898,#14899,#14900,#14901,#14902,#14903,#14904,#14905,#14906,
#14907,#14908,#14909,#14910,#14911,#14912,#14913,#14914,#14915,#14916,#14917,
#14918,#14919,#14920,#14921,#14922,#14923,#14924,#14925,#14926,#14927,#14928,
#14929,#14930,#14931,#14932,#14933,#14934,#14935,#14936,#14937,#14938,#14939,
#14940,#14941,#14942,#14943,#14944,#14945,#14946,#14947,#14948,#14949,#14950,
#14951,#14952,#14953,#14954,#14955,#14956,#14957,#14958,#14959,#14960,#14961,
#14962,#14963,#14964,#14965,#14966,#14967),.UNSPECIFIED.,.F.,.F.,(4,3,3,
3,3,3,3,3,3,3,3,3,3,3,3,3,3,3,3,3,3,3,3,3,3,3,3,3,3,4),(0.,0.000288594368059549,
0.000577175639970858,0.00114871783547251,0.00115433020342524,0.00229743567094501,
0.00230866043814268,0.00359206730237028,0.00459487134189001,0.00461731070067686,
0.00543466283320275,0.00627129552525818,0.00689230701283501,0.00691299933338874,
0.00918974268378,0.00920315969262419,0.0101295449954259,0.01105604718127,
0.011487178354725,0.0114986296353845,0.01378461402567,0.0137972845775347,
0.0148523132937294,0.0158566070086,0.016082049696615,0.0172307675320875,
0.0176563774300653,0.0178051264498237,0.0180923059086919,0.01837948536756),
 .UNSPECIFIED.);
#562=B_SPLINE_CURVE_WITH_KNOTS('',3,(#14969,#14970,#14971,#14972,#14973,
#14974,#14975,#14976,#14977,#14978,#14979,#14980,#14981,#14982,#14983,#14984,
#14985,#14986,#14987,#14988,#14989,#14990,#14991,#14992,#14993,#14994,#14995,
#14996,#14997,#14998,#14999,#15000,#15001,#15002,#15003,#15004,#15005,#15006,
#15007,#15008,#15009,#15010,#15011,#15012,#15013,#15014,#15015,#15016,#15017,
#15018,#15019,#15020,#15021,#15022,#15023,#15024,#15025,#15026,#15027,#15028,
#15029,#15030,#15031,#15032),.UNSPECIFIED.,.F.,.F.,(4,3,3,3,3,3,3,3,3,3,
3,3,3,3,3,3,3,3,3,3,3,4),(-4.46439725204971E-5,0.00185117246158491,0.00227381448108429,
0.0041582862784131,0.00459227293468908,0.00459331693554219,0.00665251407724604,
0.00868942278715934,0.00922918984189866,0.00923169636203865,0.0115471745933288,
0.0115476482955035,0.0128084107214943,0.0138639458401934,0.0138661067491082,
0.016183484747818,0.016184565202713,0.0173432542020993,0.0173437944295154,
0.0179231270235523,0.0182130679058973,0.0185030236563178),.UNSPECIFIED.);
#563=B_SPLINE_CURVE_WITH_KNOTS('',3,(#15033,#15034,#15035,#15036),
 .UNSPECIFIED.,.F.,.F.,(4,4),(0.,0.00310259288126471),.UNSPECIFIED.);
#564=B_SPLINE_CURVE_WITH_KNOTS('',3,(#15045,#15046,#15047,#15048,#15049,
#15050,#15051,#15052,#15053,#15054,#15055,#15056,#15057,#15058,#15059,#15060,
#15061,#15062,#15063,#15064,#15065,#15066,#15067,#15068,#15069,#15070,#15071,
#15072,#15073,#15074,#15075,#15076,#15077,#15078,#15079,#15080,#15081,#15082,
#15083,#15084,#15085,#15086,#15087,#15088,#15089,#15090,#15091,#15092,#15093,
#15094,#15095,#15096),.UNSPECIFIED.,.F.,.F.,(4,3,3,3,3,3,3,3,3,3,3,3,3,
3,3,3,3,4),(0.00277080264391651,0.00293212141733799,0.00306062177311605,
0.0031161226260969,0.00324851187334901,0.00335821405905974,0.003462358473441,
0.00364274939856266,0.00382880230054904,0.00399591545353225,0.0041548301681292,
0.00436143559541393,0.00457232483906153,0.00478955939058047,0.0048473018628174,
0.00507782428691642,0.00531647499823543,0.0055397735575056),
 .UNSPECIFIED.);
#565=B_SPLINE_CURVE_WITH_KNOTS('',3,(#15097,#15098,#15099,#15100,#15101,
#15102,#15103,#15104,#15105,#15106,#15107,#15108,#15109,#15110,#15111,#15112,
#15113,#15114,#15115,#15116,#15117,#15118,#15119,#15120,#15121,#15122,#15123,
#15124,#15125,#15126,#15127,#15128,#15129,#15130,#15131,#15132,#15133,#15134,
#15135,#15136,#15137,#15138,#15139,#15140,#15141,#15142,#15143,#15144,#15145,
#15146,#15147,#15148,#15149,#15150,#15151,#15152,#15153,#15154,#15155,#15156,
#15157,#15158,#15159,#15160,#15161,#15162,#15163,#15164,#15165,#15166,#15167,
#15168,#15169,#15170,#15171,#15172,#15173,#15174,#15175,#15176,#15177,#15178,
#15179,#15180,#15181,#15182,#15183,#15184,#15185,#15186,#15187,#15188,#15189,
#15190,#15191,#15192,#15193,#15194,#15195,#15196,#15197,#15198,#15199,#15200,
#15201,#15202,#15203,#15204,#15205,#15206,#15207,#15208,#15209,#15210,#15211,
#15212,#15213,#15214,#15215,#15216,#15217,#15218,#15219,#15220,#15221,#15222,
#15223,#15224,#15225,#15226,#15227,#15228,#15229,#15230,#15231,#15232,#15233,
#15234,#15235,#15236,#15237,#15238,#15239,#15240,#15241,#15242,#15243,#15244,
#15245,#15246,#15247,#15248,#15249,#15250,#15251,#15252,#15253,#15254,#15255,
#15256,#15257,#15258,#15259,#15260,#15261,#15262,#15263,#15264,#15265,#15266,
#15267,#15268,#15269,#15270,#15271,#15272,#15273,#15274,#15275,#15276,#15277,
#15278,#15279,#15280,#15281,#15282,#15283,#15284,#15285,#15286,#15287,#15288,
#15289,#15290,#15291,#15292,#15293,#15294,#15295,#15296,#15297,#15298),
 .UNSPECIFIED.,.F.,.F.,(4,3,3,3,3,3,3,3,3,3,3,3,3,3,3,3,3,3,3,3,3,3,3,3,
3,3,3,3,3,3,3,3,3,3,3,3,3,3,3,3,3,3,3,3,3,3,3,3,3,3,3,3,3,3,3,3,3,3,3,3,
3,3,3,3,3,3,3,4),(0.,0.000340175691735185,0.000675474340953183,0.00101808855394696,
0.00136070276694074,0.00167669716890443,0.00171086518500347,0.00196577589295814,
0.00226595430547292,0.00252797514521974,0.00256629777750519,0.00286050548522501,
0.00299401407375605,0.0031748036777214,0.00335423798418269,0.00342173037000691,
0.00408388793721925,0.00427716296250863,0.00444284813951019,0.00452758478188326,
0.00469321101548466,0.00470487925875949,0.00501526856889436,0.00513259555501034,
0.00539687869229736,0.00552086330798511,0.00580159241745631,0.00598802814751206,
0.00629385847569466,0.00659968880387725,0.00684346074001378,0.00715186160191428,
0.00746782759000774,0.00769889333251549,0.00803469603381836,0.00837663399754488,
0.00855432592501721,0.0089155447774318,0.00917831546395288,0.00950363410224399,
0.00984133208955611,0.00993830453848906,0.0102651911100207,0.0107425161623785,
0.0112282340743661,0.0117224019296413,0.0119760562950241,0.0124966589117128,
0.0131154536646652,0.0136869214800275,0.0144195285788496,0.015146314613406,
0.0158818322443608,0.0166173498753156,0.0171086518500344,0.0176708895680441,
0.0177821681188111,0.0188947601276208,0.0189922862057886,0.0201663710327867,
0.0205303822200413,0.0215582587898393,0.0228151166104153,0.0239521125900482,
0.0243404099042828,0.0256629777750517,0.0265883729594407,0.0273738429600551),
 .UNSPECIFIED.);
#566=B_SPLINE_CURVE_WITH_KNOTS('',3,(#15300,#15301,#15302,#15303,#15304,
#15305,#15306,#15307,#15308,#15309,#15310,#15311,#15312,#15313,#15314,#15315,
#15316,#15317,#15318,#15319,#15320,#15321,#15322,#15323,#15324,#15325,#15326,
#15327,#15328,#15329,#15330,#15331,#15332,#15333,#15334,#15335,#15336,#15337,
#15338,#15339,#15340,#15341,#15342,#15343,#15344,#15345,#15346,#15347,#15348,
#15349,#15350,#15351,#15352,#15353,#15354,#15355,#15356,#15357,#15358,#15359,
#15360,#15361,#15362,#15363,#15364,#15365,#15366,#15367,#15368,#15369,#15370,
#15371,#15372,#15373,#15374,#15375,#15376,#15377,#15378,#15379,#15380,#15381,
#15382,#15383,#15384,#15385,#15386,#15387,#15388,#15389,#15390,#15391,#15392,
#15393,#15394,#15395,#15396,#15397,#15398,#15399,#15400,#15401,#15402,#15403,
#15404,#15405,#15406,#15407,#15408,#15409,#15410,#15411,#15412,#15413,#15414,
#15415,#15416,#15417,#15418,#15419,#15420,#15421,#15422,#15423,#15424,#15425,
#15426,#15427,#15428,#15429,#15430,#15431,#15432,#15433,#15434,#15435,#15436,
#15437,#15438,#15439,#15440,#15441,#15442,#15443,#15444,#15445,#15446,#15447,
#15448,#15449,#15450,#15451,#15452,#15453,#15454,#15455,#15456,#15457,#15458,
#15459,#15460,#15461,#15462,#15463,#15464,#15465,#15466,#15467,#15468,#15469,
#15470,#15471,#15472,#15473,#15474,#15475,#15476,#15477,#15478,#15479,#15480,
#15481,#15482,#15483,#15484,#15485,#15486,#15487,#15488,#15489,#15490,#15491,
#15492,#15493,#15494,#15495,#15496,#15497,#15498,#15499,#15500,#15501),
 .UNSPECIFIED.,.F.,.F.,(4,3,3,3,3,3,3,3,3,3,3,3,3,3,3,3,3,3,3,3,3,3,3,3,
3,3,3,3,3,3,3,3,3,3,3,3,3,3,3,3,3,3,3,3,3,3,3,3,3,3,3,3,3,3,3,3,3,3,3,3,
3,3,3,3,3,3,3,4),(-4.12191685327121E-5,0.00134365323327312,0.00266981737417628,
0.00298526322249882,0.0042758199183551,0.00549924207753177,0.00576110409467799,
0.0067865453003314,0.00795794545576501,0.00832117904489857,0.0094313041967944,
0.00952851739737183,0.0100894715329932,0.0102004275347635,0.0106906600420225,
0.0114215724738158,0.0121474549948729,0.0128808823820342,0.0136143097691955,
0.0142316850267863,0.0148018855520596,0.0153212508864116,0.0158152842107737,
0.0163008195651895,0.0165519989006371,0.0170281920036276,0.0173543633216557,
0.0176922781173,0.0180175516899865,0.0181126066147906,0.0184729983898973,
0.0187351331208436,0.0190770274958923,0.0194127390567275,0.0195886036794517,
0.0199052822990516,0.0202139762108961,0.0204420742380597,0.0206853098848451,
0.0209904273407564,0.0212955447966677,0.0215756224355253,0.0217616571699925,
0.0220253282929461,0.0221490153552757,0.0222660905809035,0.0225757506345797,
0.0227409940235605,0.0227526541063417,0.0229179562787235,0.0230024859138837,
0.0236631190939991,0.0238559564724917,0.0240349050279617,0.0242151179796911,
0.0242826917517957,0.024576223221583,0.0247094270310997,0.0247476705064236,
0.0250471595594179,0.0253085783382894,0.0255628975897077,0.0258781659521826,
0.025912261569786,0.0262516558540705,0.0265849804311658,0.0269274095690448,
0.0272698387069238),.UNSPECIFIED.);
#567=B_SPLINE_CURVE_WITH_KNOTS('',3,(#15503,#15504,#15505,#15506,#15507,
#15508,#15509,#15510,#15511,#15512,#15513,#15514,#15515,#15516,#15517,#15518,
#15519,#15520,#15521,#15522,#15523,#15524,#15525,#15526,#15527,#15528,#15529,
#15530,#15531,#15532,#15533,#15534,#15535,#15536,#15537,#15538,#15539,#15540,
#15541,#15542,#15543,#15544,#15545,#15546,#15547,#15548,#15549,#15550,#15551,
#15552,#15553,#15554,#15555,#15556,#15557,#15558,#15559,#15560,#15561,#15562,
#15563,#15564,#15565,#15566,#15567,#15568,#15569,#15570,#15571,#15572,#15573,
#15574,#15575,#15576,#15577,#15578,#15579,#15580,#15581,#15582,#15583,#15584,
#15585,#15586,#15587,#15588,#15589,#15590,#15591,#15592,#15593,#15594,#15595,
#15596,#15597,#15598,#15599),.UNSPECIFIED.,.F.,.F.,(4,3,3,3,3,3,3,3,3,3,
3,3,3,3,3,3,3,3,3,3,3,3,3,3,3,3,3,3,3,3,3,3,4),(0.,0.000237157711333885,
0.000465955627071617,0.000692471694688221,0.00101215149057648,0.00133755096760822,
0.00138494338937644,0.00154502472927642,0.00172378677637225,0.00190060093021846,
0.00207741508406466,0.00218381987505132,0.00244036367639352,0.00248194620057247,
0.00270340866436264,0.00276988677875289,0.00277353313349095,0.0030435391747074,
0.003116122626097,0.00324814486575857,0.00338255162160067,0.00346235847344111,
0.00364324318024271,0.00382965963813554,0.00399772979477703,0.00415483016812933,
0.00436117928878065,0.00457177672492627,0.0047886688078585,0.00484730186281755,
0.00507760552343842,0.00531594990564191,0.00553977355750578),
 .UNSPECIFIED.);
#568=B_SPLINE_CURVE_WITH_KNOTS('',3,(#15600,#15601,#15602,#15603,#15604,
#15605,#15606,#15607,#15608,#15609,#15610,#15611,#15612,#15613,#15614,#15615,
#15616,#15617,#15618,#15619,#15620,#15621,#15622,#15623,#15624,#15625,#15626,
#15627,#15628,#15629,#15630,#15631,#15632,#15633,#15634,#15635,#15636,#15637,
#15638,#15639,#15640,#15641,#15642,#15643,#15644,#15645,#15646,#15647,#15648,
#15649,#15650,#15651,#15652,#15653,#15654,#15655,#15656,#15657,#15658,#15659,
#15660,#15661,#15662,#15663,#15664,#15665,#15666,#15667,#15668,#15669,#15670,
#15671,#15672,#15673,#15674,#15675,#15676,#15677,#15678,#15679,#15680,#15681,
#15682,#15683,#15684,#15685,#15686,#15687,#15688,#15689,#15690,#15691,#15692,
#15693,#15694,#15695,#15696,#15697,#15698,#15699,#15700,#15701,#15702,#15703,
#15704,#15705,#15706,#15707,#15708,#15709,#15710,#15711,#15712,#15713,#15714,
#15715,#15716,#15717,#15718,#15719,#15720,#15721,#15722,#15723,#15724,#15725,
#15726,#15727,#15728,#15729,#15730,#15731,#15732,#15733,#15734,#15735,#15736,
#15737,#15738,#15739,#15740,#15741,#15742,#15743,#15744,#15745,#15746,#15747,
#15748,#15749,#15750,#15751,#15752,#15753,#15754,#15755,#15756,#15757,#15758,
#15759,#15760,#15761,#15762,#15763,#15764,#15765,#15766,#15767,#15768,#15769,
#15770,#15771,#15772,#15773,#15774,#15775,#15776,#15777,#15778,#15779,#15780,
#15781,#15782,#15783,#15784,#15785,#15786,#15787,#15788,#15789,#15790,#15791,
#15792,#15793,#15794,#15795,#15796,#15797,#15798,#15799,#15800,#15801),
 .UNSPECIFIED.,.F.,.F.,(4,3,3,3,3,3,3,3,3,3,3,3,3,3,3,3,3,3,3,3,3,3,3,3,
3,3,3,3,3,3,3,3,3,3,3,3,3,3,3,3,3,3,3,3,3,3,3,3,3,3,3,3,3,3,3,3,3,3,3,3,
3,3,3,3,3,3,3,4),(0.,0.000340175691736026,0.000675474341465466,0.00101808855420478,
0.0013607027669441,0.00167669716893931,0.0017108651850034,0.00196577589296195,
0.00226595430562214,0.00252797514522077,0.00256629777750511,0.00286050548518003,
0.00299401407375597,0.00317480367773506,0.00335423798419973,0.00342173037000683,
0.00408388793877329,0.00427716296250855,0.00444284813951406,0.00452758478188384,
0.00469321101548644,0.00470487925875941,0.00501526856889609,0.00513259555501027,
0.0053968786924259,0.00552086330798684,0.00580159241725754,0.00598802814751199,
0.00629385847569525,0.00659968880387851,0.00684346074001371,0.00715186160180756,
0.00746782758975846,0.00769889333251542,0.00803469603398907,0.00837663399785215,
0.00855432592501714,0.00891554477746769,0.00917831546395363,0.0095036341029607,
0.0098413320909301,0.00993830453849759,0.0102651911100206,0.010742516162387,
0.0112282340744698,0.0117224019298567,0.011976056295024,0.0124966589117161,
0.013115453665662,0.0136869214800275,0.0144195285788502,0.0151463146137948,
0.0158818322445567,0.0166173498753185,0.0171086518500343,0.017670889568476,
0.0177821681188137,0.0188947601244791,0.0189922862057895,0.0201663710329349,
0.0205303822200412,0.0215582587898413,0.0228151166108405,0.023952112590048,
0.0243404099042828,0.0256629777750514,0.0265883729179494,0.0273738429600549),
 .UNSPECIFIED.);
#569=B_SPLINE_CURVE_WITH_KNOTS('',3,(#15803,#15804,#15805,#15806,#15807,
#15808,#15809,#15810,#15811,#15812,#15813,#15814,#15815,#15816,#15817,#15818,
#15819,#15820,#15821,#15822,#15823,#15824,#15825,#15826,#15827,#15828,#15829,
#15830,#15831,#15832,#15833,#15834,#15835,#15836,#15837,#15838,#15839,#15840,
#15841,#15842,#15843,#15844,#15845,#15846,#15847,#15848,#15849,#15850,#15851,
#15852,#15853,#15854,#15855,#15856,#15857,#15858,#15859,#15860,#15861,#15862,
#15863,#15864,#15865,#15866,#15867,#15868,#15869,#15870,#15871,#15872,#15873,
#15874,#15875,#15876,#15877,#15878,#15879,#15880,#15881,#15882,#15883,#15884,
#15885,#15886,#15887,#15888,#15889,#15890,#15891,#15892,#15893,#15894,#15895,
#15896,#15897,#15898,#15899,#15900,#15901,#15902,#15903,#15904,#15905,#15906,
#15907,#15908,#15909,#15910,#15911,#15912,#15913,#15914,#15915,#15916,#15917,
#15918,#15919,#15920,#15921,#15922,#15923,#15924,#15925,#15926,#15927,#15928,
#15929,#15930,#15931,#15932,#15933,#15934,#15935,#15936,#15937,#15938,#15939,
#15940,#15941,#15942,#15943,#15944,#15945,#15946,#15947,#15948,#15949,#15950,
#15951,#15952,#15953,#15954,#15955,#15956,#15957,#15958,#15959,#15960,#15961,
#15962,#15963,#15964,#15965,#15966,#15967,#15968,#15969,#15970,#15971,#15972,
#15973,#15974,#15975,#15976,#15977,#15978,#15979,#15980,#15981,#15982,#15983,
#15984,#15985,#15986,#15987,#15988,#15989,#15990,#15991,#15992,#15993,#15994,
#15995,#15996,#15997,#15998,#15999,#16000,#16001,#16002,#16003,#16004),
 .UNSPECIFIED.,.F.,.F.,(4,3,3,3,3,3,3,3,3,3,3,3,3,3,3,3,3,3,3,3,3,3,3,3,
3,3,3,3,3,3,3,3,3,3,3,3,3,3,3,3,3,3,3,3,3,3,3,3,3,3,3,3,3,3,3,3,3,3,3,3,
3,3,3,3,3,3,3,4),(-4.12191685326785E-5,0.00134365322910891,0.00266981736923567,
0.0029852632224583,0.00427581991812639,0.00549924207859078,0.00576110409467375,
0.00678654530033131,0.00795794545614227,0.00832117904489245,0.00943130419171935,
0.00952851739736535,0.0100894715305543,0.0102004275347633,0.0106906600420251,
0.0114215724738176,0.0121474549939761,0.0128808823815857,0.0136143097691953,
0.0142316850264925,0.0148018855520585,0.0153212508864113,0.0158152842110432,
0.0163008195657759,0.0165519989006382,0.0170281920036273,0.0173543633216574,
0.0176922781166802,0.0180175516886633,0.0181126066147891,0.0184729983898273,
0.0187351331208433,0.0190770274957655,0.0194127390564447,0.0195886036794513,
0.0199052822991559,0.0202139762110683,0.0204420742380593,0.0206853098848451,
0.0209904273407562,0.0212955447966673,0.0215756224361278,0.0217616571699925,
0.0220253282935128,0.0221490153552753,0.0222660905809034,0.0225757506345793,
0.0227409940235518,0.0227526541063411,0.0229179562787035,0.0230024859138833,
0.0236631190935958,0.0238559564724913,0.0240349050279607,0.024215117979687,
0.0242826917517953,0.0245762232216197,0.0247094270310993,0.0247476705064231,
0.0250471595592009,0.0253085783382907,0.0255628975897073,0.0258781659535221,
0.0259122615697878,0.0262516558540717,0.0265849804309141,0.0269274095689187,
0.0272698387069233),.UNSPECIFIED.);
#570=B_SPLINE_CURVE_WITH_KNOTS('',3,(#16005,#16006,#16007,#16008,#16009,
#16010,#16011,#16012,#16013,#16014,#16015,#16016,#16017,#16018,#16019,#16020,
#16021,#16022,#16023,#16024,#16025,#16026,#16027,#16028,#16029,#16030,#16031,
#16032,#16033,#16034,#16035,#16036,#16037,#16038,#16039,#16040,#16041,#16042,
#16043,#16044,#16045,#16046,#16047,#16048,#16049,#16050,#16051,#16052,#16053),
 .UNSPECIFIED.,.F.,.F.,(4,3,3,3,3,3,3,3,3,3,3,3,3,3,3,3,4),(0.,0.000236842439941471,
0.000465418231564533,0.0006924716946882,0.00101111078066431,0.00133487521500561,
0.0013849433893764,0.00154319593245401,0.0017222487783158,0.0018998319311902,
0.0020774150840646,0.00228352041032069,0.00248574199847713,0.00268332977810061,
0.00276807256049863,0.0027698867787528,0.00277080264391651),
 .UNSPECIFIED.);
#571=B_SPLINE_CURVE_WITH_KNOTS('',3,(#16164,#16165,#16166,#16167,#16168,
#16169,#16170,#16171,#16172,#16173,#16174,#16175,#16176,#16177,#16178,#16179,
#16180,#16181,#16182,#16183,#16184,#16185,#16186,#16187),.UNSPECIFIED.,
 .F.,.F.,(4,2,2,2,2,2,2,2,2,2,2,4),(0.,0.000297119359731175,0.00059423871946235,
0.0011884774389247,0.0023769548778494,0.00475390975569881,0.00713086463354823,
0.00950781951139764,0.0142617292670965,0.0166386841449459,0.0178271615838706,
0.0190156390227953),.UNSPECIFIED.);
#572=B_SPLINE_CURVE_WITH_KNOTS('',3,(#16342,#16343,#16344,#16345,#16346,
#16347,#16348,#16349,#16350,#16351,#16352,#16353,#16354,#16355,#16356,#16357,
#16358,#16359,#16360,#16361),.UNSPECIFIED.,.F.,.F.,(4,2,2,2,2,2,2,2,2,4),
(-4.50312400614093E-5,0.00472460449543289,0.00949424023092719,0.0118790580986743,
0.0142638759664215,0.0166486938341686,0.0178411027680422,0.018437307234979,
0.0187354094684474,0.0190335117019158),.UNSPECIFIED.);
#573=B_SPLINE_CURVE_WITH_KNOTS('',3,(#16471,#16472,#16473,#16474,#16475,
#16476,#16477,#16478,#16479,#16480,#16481,#16482,#16483,#16484,#16485,#16486,
#16487,#16488,#16489,#16490),.UNSPECIFIED.,.F.,.F.,(4,2,2,2,2,2,2,2,2,4),
(-4.50312400612699E-5,0.00472460449542813,0.00949424023091753,0.0118790580986622,
0.0142638759664069,0.0166486938341516,0.017841102768024,0.0184373072349602,
0.0187354094684283,0.0190335117018964),.UNSPECIFIED.);
#574=B_SPLINE_CURVE_WITH_KNOTS('',3,(#16646,#16647,#16648,#16649,#16650,
#16651,#16652,#16653,#16654,#16655,#16656,#16657,#16658,#16659,#16660,#16661,
#16662,#16663,#16664,#16665,#16666,#16667,#16668,#16669),.UNSPECIFIED.,
 .F.,.F.,(4,2,2,2,2,2,2,2,2,2,2,4),(8.56187529156079E-17,0.000297119359731277,
0.000594238719462469,0.00118847743892484,0.00237695487784958,0.00475390975569906,
0.00713086463354855,0.00950781951139803,0.014261729267097,0.0166386841449465,
0.0178271615838712,0.019015639022796),.UNSPECIFIED.);
#575=B_SPLINE_CURVE_WITH_KNOTS('',3,(#17026,#17027,#17028,#17029,#17030,
#17031,#17032,#17033,#17034,#17035,#17036,#17037,#17038,#17039,#17040,#17041,
#17042,#17043,#17044,#17045,#17046,#17047,#17048,#17049,#17050,#17051,#17052,
#17053),.UNSPECIFIED.,.F.,.F.,(4,3,3,3,3,3,3,3,3,4),(0.,0.000231294325945477,
0.000464822662229606,0.000605683234682749,0.000808855738910866,0.0010118571627786,
0.0012113664693655,0.00144599958458062,0.00168128722210177,0.0018161530161823),
 .UNSPECIFIED.);
#576=B_SPLINE_CURVE_WITH_KNOTS('',3,(#17054,#17055,#17056,#17057,#17058,
#17059,#17060,#17061,#17062,#17063,#17064,#17065,#17066,#17067,#17068,#17069,
#17070,#17071,#17072,#17073,#17074,#17075,#17076,#17077,#17078,#17079,#17080,
#17081,#17082,#17083,#17084,#17085,#17086,#17087,#17088,#17089,#17090,#17091,
#17092,#17093,#17094,#17095,#17096,#17097,#17098,#17099,#17100,#17101,#17102,
#17103,#17104,#17105,#17106,#17107,#17108,#17109,#17110,#17111,#17112,#17113,
#17114,#17115,#17116,#17117,#17118,#17119,#17120,#17121,#17122,#17123,#17124,
#17125,#17126,#17127,#17128,#17129,#17130,#17131,#17132,#17133,#17134,#17135,
#17136,#17137,#17138,#17139,#17140,#17141,#17142,#17143,#17144,#17145,#17146,
#17147,#17148,#17149,#17150,#17151,#17152,#17153,#17154,#17155,#17156,#17157,
#17158,#17159,#17160,#17161,#17162,#17163,#17164,#17165,#17166,#17167,#17168,
#17169,#17170,#17171,#17172,#17173,#17174,#17175,#17176,#17177,#17178,#17179,
#17180,#17181,#17182,#17183,#17184,#17185,#17186,#17187,#17188,#17189,#17190,
#17191,#17192,#17193,#17194,#17195,#17196,#17197,#17198,#17199,#17200,#17201,
#17202,#17203,#17204,#17205,#17206,#17207,#17208,#17209,#17210,#17211,#17212,
#17213,#17214,#17215,#17216,#17217,#17218,#17219,#17220,#17221,#17222,#17223,
#17224,#17225,#17226,#17227,#17228,#17229,#17230,#17231,#17232,#17233,#17234,
#17235,#17236,#17237,#17238,#17239,#17240,#17241,#17242,#17243,#17244,#17245,
#17246,#17247,#17248,#17249,#17250,#17251,#17252,#17253,#17254,#17255,#17256,
#17257,#17258,#17259,#17260,#17261,#17262,#17263,#17264,#17265,#17266,#17267,
#17268,#17269,#17270,#17271,#17272,#17273,#17274,#17275,#17276,#17277,#17278,
#17279,#17280,#17281,#17282,#17283,#17284,#17285,#17286,#17287,#17288,#17289,
#17290,#17291,#17292,#17293,#17294,#17295,#17296,#17297,#17298,#17299,#17300,
#17301,#17302,#17303,#17304,#17305,#17306,#17307,#17308,#17309,#17310,#17311,
#17312,#17313,#17314,#17315,#17316,#17317,#17318,#17319,#17320,#17321,#17322,
#17323,#17324),.UNSPECIFIED.,.F.,.F.,(4,3,3,3,3,3,3,3,3,3,3,3,3,3,3,3,3,
3,3,3,3,3,3,3,3,3,3,3,3,3,3,3,3,3,3,3,3,3,3,3,3,3,3,3,3,3,3,3,3,3,3,3,3,
3,3,3,3,3,3,3,3,3,3,3,3,3,3,3,3,3,3,3,3,3,3,3,3,3,3,3,3,3,3,3,3,3,3,3,3,
3,4),(0.0018161530161823,0.00181704970404825,0.00200583370208725,0.00219446082802312,
0.00238336003013788,0.00242273293873099,0.00265759191053558,0.00289143223371987,
0.00302841617341374,0.00327576515313478,0.00352338277376447,0.00363409940809649,
0.00391111582115793,0.00418763440557408,0.00423978264277924,0.00447293482787131,
0.00470764138266438,0.00484546587746199,0.00503561213322781,0.00522552979015431,
0.00541560630890245,0.00545114911214474,0.00568628229470434,0.00592131468169729,
0.00605683234682749,0.00625531156903434,0.00645891357527229,0.00666251558151024,
0.00689644101753518,0.00712864478231464,0.00726819881619298,0.00752881290938141,
0.00779301232002778,0.00787388205087573,0.00808290763071909,0.00829174641109551,
0.00847956528555848,0.00871398900637753,0.00894924091999715,0.00908524852024123,
0.00927328004700098,0.00946113685411365,0.0096492486498554,0.00969093175492398,
0.00992591903218147,0.0101600600236151,0.0102966149896067,0.0105267869044746,
0.0107572068987285,0.0109022982242895,0.0112461276330547,0.0115079814589722,
0.0117407454265451,0.0119752296007021,0.012113664693655,0.0123056711978274,
0.0124974413983672,0.0126893421942621,0.0127193479283377,0.0129544208220635,
0.0131895714004269,0.0133250311630205,0.0135200587949984,0.0137150013702892,
0.0139102531895133,0.0139307143977032,0.0141649164284798,0.0143975585284212,
0.014536397632386,0.0148611323777672,0.0151420808670687,0.0153588623255755,
0.0155754441480225,0.0157477641017515,0.0159819424694056,0.0162171239137906,
0.0163534473364342,0.0165412047623366,0.0167287716064859,0.0169165741256843,
0.016959130571117,0.017194210781073,0.0174286191974533,0.0175648138057997,
0.0177834673516284,0.0180023569372318,0.0181704970404825,0.0184733386578238,
0.0187705466100904,0.0190762050599692,0.019381863509848),.UNSPECIFIED.);
#577=B_SPLINE_CURVE_WITH_KNOTS('',3,(#17327,#17328,#17329,#17330,#17331,
#17332,#17333,#17334,#17335,#17336,#17337,#17338,#17339,#17340,#17341,#17342,
#17343,#17344,#17345,#17346,#17347,#17348,#17349,#17350,#17351,#17352,#17353,
#17354,#17355,#17356,#17357,#17358,#17359,#17360,#17361,#17362,#17363,#17364,
#17365,#17366,#17367,#17368,#17369,#17370,#17371,#17372,#17373,#17374,#17375,
#17376,#17377,#17378,#17379,#17380,#17381,#17382,#17383,#17384,#17385,#17386,
#17387,#17388,#17389,#17390,#17391,#17392,#17393,#17394,#17395,#17396,#17397,
#17398,#17399,#17400,#17401,#17402,#17403,#17404,#17405,#17406,#17407,#17408,
#17409,#17410,#17411,#17412,#17413,#17414,#17415,#17416,#17417,#17418,#17419,
#17420,#17421,#17422,#17423,#17424,#17425,#17426,#17427,#17428,#17429,#17430,
#17431,#17432,#17433,#17434,#17435,#17436,#17437,#17438,#17439,#17440,#17441,
#17442,#17443,#17444,#17445,#17446,#17447,#17448,#17449,#17450,#17451,#17452,
#17453,#17454,#17455,#17456,#17457,#17458,#17459,#17460,#17461,#17462,#17463,
#17464,#17465,#17466,#17467,#17468,#17469,#17470,#17471,#17472,#17473,#17474,
#17475,#17476,#17477,#17478,#17479,#17480,#17481,#17482,#17483,#17484,#17485,
#17486,#17487,#17488,#17489,#17490,#17491,#17492,#17493,#17494,#17495,#17496,
#17497,#17498,#17499,#17500,#17501,#17502,#17503,#17504,#17505,#17506,#17507,
#17508,#17509,#17510,#17511,#17512,#17513,#17514,#17515,#17516,#17517,#17518,
#17519,#17520,#17521,#17522,#17523,#17524,#17525,#17526,#17527,#17528,#17529,
#17530,#17531,#17532,#17533,#17534,#17535,#17536,#17537,#17538,#17539,#17540,
#17541,#17542,#17543,#17544,#17545,#17546,#17547,#17548,#17549,#17550,#17551,
#17552,#17553,#17554,#17555,#17556,#17557,#17558,#17559,#17560,#17561,#17562,
#17563,#17564,#17565,#17566,#17567,#17568,#17569,#17570,#17571,#17572,#17573,
#17574,#17575,#17576,#17577,#17578,#17579,#17580,#17581,#17582,#17583,#17584,
#17585,#17586,#17587,#17588,#17589,#17590,#17591,#17592,#17593,#17594,#17595,
#17596,#17597,#17598,#17599,#17600,#17601,#17602,#17603),.UNSPECIFIED.,
 .F.,.F.,(4,3,3,3,3,3,3,3,3,3,3,3,3,3,3,3,3,3,3,3,3,3,3,3,3,3,3,3,3,3,3,
3,3,3,3,3,3,3,3,3,3,3,3,3,3,3,3,3,3,3,3,3,3,3,3,3,3,3,3,3,3,3,3,3,3,3,3,
3,3,3,3,3,3,3,3,3,3,3,3,3,3,3,3,3,3,3,3,3,3,3,3,3,4),(0.,0.000231293909478829,
0.000464821929767556,0.00060568320508766,0.000808857863905471,0.00101186144647658,
0.00121136641017532,0.00144600104230718,0.00168128763074085,0.00181704961526298,
0.00200583317153906,0.00219445983447999,0.00238335854916359,0.00242273282035064,
0.00265759194929965,0.00289143243005884,0.0030284160254383,0.003275743635374,
0.00352333983374325,0.00363409923052596,0.00391114756596992,0.00418769750088776,
0.00423978243561362,0.00447293416717338,0.00470764050251022,0.00484546564070128,
0.00503561332151353,0.00522553241631793,0.00541561037723325,0.00545114884578894,
0.0056862816780372,0.00592131384823276,0.0060568320508766,0.00625531070847705,
0.00645891298222066,0.00666251525596426,0.00689644055875581,0.00712864418863787,
0.00726819846105192,0.00752884048815537,0.00779306949700858,0.00787388166613958,
0.00808291222402555,0.00829175595352107,0.00847956487122724,0.00871398849583979,
0.00894924051298378,0.0090852480763149,0.00927327916167684,0.00946113552646327,
0.0096492468822708,0.00969093128140256,0.00992591855977248,0.0101600597593885,
0.0102966144864902,0.0105267831616192,0.0107571999178322,0.0109022976915779,
0.0112461788451932,0.0115079808966655,0.0117407448529832,0.0119752289995473,
0.0121136641017532,0.0123056716422985,0.0124974428571561,0.0126893446268732,
0.0127193473068409,0.0129544204495954,0.0131895713760254,0.0133250305119285,
0.0135200544620049,0.0137149933329001,0.0139102414502059,0.0139307137170162,
0.0141649161753979,0.0143975589201434,0.0145363969221038,0.0148611855057929,
0.0151420801271915,0.0153588661585815,0.0155754525660823,0.0157477633322792,
0.0159819413893676,0.0162171225409267,0.0163534465373668,0.0165412039988469,
0.016728770858437,0.0169165733652975,0.0169591297424545,0.0171942100555913,
0.0174286185839122,0.0175648129475421,0.0175712098172771),.UNSPECIFIED.);
#578=B_SPLINE_CURVE_WITH_KNOTS('',3,(#17604,#17605,#17606,#17607,#17608,
#17609,#17610,#17611,#17612,#17613,#17614,#17615,#17616,#17617,#17618,#17619,
#17620,#17621,#17622,#17623,#17624,#17625),.UNSPECIFIED.,.F.,.F.,(4,3,3,
3,3,3,3,4),(0.0175712098172771,0.0177898520948126,0.0180087321653697,0.0181704961526298,
0.0184733377551736,0.0187705437287487,0.0190762031457769,0.0193818625628051),
 .UNSPECIFIED.);
#753=PLANE('',#10389);
#754=PLANE('',#10390);
#755=PLANE('',#10391);
#756=PLANE('',#10392);
#757=PLANE('',#10393);
#758=PLANE('',#10394);
#759=PLANE('',#10395);
#760=PLANE('',#10396);
#761=PLANE('',#10397);
#762=PLANE('',#10398);
#763=PLANE('',#10399);
#764=PLANE('',#10400);
#765=PLANE('',#10401);
#766=PLANE('',#10402);
#767=PLANE('',#10403);
#768=PLANE('',#10404);
#769=PLANE('',#10405);
#770=PLANE('',#10406);
#771=PLANE('',#10407);
#772=PLANE('',#10408);
#773=PLANE('',#10409);
#774=PLANE('',#10410);
#775=PLANE('',#10411);
#776=PLANE('',#10412);
#777=PLANE('',#10413);
#778=PLANE('',#10414);
#779=PLANE('',#10415);
#780=PLANE('',#10416);
#781=PLANE('',#10417);
#782=PLANE('',#10418);
#783=PLANE('',#10419);
#784=PLANE('',#10420);
#785=PLANE('',#10421);
#786=PLANE('',#10422);
#787=PLANE('',#10423);
#788=PLANE('',#10424);
#789=PLANE('',#10425);
#790=PLANE('',#10426);
#791=PLANE('',#10427);
#792=PLANE('',#10428);
#793=PLANE('',#10429);
#794=PLANE('',#10430);
#795=PLANE('',#10431);
#796=PLANE('',#10432);
#797=PLANE('',#10433);
#798=PLANE('',#10434);
#799=PLANE('',#10435);
#800=PLANE('',#10436);
#801=PLANE('',#10437);
#802=PLANE('',#10438);
#803=PLANE('',#10439);
#804=PLANE('',#10440);
#805=PLANE('',#10441);
#806=PLANE('',#10442);
#807=PLANE('',#10443);
#808=PLANE('',#10444);
#809=PLANE('',#10445);
#810=PLANE('',#10446);
#811=PLANE('',#10447);
#812=PLANE('',#10448);
#813=PLANE('',#10449);
#814=PLANE('',#10450);
#815=PLANE('',#10451);
#816=PLANE('',#10452);
#817=PLANE('',#10453);
#818=PLANE('',#10454);
#819=PLANE('',#10455);
#820=PLANE('',#10456);
#821=PLANE('',#10457);
#822=PLANE('',#10458);
#823=PLANE('',#10459);
#824=PLANE('',#10460);
#825=PLANE('',#10461);
#826=PLANE('',#10462);
#827=PLANE('',#10463);
#828=PLANE('',#10464);
#829=PLANE('',#10465);
#830=PLANE('',#10466);
#831=PLANE('',#10467);
#832=PLANE('',#10468);
#833=PLANE('',#10472);
#834=PLANE('',#10474);
#835=PLANE('',#10489);
#836=PLANE('',#10500);
#837=PLANE('',#10512);
#838=PLANE('',#10513);
#839=PLANE('',#10514);
#840=PLANE('',#10515);
#841=PLANE('',#10516);
#842=PLANE('',#10517);
#1020=FACE_OUTER_BOUND('',#1576,.T.);
#1021=FACE_OUTER_BOUND('',#1577,.T.);
#1022=FACE_OUTER_BOUND('',#1578,.T.);
#1023=FACE_OUTER_BOUND('',#1579,.T.);
#1024=FACE_OUTER_BOUND('',#1580,.T.);
#1025=FACE_OUTER_BOUND('',#1581,.T.);
#1026=FACE_OUTER_BOUND('',#1582,.T.);
#1027=FACE_OUTER_BOUND('',#1583,.T.);
#1028=FACE_OUTER_BOUND('',#1584,.T.);
#1029=FACE_OUTER_BOUND('',#1585,.T.);
#1030=FACE_OUTER_BOUND('',#1586,.T.);
#1031=FACE_OUTER_BOUND('',#1587,.T.);
#1032=FACE_OUTER_BOUND('',#1588,.T.);
#1033=FACE_OUTER_BOUND('',#1589,.T.);
#1034=FACE_OUTER_BOUND('',#1590,.T.);
#1035=FACE_OUTER_BOUND('',#1591,.T.);
#1036=FACE_OUTER_BOUND('',#1592,.T.);
#1037=FACE_OUTER_BOUND('',#1593,.T.);
#1038=FACE_OUTER_BOUND('',#1594,.T.);
#1039=FACE_OUTER_BOUND('',#1595,.T.);
#1040=FACE_OUTER_BOUND('',#1596,.T.);
#1041=FACE_OUTER_BOUND('',#1597,.T.);
#1042=FACE_OUTER_BOUND('',#1598,.T.);
#1043=FACE_OUTER_BOUND('',#1599,.T.);
#1044=FACE_OUTER_BOUND('',#1600,.T.);
#1045=FACE_OUTER_BOUND('',#1601,.T.);
#1046=FACE_OUTER_BOUND('',#1602,.T.);
#1047=FACE_OUTER_BOUND('',#1603,.T.);
#1048=FACE_OUTER_BOUND('',#1604,.T.);
#1049=FACE_OUTER_BOUND('',#1605,.T.);
#1050=FACE_OUTER_BOUND('',#1606,.T.);
#1051=FACE_OUTER_BOUND('',#1607,.T.);
#1052=FACE_OUTER_BOUND('',#1608,.T.);
#1053=FACE_OUTER_BOUND('',#1609,.T.);
#1054=FACE_OUTER_BOUND('',#1610,.T.);
#1055=FACE_OUTER_BOUND('',#1611,.T.);
#1056=FACE_OUTER_BOUND('',#1612,.T.);
#1057=FACE_OUTER_BOUND('',#1613,.T.);
#1058=FACE_OUTER_BOUND('',#1614,.T.);
#1059=FACE_OUTER_BOUND('',#1615,.T.);
#1060=FACE_OUTER_BOUND('',#1616,.T.);
#1061=FACE_OUTER_BOUND('',#1617,.T.);
#1062=FACE_OUTER_BOUND('',#1618,.T.);
#1063=FACE_OUTER_BOUND('',#1619,.T.);
#1064=FACE_OUTER_BOUND('',#1620,.T.);
#1065=FACE_OUTER_BOUND('',#1621,.T.);
#1066=FACE_OUTER_BOUND('',#1622,.T.);
#1067=FACE_OUTER_BOUND('',#1623,.T.);
#1068=FACE_OUTER_BOUND('',#1624,.T.);
#1069=FACE_OUTER_BOUND('',#1625,.T.);
#1070=FACE_OUTER_BOUND('',#1626,.T.);
#1071=FACE_OUTER_BOUND('',#1627,.T.);
#1072=FACE_OUTER_BOUND('',#1628,.T.);
#1073=FACE_OUTER_BOUND('',#1629,.T.);
#1074=FACE_OUTER_BOUND('',#1630,.T.);
#1075=FACE_OUTER_BOUND('',#1631,.T.);
#1076=FACE_OUTER_BOUND('',#1632,.T.);
#1077=FACE_OUTER_BOUND('',#1633,.T.);
#1078=FACE_OUTER_BOUND('',#1634,.T.);
#1079=FACE_OUTER_BOUND('',#1635,.T.);
#1080=FACE_OUTER_BOUND('',#1636,.T.);
#1081=FACE_OUTER_BOUND('',#1637,.T.);
#1082=FACE_OUTER_BOUND('',#1638,.T.);
#1083=FACE_OUTER_BOUND('',#1639,.T.);
#1084=FACE_OUTER_BOUND('',#1640,.T.);
#1085=FACE_OUTER_BOUND('',#1641,.T.);
#1086=FACE_OUTER_BOUND('',#1642,.T.);
#1087=FACE_OUTER_BOUND('',#1643,.T.);
#1088=FACE_OUTER_BOUND('',#1644,.T.);
#1089=FACE_OUTER_BOUND('',#1645,.T.);
#1090=FACE_OUTER_BOUND('',#1646,.T.);
#1091=FACE_OUTER_BOUND('',#1647,.T.);
#1092=FACE_OUTER_BOUND('',#1648,.T.);
#1093=FACE_OUTER_BOUND('',#1649,.T.);
#1094=FACE_OUTER_BOUND('',#1650,.T.);
#1095=FACE_OUTER_BOUND('',#1651,.T.);
#1096=FACE_OUTER_BOUND('',#1652,.T.);
#1097=FACE_OUTER_BOUND('',#1653,.T.);
#1098=FACE_OUTER_BOUND('',#1654,.T.);
#1099=FACE_OUTER_BOUND('',#1655,.T.);
#1100=FACE_OUTER_BOUND('',#1656,.T.);
#1101=FACE_OUTER_BOUND('',#1657,.T.);
#1102=FACE_OUTER_BOUND('',#1658,.T.);
#1103=FACE_OUTER_BOUND('',#1659,.T.);
#1104=FACE_OUTER_BOUND('',#1660,.T.);
#1105=FACE_OUTER_BOUND('',#1661,.T.);
#1106=FACE_OUTER_BOUND('',#1662,.T.);
#1107=FACE_OUTER_BOUND('',#1663,.T.);
#1108=FACE_OUTER_BOUND('',#1664,.T.);
#1109=FACE_OUTER_BOUND('',#1665,.T.);
#1110=FACE_OUTER_BOUND('',#1666,.T.);
#1111=FACE_OUTER_BOUND('',#1667,.T.);
#1112=FACE_OUTER_BOUND('',#1668,.T.);
#1113=FACE_OUTER_BOUND('',#1669,.T.);
#1114=FACE_OUTER_BOUND('',#1670,.T.);
#1115=FACE_OUTER_BOUND('',#1671,.T.);
#1116=FACE_OUTER_BOUND('',#1672,.T.);
#1117=FACE_OUTER_BOUND('',#1673,.T.);
#1118=FACE_OUTER_BOUND('',#1674,.T.);
#1119=FACE_OUTER_BOUND('',#1675,.T.);
#1120=FACE_OUTER_BOUND('',#1676,.T.);
#1121=FACE_OUTER_BOUND('',#1677,.T.);
#1122=FACE_OUTER_BOUND('',#1678,.T.);
#1123=FACE_OUTER_BOUND('',#1679,.T.);
#1124=FACE_OUTER_BOUND('',#1680,.T.);
#1125=FACE_OUTER_BOUND('',#1681,.T.);
#1126=FACE_OUTER_BOUND('',#1682,.T.);
#1127=FACE_OUTER_BOUND('',#1683,.T.);
#1128=FACE_OUTER_BOUND('',#1684,.T.);
#1129=FACE_OUTER_BOUND('',#1685,.T.);
#1130=FACE_OUTER_BOUND('',#1686,.T.);
#1131=FACE_OUTER_BOUND('',#1687,.T.);
#1132=FACE_OUTER_BOUND('',#1688,.T.);
#1133=FACE_OUTER_BOUND('',#1689,.T.);
#1134=FACE_OUTER_BOUND('',#1690,.T.);
#1135=FACE_OUTER_BOUND('',#1691,.T.);
#1136=FACE_OUTER_BOUND('',#1692,.T.);
#1137=FACE_OUTER_BOUND('',#1693,.T.);
#1138=FACE_OUTER_BOUND('',#1694,.T.);
#1139=FACE_OUTER_BOUND('',#1695,.T.);
#1140=FACE_OUTER_BOUND('',#1696,.T.);
#1141=FACE_OUTER_BOUND('',#1697,.T.);
#1142=FACE_OUTER_BOUND('',#1699,.T.);
#1143=FACE_OUTER_BOUND('',#1701,.T.);
#1144=FACE_OUTER_BOUND('',#1702,.T.);
#1145=FACE_OUTER_BOUND('',#1703,.T.);
#1146=FACE_OUTER_BOUND('',#1704,.T.);
#1147=FACE_OUTER_BOUND('',#1705,.T.);
#1148=FACE_OUTER_BOUND('',#1706,.T.);
#1149=FACE_OUTER_BOUND('',#1707,.T.);
#1150=FACE_OUTER_BOUND('',#1708,.T.);
#1151=FACE_OUTER_BOUND('',#1709,.T.);
#1152=FACE_OUTER_BOUND('',#1711,.T.);
#1153=FACE_OUTER_BOUND('',#1712,.T.);
#1154=FACE_OUTER_BOUND('',#1713,.T.);
#1155=FACE_OUTER_BOUND('',#1714,.T.);
#1156=FACE_OUTER_BOUND('',#1715,.T.);
#1157=FACE_OUTER_BOUND('',#1716,.T.);
#1158=FACE_OUTER_BOUND('',#1717,.T.);
#1159=FACE_OUTER_BOUND('',#1718,.T.);
#1160=FACE_OUTER_BOUND('',#1719,.T.);
#1161=FACE_OUTER_BOUND('',#1720,.T.);
#1162=FACE_OUTER_BOUND('',#1721,.T.);
#1163=FACE_OUTER_BOUND('',#1723,.T.);
#1164=FACE_OUTER_BOUND('',#1724,.T.);
#1165=FACE_OUTER_BOUND('',#1727,.T.);
#1166=FACE_OUTER_BOUND('',#1728,.T.);
#1167=FACE_OUTER_BOUND('',#1729,.T.);
#1168=FACE_OUTER_BOUND('',#1730,.T.);
#1169=FACE_OUTER_BOUND('',#1732,.T.);
#1170=FACE_OUTER_BOUND('',#1733,.T.);
#1171=FACE_OUTER_BOUND('',#1734,.T.);
#1172=FACE_OUTER_BOUND('',#1735,.T.);
#1173=FACE_OUTER_BOUND('',#1736,.T.);
#1576=EDGE_LOOP('',(#6424,#6425,#6426,#6427));
#1577=EDGE_LOOP('',(#6428,#6429,#6430,#6431));
#1578=EDGE_LOOP('',(#6432,#6433,#6434,#6435));
#1579=EDGE_LOOP('',(#6436,#6437,#6438,#6439));
#1580=EDGE_LOOP('',(#6440,#6441,#6442,#6443));
#1581=EDGE_LOOP('',(#6444,#6445,#6446,#6447));
#1582=EDGE_LOOP('',(#6448,#6449,#6450,#6451));
#1583=EDGE_LOOP('',(#6452,#6453,#6454,#6455));
#1584=EDGE_LOOP('',(#6456,#6457,#6458,#6459));
#1585=EDGE_LOOP('',(#6460,#6461,#6462,#6463));
#1586=EDGE_LOOP('',(#6464,#6465,#6466,#6467));
#1587=EDGE_LOOP('',(#6468,#6469,#6470,#6471));
#1588=EDGE_LOOP('',(#6472,#6473,#6474,#6475));
#1589=EDGE_LOOP('',(#6476,#6477,#6478,#6479));
#1590=EDGE_LOOP('',(#6480,#6481,#6482,#6483));
#1591=EDGE_LOOP('',(#6484,#6485,#6486,#6487));
#1592=EDGE_LOOP('',(#6488,#6489,#6490,#6491));
#1593=EDGE_LOOP('',(#6492,#6493,#6494,#6495));
#1594=EDGE_LOOP('',(#6496,#6497,#6498,#6499));
#1595=EDGE_LOOP('',(#6500,#6501,#6502,#6503));
#1596=EDGE_LOOP('',(#6504,#6505,#6506,#6507));
#1597=EDGE_LOOP('',(#6508,#6509,#6510,#6511));
#1598=EDGE_LOOP('',(#6512,#6513,#6514,#6515));
#1599=EDGE_LOOP('',(#6516,#6517,#6518,#6519));
#1600=EDGE_LOOP('',(#6520,#6521,#6522,#6523));
#1601=EDGE_LOOP('',(#6524,#6525,#6526,#6527));
#1602=EDGE_LOOP('',(#6528,#6529,#6530,#6531));
#1603=EDGE_LOOP('',(#6532,#6533,#6534,#6535));
#1604=EDGE_LOOP('',(#6536,#6537,#6538,#6539));
#1605=EDGE_LOOP('',(#6540,#6541,#6542,#6543));
#1606=EDGE_LOOP('',(#6544,#6545,#6546,#6547));
#1607=EDGE_LOOP('',(#6548,#6549,#6550,#6551));
#1608=EDGE_LOOP('',(#6552,#6553,#6554,#6555));
#1609=EDGE_LOOP('',(#6556,#6557,#6558,#6559));
#1610=EDGE_LOOP('',(#6560,#6561,#6562,#6563));
#1611=EDGE_LOOP('',(#6564,#6565,#6566,#6567));
#1612=EDGE_LOOP('',(#6568,#6569,#6570,#6571));
#1613=EDGE_LOOP('',(#6572,#6573,#6574,#6575));
#1614=EDGE_LOOP('',(#6576,#6577,#6578,#6579));
#1615=EDGE_LOOP('',(#6580,#6581,#6582,#6583));
#1616=EDGE_LOOP('',(#6584,#6585,#6586,#6587));
#1617=EDGE_LOOP('',(#6588,#6589,#6590,#6591));
#1618=EDGE_LOOP('',(#6592,#6593,#6594,#6595));
#1619=EDGE_LOOP('',(#6596,#6597,#6598,#6599));
#1620=EDGE_LOOP('',(#6600,#6601,#6602,#6603));
#1621=EDGE_LOOP('',(#6604,#6605,#6606,#6607));
#1622=EDGE_LOOP('',(#6608,#6609,#6610,#6611));
#1623=EDGE_LOOP('',(#6612,#6613,#6614,#6615));
#1624=EDGE_LOOP('',(#6616,#6617,#6618,#6619));
#1625=EDGE_LOOP('',(#6620,#6621,#6622,#6623));
#1626=EDGE_LOOP('',(#6624,#6625,#6626,#6627));
#1627=EDGE_LOOP('',(#6628,#6629,#6630,#6631));
#1628=EDGE_LOOP('',(#6632,#6633,#6634,#6635));
#1629=EDGE_LOOP('',(#6636,#6637,#6638,#6639));
#1630=EDGE_LOOP('',(#6640,#6641,#6642,#6643));
#1631=EDGE_LOOP('',(#6644,#6645,#6646,#6647));
#1632=EDGE_LOOP('',(#6648,#6649,#6650,#6651));
#1633=EDGE_LOOP('',(#6652,#6653,#6654,#6655));
#1634=EDGE_LOOP('',(#6656,#6657,#6658,#6659));
#1635=EDGE_LOOP('',(#6660,#6661,#6662,#6663));
#1636=EDGE_LOOP('',(#6664,#6665,#6666,#6667));
#1637=EDGE_LOOP('',(#6668,#6669,#6670,#6671));
#1638=EDGE_LOOP('',(#6672,#6673,#6674,#6675));
#1639=EDGE_LOOP('',(#6676,#6677,#6678,#6679));
#1640=EDGE_LOOP('',(#6680,#6681,#6682,#6683));
#1641=EDGE_LOOP('',(#6684,#6685,#6686,#6687));
#1642=EDGE_LOOP('',(#6688,#6689,#6690,#6691));
#1643=EDGE_LOOP('',(#6692,#6693,#6694,#6695));
#1644=EDGE_LOOP('',(#6696,#6697,#6698,#6699));
#1645=EDGE_LOOP('',(#6700,#6701,#6702,#6703));
#1646=EDGE_LOOP('',(#6704,#6705,#6706,#6707));
#1647=EDGE_LOOP('',(#6708,#6709,#6710,#6711));
#1648=EDGE_LOOP('',(#6712,#6713,#6714,#6715));
#1649=EDGE_LOOP('',(#6716,#6717,#6718,#6719));
#1650=EDGE_LOOP('',(#6720,#6721,#6722,#6723));
#1651=EDGE_LOOP('',(#6724,#6725,#6726,#6727));
#1652=EDGE_LOOP('',(#6728,#6729,#6730,#6731));
#1653=EDGE_LOOP('',(#6732,#6733,#6734,#6735));
#1654=EDGE_LOOP('',(#6736,#6737,#6738,#6739));
#1655=EDGE_LOOP('',(#6740,#6741,#6742,#6743));
#1656=EDGE_LOOP('',(#6744,#6745,#6746,#6747));
#1657=EDGE_LOOP('',(#6748,#6749,#6750,#6751));
#1658=EDGE_LOOP('',(#6752,#6753,#6754,#6755));
#1659=EDGE_LOOP('',(#6756,#6757,#6758,#6759));
#1660=EDGE_LOOP('',(#6760,#6761,#6762,#6763));
#1661=EDGE_LOOP('',(#6764,#6765,#6766,#6767));
#1662=EDGE_LOOP('',(#6768,#6769,#6770,#6771));
#1663=EDGE_LOOP('',(#6772,#6773,#6774,#6775));
#1664=EDGE_LOOP('',(#6776,#6777,#6778,#6779));
#1665=EDGE_LOOP('',(#6780,#6781,#6782,#6783));
#1666=EDGE_LOOP('',(#6784,#6785,#6786,#6787));
#1667=EDGE_LOOP('',(#6788,#6789,#6790,#6791));
#1668=EDGE_LOOP('',(#6792,#6793,#6794,#6795));
#1669=EDGE_LOOP('',(#6796,#6797,#6798,#6799));
#1670=EDGE_LOOP('',(#6800,#6801,#6802,#6803));
#1671=EDGE_LOOP('',(#6804,#6805,#6806,#6807));
#1672=EDGE_LOOP('',(#6808,#6809,#6810,#6811));
#1673=EDGE_LOOP('',(#6812,#6813,#6814,#6815));
#1674=EDGE_LOOP('',(#6816,#6817,#6818,#6819));
#1675=EDGE_LOOP('',(#6820,#6821,#6822,#6823));
#1676=EDGE_LOOP('',(#6824,#6825,#6826,#6827));
#1677=EDGE_LOOP('',(#6828,#6829,#6830,#6831));
#1678=EDGE_LOOP('',(#6832,#6833,#6834,#6835));
#1679=EDGE_LOOP('',(#6836,#6837,#6838,#6839));
#1680=EDGE_LOOP('',(#6840,#6841,#6842,#6843));
#1681=EDGE_LOOP('',(#6844,#6845,#6846,#6847));
#1682=EDGE_LOOP('',(#6848,#6849,#6850,#6851));
#1683=EDGE_LOOP('',(#6852,#6853,#6854,#6855));
#1684=EDGE_LOOP('',(#6856,#6857,#6858,#6859));
#1685=EDGE_LOOP('',(#6860,#6861,#6862,#6863));
#1686=EDGE_LOOP('',(#6864,#6865,#6866,#6867));
#1687=EDGE_LOOP('',(#6868,#6869,#6870,#6871));
#1688=EDGE_LOOP('',(#6872,#6873,#6874,#6875));
#1689=EDGE_LOOP('',(#6876,#6877,#6878,#6879));
#1690=EDGE_LOOP('',(#6880,#6881,#6882,#6883));
#1691=EDGE_LOOP('',(#6884,#6885,#6886,#6887));
#1692=EDGE_LOOP('',(#6888,#6889,#6890,#6891));
#1693=EDGE_LOOP('',(#6892,#6893,#6894,#6895));
#1694=EDGE_LOOP('',(#6896,#6897,#6898,#6899));
#1695=EDGE_LOOP('',(#6900,#6901,#6902,#6903));
#1696=EDGE_LOOP('',(#6904,#6905,#6906,#6907));
#1697=EDGE_LOOP('',(#6908,#6909,#6910,#6911,#6912));
#1698=EDGE_LOOP('',(#6913,#6914,#6915,#6916,#6917,#6918,#6919,#6920,#6921,
#6922,#6923,#6924,#6925,#6926,#6927,#6928,#6929,#6930,#6931,#6932,#6933,
#6934,#6935,#6936,#6937,#6938,#6939,#6940,#6941,#6942,#6943,#6944,#6945,
#6946,#6947,#6948,#6949,#6950,#6951,#6952,#6953,#6954,#6955,#6956,#6957,
#6958,#6959,#6960,#6961,#6962,#6963,#6964,#6965,#6966,#6967,#6968,#6969,
#6970,#6971,#6972,#6973,#6974,#6975,#6976,#6977,#6978,#6979,#6980,#6981,
#6982,#6983,#6984,#6985,#6986,#6987,#6988,#6989,#6990,#6991,#6992,#6993,
#6994,#6995,#6996,#6997,#6998,#6999,#7000,#7001,#7002,#7003,#7004,#7005,
#7006,#7007,#7008,#7009,#7010,#7011,#7012,#7013,#7014,#7015,#7016,#7017,
#7018,#7019,#7020,#7021,#7022,#7023,#7024,#7025,#7026,#7027,#7028,#7029,
#7030,#7031,#7032));
#1699=EDGE_LOOP('',(#7033,#7034,#7035,#7036,#7037));
#1700=EDGE_LOOP('',(#7038));
#1701=EDGE_LOOP('',(#7039,#7040,#7041,#7042,#7043,#7044,#7045,#7046,#7047,
#7048));
#1702=EDGE_LOOP('',(#7049,#7050,#7051));
#1703=EDGE_LOOP('',(#7052,#7053,#7054,#7055,#7056,#7057));
#1704=EDGE_LOOP('',(#7058,#7059,#7060));
#1705=EDGE_LOOP('',(#7061,#7062,#7063));
#1706=EDGE_LOOP('',(#7064,#7065,#7066,#7067,#7068,#7069,#7070));
#1707=EDGE_LOOP('',(#7071,#7072,#7073));
#1708=EDGE_LOOP('',(#7074,#7075,#7076,#7077));
#1709=EDGE_LOOP('',(#7078));
#1710=EDGE_LOOP('',(#7079,#7080,#7081,#7082,#7083,#7084,#7085,#7086,#7087,
#7088,#7089,#7090,#7091,#7092,#7093,#7094,#7095,#7096,#7097,#7098,#7099,
#7100,#7101,#7102,#7103,#7104,#7105,#7106,#7107,#7108,#7109,#7110,#7111,
#7112,#7113,#7114,#7115,#7116,#7117,#7118,#7119,#7120,#7121,#7122,#7123,
#7124,#7125,#7126,#7127,#7128,#7129,#7130,#7131,#7132,#7133,#7134,#7135,
#7136,#7137,#7138,#7139,#7140,#7141,#7142,#7143,#7144,#7145,#7146,#7147,
#7148,#7149,#7150,#7151,#7152,#7153,#7154,#7155,#7156,#7157,#7158,#7159,
#7160,#7161,#7162,#7163,#7164,#7165,#7166,#7167,#7168,#7169,#7170,#7171,
#7172,#7173,#7174,#7175,#7176,#7177,#7178,#7179,#7180,#7181,#7182,#7183,
#7184,#7185,#7186,#7187,#7188,#7189,#7190,#7191,#7192,#7193,#7194,#7195,
#7196,#7197,#7198));
#1711=EDGE_LOOP('',(#7199,#7200,#7201));
#1712=EDGE_LOOP('',(#7202,#7203,#7204,#7205));
#1713=EDGE_LOOP('',(#7206,#7207,#7208,#7209));
#1714=EDGE_LOOP('',(#7210,#7211,#7212,#7213));
#1715=EDGE_LOOP('',(#7214,#7215,#7216));
#1716=EDGE_LOOP('',(#7217,#7218,#7219));
#1717=EDGE_LOOP('',(#7220,#7221,#7222,#7223));
#1718=EDGE_LOOP('',(#7224,#7225,#7226,#7227));
#1719=EDGE_LOOP('',(#7228,#7229,#7230,#7231));
#1720=EDGE_LOOP('',(#7232,#7233,#7234));
#1721=EDGE_LOOP('',(#7235));
#1722=EDGE_LOOP('',(#7236));
#1723=EDGE_LOOP('',(#7237,#7238,#7239,#7240));
#1724=EDGE_LOOP('',(#7241,#7242,#7243,#7244));
#1725=EDGE_LOOP('',(#7245,#7246));
#1726=EDGE_LOOP('',(#7247,#7248));
#1727=EDGE_LOOP('',(#7249,#7250,#7251,#7252));
#1728=EDGE_LOOP('',(#7253,#7254,#7255,#7256));
#1729=EDGE_LOOP('',(#7257,#7258,#7259,#7260,#7261,#7262));
#1730=EDGE_LOOP('',(#7263));
#1731=EDGE_LOOP('',(#7264,#7265,#7266,#7267));
#1732=EDGE_LOOP('',(#7268,#7269,#7270,#7271));
#1733=EDGE_LOOP('',(#7272,#7273,#7274,#7275));
#1734=EDGE_LOOP('',(#7276,#7277,#7278,#7279));
#1735=EDGE_LOOP('',(#7280,#7281,#7282,#7283));
#1736=EDGE_LOOP('',(#7284,#7285,#7286,#7287));
#2212=CIRCLE('',#10270,18.);
#2213=CIRCLE('',#10271,18.);
#2214=CIRCLE('',#10273,18.);
#2215=CIRCLE('',#10274,18.);
#2216=CIRCLE('',#10276,18.);
#2217=CIRCLE('',#10277,18.);
#2218=CIRCLE('',#10279,18.);
#2219=CIRCLE('',#10280,18.);
#2220=CIRCLE('',#10282,18.);
#2221=CIRCLE('',#10283,18.);
#2222=CIRCLE('',#10285,18.);
#2223=CIRCLE('',#10286,18.);
#2224=CIRCLE('',#10288,18.);
#2225=CIRCLE('',#10289,18.);
#2226=CIRCLE('',#10291,18.);
#2227=CIRCLE('',#10292,18.);
#2228=CIRCLE('',#10294,18.);
#2229=CIRCLE('',#10295,18.);
#2230=CIRCLE('',#10297,18.);
#2231=CIRCLE('',#10298,18.);
#2232=CIRCLE('',#10300,18.);
#2233=CIRCLE('',#10301,18.);
#2234=CIRCLE('',#10303,18.);
#2235=CIRCLE('',#10304,18.);
#2236=CIRCLE('',#10306,18.);
#2237=CIRCLE('',#10307,18.);
#2238=CIRCLE('',#10309,18.);
#2239=CIRCLE('',#10310,18.);
#2240=CIRCLE('',#10312,18.);
#2241=CIRCLE('',#10313,18.);
#2242=CIRCLE('',#10315,18.);
#2243=CIRCLE('',#10316,18.);
#2244=CIRCLE('',#10318,18.);
#2245=CIRCLE('',#10319,18.);
#2246=CIRCLE('',#10321,18.);
#2247=CIRCLE('',#10322,18.);
#2248=CIRCLE('',#10324,18.);
#2249=CIRCLE('',#10325,18.);
#2250=CIRCLE('',#10327,18.);
#2251=CIRCLE('',#10328,18.);
#2252=CIRCLE('',#10330,18.);
#2253=CIRCLE('',#10331,18.);
#2254=CIRCLE('',#10333,18.);
#2255=CIRCLE('',#10334,18.);
#2256=CIRCLE('',#10336,18.);
#2257=CIRCLE('',#10337,18.);
#2258=CIRCLE('',#10339,18.);
#2259=CIRCLE('',#10340,18.);
#2260=CIRCLE('',#10342,18.);
#2261=CIRCLE('',#10343,18.);
#2262=CIRCLE('',#10345,18.);
#2263=CIRCLE('',#10346,18.);
#2264=CIRCLE('',#10348,18.);
#2265=CIRCLE('',#10349,18.);
#2266=CIRCLE('',#10351,18.);
#2267=CIRCLE('',#10352,18.);
#2268=CIRCLE('',#10354,18.);
#2269=CIRCLE('',#10355,18.);
#2270=CIRCLE('',#10357,18.);
#2271=CIRCLE('',#10358,18.);
#2272=CIRCLE('',#10360,18.);
#2273=CIRCLE('',#10361,18.);
#2274=CIRCLE('',#10363,18.);
#2275=CIRCLE('',#10364,18.);
#2276=CIRCLE('',#10366,18.);
#2277=CIRCLE('',#10367,18.);
#2278=CIRCLE('',#10369,18.);
#2279=CIRCLE('',#10370,18.);
#2280=CIRCLE('',#10372,18.);
#2281=CIRCLE('',#10373,18.);
#2282=CIRCLE('',#10375,18.);
#2283=CIRCLE('',#10376,18.);
#2284=CIRCLE('',#10378,18.);
#2285=CIRCLE('',#10379,18.);
#2286=CIRCLE('',#10381,18.);
#2287=CIRCLE('',#10382,18.);
#2288=CIRCLE('',#10384,18.);
#2289=CIRCLE('',#10385,18.);
#2290=CIRCLE('',#10387,18.);
#2291=CIRCLE('',#10388,18.);
#2292=CIRCLE('',#10470,25.);
#2293=CIRCLE('',#10471,25.);
#2294=CIRCLE('',#10473,24.);
#2295=CIRCLE('',#10475,24.);
#2296=CIRCLE('',#10476,20.);
#2297=CIRCLE('',#10478,10.75);
#2298=CIRCLE('',#10479,40.);
#2299=CIRCLE('',#10480,40.);
#2300=CIRCLE('',#10483,40.);
#2301=CIRCLE('',#10486,40.);
#2302=CIRCLE('',#10488,20.);
#2303=CIRCLE('',#10490,1.);
#2304=CIRCLE('',#10491,1.);
#2305=CIRCLE('',#10493,1.);
#2306=CIRCLE('',#10494,1.);
#2307=CIRCLE('',#10495,0.999999999999999);
#2308=CIRCLE('',#10496,1.);
#2309=CIRCLE('',#10498,1.);
#2310=CIRCLE('',#10499,1.);
#2311=CIRCLE('',#10501,10.7);
#2312=CIRCLE('',#10503,8.35);
#2313=CIRCLE('',#10504,8.35);
#2314=CIRCLE('',#10505,9.33888888888891);
#2315=CIRCLE('',#10506,8.35);
#2316=CIRCLE('',#10508,6.18146853146853);
#2317=CIRCLE('',#10510,2.35);
#2600=LINE('',#13920,#3350);
#2601=LINE('',#13924,#3351);
#2602=LINE('',#13929,#3352);
#2603=LINE('',#13933,#3353);
#2604=LINE('',#13938,#3354);
#2605=LINE('',#13942,#3355);
#2606=LINE('',#13947,#3356);
#2607=LINE('',#13951,#3357);
#2608=LINE('',#13956,#3358);
#2609=LINE('',#13960,#3359);
#2610=LINE('',#13965,#3360);
#2611=LINE('',#13969,#3361);
#2612=LINE('',#13974,#3362);
#2613=LINE('',#13978,#3363);
#2614=LINE('',#13983,#3364);
#2615=LINE('',#13987,#3365);
#2616=LINE('',#13992,#3366);
#2617=LINE('',#13996,#3367);
#2618=LINE('',#14001,#3368);
#2619=LINE('',#14005,#3369);
#2620=LINE('',#14010,#3370);
#2621=LINE('',#14014,#3371);
#2622=LINE('',#14019,#3372);
#2623=LINE('',#14023,#3373);
#2624=LINE('',#14028,#3374);
#2625=LINE('',#14032,#3375);
#2626=LINE('',#14037,#3376);
#2627=LINE('',#14041,#3377);
#2628=LINE('',#14046,#3378);
#2629=LINE('',#14050,#3379);
#2630=LINE('',#14055,#3380);
#2631=LINE('',#14059,#3381);
#2632=LINE('',#14064,#3382);
#2633=LINE('',#14068,#3383);
#2634=LINE('',#14073,#3384);
#2635=LINE('',#14077,#3385);
#2636=LINE('',#14082,#3386);
#2637=LINE('',#14086,#3387);
#2638=LINE('',#14091,#3388);
#2639=LINE('',#14095,#3389);
#2640=LINE('',#14100,#3390);
#2641=LINE('',#14104,#3391);
#2642=LINE('',#14109,#3392);
#2643=LINE('',#14113,#3393);
#2644=LINE('',#14118,#3394);
#2645=LINE('',#14122,#3395);
#2646=LINE('',#14127,#3396);
#2647=LINE('',#14131,#3397);
#2648=LINE('',#14136,#3398);
#2649=LINE('',#14140,#3399);
#2650=LINE('',#14145,#3400);
#2651=LINE('',#14149,#3401);
#2652=LINE('',#14154,#3402);
#2653=LINE('',#14158,#3403);
#2654=LINE('',#14163,#3404);
#2655=LINE('',#14167,#3405);
#2656=LINE('',#14172,#3406);
#2657=LINE('',#14176,#3407);
#2658=LINE('',#14181,#3408);
#2659=LINE('',#14185,#3409);
#2660=LINE('',#14190,#3410);
#2661=LINE('',#14194,#3411);
#2662=LINE('',#14199,#3412);
#2663=LINE('',#14203,#3413);
#2664=LINE('',#14208,#3414);
#2665=LINE('',#14212,#3415);
#2666=LINE('',#14217,#3416);
#2667=LINE('',#14221,#3417);
#2668=LINE('',#14226,#3418);
#2669=LINE('',#14230,#3419);
#2670=LINE('',#14235,#3420);
#2671=LINE('',#14239,#3421);
#2672=LINE('',#14244,#3422);
#2673=LINE('',#14248,#3423);
#2674=LINE('',#14253,#3424);
#2675=LINE('',#14257,#3425);
#2676=LINE('',#14262,#3426);
#2677=LINE('',#14266,#3427);
#2678=LINE('',#14271,#3428);
#2679=LINE('',#14275,#3429);
#2680=LINE('',#14279,#3430);
#2681=LINE('',#14281,#3431);
#2682=LINE('',#14282,#3432);
#2683=LINE('',#14284,#3433);
#2684=LINE('',#14285,#3434);
#2685=LINE('',#14288,#3435);
#2686=LINE('',#14290,#3436);
#2687=LINE('',#14291,#3437);
#2688=LINE('',#14293,#3438);
#2689=LINE('',#14294,#3439);
#2690=LINE('',#14297,#3440);
#2691=LINE('',#14299,#3441);
#2692=LINE('',#14300,#3442);
#2693=LINE('',#14302,#3443);
#2694=LINE('',#14303,#3444);
#2695=LINE('',#14306,#3445);
#2696=LINE('',#14308,#3446);
#2697=LINE('',#14309,#3447);
#2698=LINE('',#14311,#3448);
#2699=LINE('',#14312,#3449);
#2700=LINE('',#14315,#3450);
#2701=LINE('',#14317,#3451);
#2702=LINE('',#14318,#3452);
#2703=LINE('',#14320,#3453);
#2704=LINE('',#14321,#3454);
#2705=LINE('',#14324,#3455);
#2706=LINE('',#14326,#3456);
#2707=LINE('',#14327,#3457);
#2708=LINE('',#14329,#3458);
#2709=LINE('',#14330,#3459);
#2710=LINE('',#14333,#3460);
#2711=LINE('',#14335,#3461);
#2712=LINE('',#14336,#3462);
#2713=LINE('',#14338,#3463);
#2714=LINE('',#14339,#3464);
#2715=LINE('',#14342,#3465);
#2716=LINE('',#14344,#3466);
#2717=LINE('',#14345,#3467);
#2718=LINE('',#14347,#3468);
#2719=LINE('',#14348,#3469);
#2720=LINE('',#14351,#3470);
#2721=LINE('',#14353,#3471);
#2722=LINE('',#14354,#3472);
#2723=LINE('',#14356,#3473);
#2724=LINE('',#14357,#3474);
#2725=LINE('',#14360,#3475);
#2726=LINE('',#14362,#3476);
#2727=LINE('',#14363,#3477);
#2728=LINE('',#14365,#3478);
#2729=LINE('',#14366,#3479);
#2730=LINE('',#14369,#3480);
#2731=LINE('',#14371,#3481);
#2732=LINE('',#14372,#3482);
#2733=LINE('',#14374,#3483);
#2734=LINE('',#14375,#3484);
#2735=LINE('',#14378,#3485);
#2736=LINE('',#14380,#3486);
#2737=LINE('',#14381,#3487);
#2738=LINE('',#14383,#3488);
#2739=LINE('',#14384,#3489);
#2740=LINE('',#14387,#3490);
#2741=LINE('',#14389,#3491);
#2742=LINE('',#14390,#3492);
#2743=LINE('',#14392,#3493);
#2744=LINE('',#14393,#3494);
#2745=LINE('',#14396,#3495);
#2746=LINE('',#14398,#3496);
#2747=LINE('',#14399,#3497);
#2748=LINE('',#14401,#3498);
#2749=LINE('',#14402,#3499);
#2750=LINE('',#14405,#3500);
#2751=LINE('',#14407,#3501);
#2752=LINE('',#14408,#3502);
#2753=LINE('',#14410,#3503);
#2754=LINE('',#14411,#3504);
#2755=LINE('',#14414,#3505);
#2756=LINE('',#14416,#3506);
#2757=LINE('',#14417,#3507);
#2758=LINE('',#14419,#3508);
#2759=LINE('',#14420,#3509);
#2760=LINE('',#14423,#3510);
#2761=LINE('',#14425,#3511);
#2762=LINE('',#14426,#3512);
#2763=LINE('',#14428,#3513);
#2764=LINE('',#14429,#3514);
#2765=LINE('',#14432,#3515);
#2766=LINE('',#14434,#3516);
#2767=LINE('',#14435,#3517);
#2768=LINE('',#14437,#3518);
#2769=LINE('',#14438,#3519);
#2770=LINE('',#14441,#3520);
#2771=LINE('',#14443,#3521);
#2772=LINE('',#14444,#3522);
#2773=LINE('',#14446,#3523);
#2774=LINE('',#14447,#3524);
#2775=LINE('',#14450,#3525);
#2776=LINE('',#14452,#3526);
#2777=LINE('',#14453,#3527);
#2778=LINE('',#14455,#3528);
#2779=LINE('',#14456,#3529);
#2780=LINE('',#14459,#3530);
#2781=LINE('',#14461,#3531);
#2782=LINE('',#14462,#3532);
#2783=LINE('',#14464,#3533);
#2784=LINE('',#14465,#3534);
#2785=LINE('',#14468,#3535);
#2786=LINE('',#14470,#3536);
#2787=LINE('',#14471,#3537);
#2788=LINE('',#14473,#3538);
#2789=LINE('',#14474,#3539);
#2790=LINE('',#14477,#3540);
#2791=LINE('',#14479,#3541);
#2792=LINE('',#14480,#3542);
#2793=LINE('',#14482,#3543);
#2794=LINE('',#14483,#3544);
#2795=LINE('',#14486,#3545);
#2796=LINE('',#14488,#3546);
#2797=LINE('',#14489,#3547);
#2798=LINE('',#14491,#3548);
#2799=LINE('',#14492,#3549);
#2800=LINE('',#14495,#3550);
#2801=LINE('',#14497,#3551);
#2802=LINE('',#14498,#3552);
#2803=LINE('',#14500,#3553);
#2804=LINE('',#14501,#3554);
#2805=LINE('',#14504,#3555);
#2806=LINE('',#14506,#3556);
#2807=LINE('',#14507,#3557);
#2808=LINE('',#14509,#3558);
#2809=LINE('',#14510,#3559);
#2810=LINE('',#14513,#3560);
#2811=LINE('',#14515,#3561);
#2812=LINE('',#14516,#3562);
#2813=LINE('',#14518,#3563);
#2814=LINE('',#14519,#3564);
#2815=LINE('',#14522,#3565);
#2816=LINE('',#14524,#3566);
#2817=LINE('',#14525,#3567);
#2818=LINE('',#14527,#3568);
#2819=LINE('',#14528,#3569);
#2820=LINE('',#14531,#3570);
#2821=LINE('',#14533,#3571);
#2822=LINE('',#14534,#3572);
#2823=LINE('',#14536,#3573);
#2824=LINE('',#14537,#3574);
#2825=LINE('',#14540,#3575);
#2826=LINE('',#14542,#3576);
#2827=LINE('',#14543,#3577);
#2828=LINE('',#14545,#3578);
#2829=LINE('',#14546,#3579);
#2830=LINE('',#14549,#3580);
#2831=LINE('',#14551,#3581);
#2832=LINE('',#14552,#3582);
#2833=LINE('',#14554,#3583);
#2834=LINE('',#14555,#3584);
#2835=LINE('',#14558,#3585);
#2836=LINE('',#14560,#3586);
#2837=LINE('',#14561,#3587);
#2838=LINE('',#14563,#3588);
#2839=LINE('',#14564,#3589);
#2840=LINE('',#14567,#3590);
#2841=LINE('',#14569,#3591);
#2842=LINE('',#14570,#3592);
#2843=LINE('',#14572,#3593);
#2844=LINE('',#14573,#3594);
#2845=LINE('',#14576,#3595);
#2846=LINE('',#14578,#3596);
#2847=LINE('',#14579,#3597);
#2848=LINE('',#14581,#3598);
#2849=LINE('',#14582,#3599);
#2850=LINE('',#14585,#3600);
#2851=LINE('',#14587,#3601);
#2852=LINE('',#14588,#3602);
#2853=LINE('',#14590,#3603);
#2854=LINE('',#14591,#3604);
#2855=LINE('',#14594,#3605);
#2856=LINE('',#14596,#3606);
#2857=LINE('',#14597,#3607);
#2858=LINE('',#14599,#3608);
#2859=LINE('',#14600,#3609);
#2860=LINE('',#14603,#3610);
#2861=LINE('',#14605,#3611);
#2862=LINE('',#14606,#3612);
#2863=LINE('',#14608,#3613);
#2864=LINE('',#14609,#3614);
#2865=LINE('',#14612,#3615);
#2866=LINE('',#14614,#3616);
#2867=LINE('',#14615,#3617);
#2868=LINE('',#14617,#3618);
#2869=LINE('',#14618,#3619);
#2870=LINE('',#14621,#3620);
#2871=LINE('',#14623,#3621);
#2872=LINE('',#14624,#3622);
#2873=LINE('',#14626,#3623);
#2874=LINE('',#14627,#3624);
#2875=LINE('',#14630,#3625);
#2876=LINE('',#14632,#3626);
#2877=LINE('',#14633,#3627);
#2878=LINE('',#14635,#3628);
#2879=LINE('',#14636,#3629);
#2880=LINE('',#15043,#3630);
#2881=LINE('',#16673,#3631);
#2882=LINE('',#16992,#3632);
#2883=LINE('',#17628,#3633);
#2884=LINE('',#17633,#3634);
#2885=LINE('',#17637,#3635);
#2886=LINE('',#17639,#3636);
#2887=LINE('',#17641,#3637);
#2888=LINE('',#17642,#3638);
#2889=LINE('',#17645,#3639);
#2890=LINE('',#17647,#3640);
#2891=LINE('',#17648,#3641);
#2892=LINE('',#17651,#3642);
#2893=LINE('',#17652,#3643);
#2894=LINE('',#17655,#3644);
#2895=LINE('',#17656,#3645);
#2896=LINE('',#17658,#3646);
#3350=VECTOR('',#11239,1000.);
#3351=VECTOR('',#11242,1000.);
#3352=VECTOR('',#11247,1000.);
#3353=VECTOR('',#11250,1000.);
#3354=VECTOR('',#11255,1000.);
#3355=VECTOR('',#11258,1000.);
#3356=VECTOR('',#11263,1000.);
#3357=VECTOR('',#11266,1000.);
#3358=VECTOR('',#11271,1000.);
#3359=VECTOR('',#11274,1000.);
#3360=VECTOR('',#11279,1000.);
#3361=VECTOR('',#11282,1000.);
#3362=VECTOR('',#11287,1000.);
#3363=VECTOR('',#11290,1000.);
#3364=VECTOR('',#11295,1000.);
#3365=VECTOR('',#11298,1000.);
#3366=VECTOR('',#11303,1000.);
#3367=VECTOR('',#11306,1000.);
#3368=VECTOR('',#11311,1000.);
#3369=VECTOR('',#11314,1000.);
#3370=VECTOR('',#11319,1000.);
#3371=VECTOR('',#11322,1000.);
#3372=VECTOR('',#11327,1000.);
#3373=VECTOR('',#11330,1000.);
#3374=VECTOR('',#11335,1000.);
#3375=VECTOR('',#11338,1000.);
#3376=VECTOR('',#11343,1000.);
#3377=VECTOR('',#11346,1000.);
#3378=VECTOR('',#11351,1000.);
#3379=VECTOR('',#11354,1000.);
#3380=VECTOR('',#11359,1000.);
#3381=VECTOR('',#11362,1000.);
#3382=VECTOR('',#11367,1000.);
#3383=VECTOR('',#11370,1000.);
#3384=VECTOR('',#11375,1000.);
#3385=VECTOR('',#11378,1000.);
#3386=VECTOR('',#11383,1000.);
#3387=VECTOR('',#11386,1000.);
#3388=VECTOR('',#11391,1000.);
#3389=VECTOR('',#11394,1000.);
#3390=VECTOR('',#11399,1000.);
#3391=VECTOR('',#11402,1000.);
#3392=VECTOR('',#11407,1000.);
#3393=VECTOR('',#11410,1000.);
#3394=VECTOR('',#11415,1000.);
#3395=VECTOR('',#11418,1000.);
#3396=VECTOR('',#11423,1000.);
#3397=VECTOR('',#11426,1000.);
#3398=VECTOR('',#11431,1000.);
#3399=VECTOR('',#11434,1000.);
#3400=VECTOR('',#11439,1000.);
#3401=VECTOR('',#11442,1000.);
#3402=VECTOR('',#11447,1000.);
#3403=VECTOR('',#11450,1000.);
#3404=VECTOR('',#11455,1000.);
#3405=VECTOR('',#11458,1000.);
#3406=VECTOR('',#11463,1000.);
#3407=VECTOR('',#11466,1000.);
#3408=VECTOR('',#11471,1000.);
#3409=VECTOR('',#11474,1000.);
#3410=VECTOR('',#11479,1000.);
#3411=VECTOR('',#11482,1000.);
#3412=VECTOR('',#11487,1000.);
#3413=VECTOR('',#11490,1000.);
#3414=VECTOR('',#11495,1000.);
#3415=VECTOR('',#11498,1000.);
#3416=VECTOR('',#11503,1000.);
#3417=VECTOR('',#11506,1000.);
#3418=VECTOR('',#11511,1000.);
#3419=VECTOR('',#11514,1000.);
#3420=VECTOR('',#11519,1000.);
#3421=VECTOR('',#11522,1000.);
#3422=VECTOR('',#11527,1000.);
#3423=VECTOR('',#11530,1000.);
#3424=VECTOR('',#11535,1000.);
#3425=VECTOR('',#11538,1000.);
#3426=VECTOR('',#11543,1000.);
#3427=VECTOR('',#11546,1000.);
#3428=VECTOR('',#11551,1000.);
#3429=VECTOR('',#11554,1000.);
#3430=VECTOR('',#11559,1000.);
#3431=VECTOR('',#11560,1000.);
#3432=VECTOR('',#11561,1000.);
#3433=VECTOR('',#11564,1000.);
#3434=VECTOR('',#11565,1000.);
#3435=VECTOR('',#11568,1000.);
#3436=VECTOR('',#11569,1000.);
#3437=VECTOR('',#11570,1000.);
#3438=VECTOR('',#11573,1000.);
#3439=VECTOR('',#11574,1000.);
#3440=VECTOR('',#11577,1000.);
#3441=VECTOR('',#11578,1000.);
#3442=VECTOR('',#11579,1000.);
#3443=VECTOR('',#11582,1000.);
#3444=VECTOR('',#11583,1000.);
#3445=VECTOR('',#11586,1000.);
#3446=VECTOR('',#11587,1000.);
#3447=VECTOR('',#11588,1000.);
#3448=VECTOR('',#11591,1000.);
#3449=VECTOR('',#11592,1000.);
#3450=VECTOR('',#11595,1000.);
#3451=VECTOR('',#11596,1000.);
#3452=VECTOR('',#11597,1000.);
#3453=VECTOR('',#11600,1000.);
#3454=VECTOR('',#11601,1000.);
#3455=VECTOR('',#11604,1000.);
#3456=VECTOR('',#11605,1000.);
#3457=VECTOR('',#11606,1000.);
#3458=VECTOR('',#11609,1000.);
#3459=VECTOR('',#11610,1000.);
#3460=VECTOR('',#11613,1000.);
#3461=VECTOR('',#11614,1000.);
#3462=VECTOR('',#11615,1000.);
#3463=VECTOR('',#11618,1000.);
#3464=VECTOR('',#11619,1000.);
#3465=VECTOR('',#11622,1000.);
#3466=VECTOR('',#11623,1000.);
#3467=VECTOR('',#11624,1000.);
#3468=VECTOR('',#11627,1000.);
#3469=VECTOR('',#11628,1000.);
#3470=VECTOR('',#11631,1000.);
#3471=VECTOR('',#11632,1000.);
#3472=VECTOR('',#11633,1000.);
#3473=VECTOR('',#11636,1000.);
#3474=VECTOR('',#11637,1000.);
#3475=VECTOR('',#11640,1000.);
#3476=VECTOR('',#11641,1000.);
#3477=VECTOR('',#11642,1000.);
#3478=VECTOR('',#11645,1000.);
#3479=VECTOR('',#11646,1000.);
#3480=VECTOR('',#11649,1000.);
#3481=VECTOR('',#11650,1000.);
#3482=VECTOR('',#11651,1000.);
#3483=VECTOR('',#11654,1000.);
#3484=VECTOR('',#11655,1000.);
#3485=VECTOR('',#11658,1000.);
#3486=VECTOR('',#11659,1000.);
#3487=VECTOR('',#11660,1000.);
#3488=VECTOR('',#11663,1000.);
#3489=VECTOR('',#11664,1000.);
#3490=VECTOR('',#11667,1000.);
#3491=VECTOR('',#11668,1000.);
#3492=VECTOR('',#11669,1000.);
#3493=VECTOR('',#11672,1000.);
#3494=VECTOR('',#11673,1000.);
#3495=VECTOR('',#11676,1000.);
#3496=VECTOR('',#11677,1000.);
#3497=VECTOR('',#11678,1000.);
#3498=VECTOR('',#11681,1000.);
#3499=VECTOR('',#11682,1000.);
#3500=VECTOR('',#11685,1000.);
#3501=VECTOR('',#11686,1000.);
#3502=VECTOR('',#11687,1000.);
#3503=VECTOR('',#11690,1000.);
#3504=VECTOR('',#11691,1000.);
#3505=VECTOR('',#11694,1000.);
#3506=VECTOR('',#11695,1000.);
#3507=VECTOR('',#11696,1000.);
#3508=VECTOR('',#11699,1000.);
#3509=VECTOR('',#11700,1000.);
#3510=VECTOR('',#11703,1000.);
#3511=VECTOR('',#11704,1000.);
#3512=VECTOR('',#11705,1000.);
#3513=VECTOR('',#11708,1000.);
#3514=VECTOR('',#11709,1000.);
#3515=VECTOR('',#11712,1000.);
#3516=VECTOR('',#11713,1000.);
#3517=VECTOR('',#11714,1000.);
#3518=VECTOR('',#11717,1000.);
#3519=VECTOR('',#11718,1000.);
#3520=VECTOR('',#11721,1000.);
#3521=VECTOR('',#11722,1000.);
#3522=VECTOR('',#11723,1000.);
#3523=VECTOR('',#11726,1000.);
#3524=VECTOR('',#11727,1000.);
#3525=VECTOR('',#11730,1000.);
#3526=VECTOR('',#11731,1000.);
#3527=VECTOR('',#11732,1000.);
#3528=VECTOR('',#11735,1000.);
#3529=VECTOR('',#11736,1000.);
#3530=VECTOR('',#11739,1000.);
#3531=VECTOR('',#11740,1000.);
#3532=VECTOR('',#11741,1000.);
#3533=VECTOR('',#11744,1000.);
#3534=VECTOR('',#11745,1000.);
#3535=VECTOR('',#11748,1000.);
#3536=VECTOR('',#11749,1000.);
#3537=VECTOR('',#11750,1000.);
#3538=VECTOR('',#11753,1000.);
#3539=VECTOR('',#11754,1000.);
#3540=VECTOR('',#11757,1000.);
#3541=VECTOR('',#11758,1000.);
#3542=VECTOR('',#11759,1000.);
#3543=VECTOR('',#11762,1000.);
#3544=VECTOR('',#11763,1000.);
#3545=VECTOR('',#11766,1000.);
#3546=VECTOR('',#11767,1000.);
#3547=VECTOR('',#11768,1000.);
#3548=VECTOR('',#11771,1000.);
#3549=VECTOR('',#11772,1000.);
#3550=VECTOR('',#11775,1000.);
#3551=VECTOR('',#11776,1000.);
#3552=VECTOR('',#11777,1000.);
#3553=VECTOR('',#11780,1000.);
#3554=VECTOR('',#11781,1000.);
#3555=VECTOR('',#11784,1000.);
#3556=VECTOR('',#11785,1000.);
#3557=VECTOR('',#11786,1000.);
#3558=VECTOR('',#11789,1000.);
#3559=VECTOR('',#11790,1000.);
#3560=VECTOR('',#11793,1000.);
#3561=VECTOR('',#11794,1000.);
#3562=VECTOR('',#11795,1000.);
#3563=VECTOR('',#11798,1000.);
#3564=VECTOR('',#11799,1000.);
#3565=VECTOR('',#11802,1000.);
#3566=VECTOR('',#11803,1000.);
#3567=VECTOR('',#11804,1000.);
#3568=VECTOR('',#11807,1000.);
#3569=VECTOR('',#11808,1000.);
#3570=VECTOR('',#11811,1000.);
#3571=VECTOR('',#11812,1000.);
#3572=VECTOR('',#11813,1000.);
#3573=VECTOR('',#11816,1000.);
#3574=VECTOR('',#11817,1000.);
#3575=VECTOR('',#11820,1000.);
#3576=VECTOR('',#11821,1000.);
#3577=VECTOR('',#11822,1000.);
#3578=VECTOR('',#11825,1000.);
#3579=VECTOR('',#11826,1000.);
#3580=VECTOR('',#11829,1000.);
#3581=VECTOR('',#11830,1000.);
#3582=VECTOR('',#11831,1000.);
#3583=VECTOR('',#11834,1000.);
#3584=VECTOR('',#11835,1000.);
#3585=VECTOR('',#11838,1000.);
#3586=VECTOR('',#11839,1000.);
#3587=VECTOR('',#11840,1000.);
#3588=VECTOR('',#11843,1000.);
#3589=VECTOR('',#11844,1000.);
#3590=VECTOR('',#11847,1000.);
#3591=VECTOR('',#11848,1000.);
#3592=VECTOR('',#11849,1000.);
#3593=VECTOR('',#11852,1000.);
#3594=VECTOR('',#11853,1000.);
#3595=VECTOR('',#11856,1000.);
#3596=VECTOR('',#11857,1000.);
#3597=VECTOR('',#11858,1000.);
#3598=VECTOR('',#11861,1000.);
#3599=VECTOR('',#11862,1000.);
#3600=VECTOR('',#11865,1000.);
#3601=VECTOR('',#11866,1000.);
#3602=VECTOR('',#11867,1000.);
#3603=VECTOR('',#11870,1000.);
#3604=VECTOR('',#11871,1000.);
#3605=VECTOR('',#11874,1000.);
#3606=VECTOR('',#11875,1000.);
#3607=VECTOR('',#11876,1000.);
#3608=VECTOR('',#11879,1000.);
#3609=VECTOR('',#11880,1000.);
#3610=VECTOR('',#11883,1000.);
#3611=VECTOR('',#11884,1000.);
#3612=VECTOR('',#11885,1000.);
#3613=VECTOR('',#11888,1000.);
#3614=VECTOR('',#11889,1000.);
#3615=VECTOR('',#11892,1000.);
#3616=VECTOR('',#11893,1000.);
#3617=VECTOR('',#11894,1000.);
#3618=VECTOR('',#11897,1000.);
#3619=VECTOR('',#11898,1000.);
#3620=VECTOR('',#11901,1000.);
#3621=VECTOR('',#11902,1000.);
#3622=VECTOR('',#11903,1000.);
#3623=VECTOR('',#11906,1000.);
#3624=VECTOR('',#11907,1000.);
#3625=VECTOR('',#11910,1000.);
#3626=VECTOR('',#11911,1000.);
#3627=VECTOR('',#11912,1000.);
#3628=VECTOR('',#11915,1000.);
#3629=VECTOR('',#11916,1000.);
#3630=VECTOR('',#11937,10.75);
#3631=VECTOR('',#11958,20.);
#3632=VECTOR('',#11989,8.35);
#3633=VECTOR('',#11998,8.35);
#3634=VECTOR('',#12007,3.1);
#3635=VECTOR('',#12010,1000.);
#3636=VECTOR('',#12011,1000.);
#3637=VECTOR('',#12012,1000.);
#3638=VECTOR('',#12013,1000.);
#3639=VECTOR('',#12016,1000.);
#3640=VECTOR('',#12017,1000.);
#3641=VECTOR('',#12018,1000.);
#3642=VECTOR('',#12021,1000.);
#3643=VECTOR('',#12022,1000.);
#3644=VECTOR('',#12025,1000.);
#3645=VECTOR('',#12026,1000.);
#3646=VECTOR('',#12029,1000.);
#4100=VERTEX_POINT('',#13918);
#4101=VERTEX_POINT('',#13919);
#4102=VERTEX_POINT('',#13921);
#4103=VERTEX_POINT('',#13923);
#4104=VERTEX_POINT('',#13927);
#4105=VERTEX_POINT('',#13928);
#4106=VERTEX_POINT('',#13930);
#4107=VERTEX_POINT('',#13932);
#4108=VERTEX_POINT('',#13936);
#4109=VERTEX_POINT('',#13937);
#4110=VERTEX_POINT('',#13939);
#4111=VERTEX_POINT('',#13941);
#4112=VERTEX_POINT('',#13945);
#4113=VERTEX_POINT('',#13946);
#4114=VERTEX_POINT('',#13948);
#4115=VERTEX_POINT('',#13950);
#4116=VERTEX_POINT('',#13954);
#4117=VERTEX_POINT('',#13955);
#4118=VERTEX_POINT('',#13957);
#4119=VERTEX_POINT('',#13959);
#4120=VERTEX_POINT('',#13963);
#4121=VERTEX_POINT('',#13964);
#4122=VERTEX_POINT('',#13966);
#4123=VERTEX_POINT('',#13968);
#4124=VERTEX_POINT('',#13972);
#4125=VERTEX_POINT('',#13973);
#4126=VERTEX_POINT('',#13975);
#4127=VERTEX_POINT('',#13977);
#4128=VERTEX_POINT('',#13981);
#4129=VERTEX_POINT('',#13982);
#4130=VERTEX_POINT('',#13984);
#4131=VERTEX_POINT('',#13986);
#4132=VERTEX_POINT('',#13990);
#4133=VERTEX_POINT('',#13991);
#4134=VERTEX_POINT('',#13993);
#4135=VERTEX_POINT('',#13995);
#4136=VERTEX_POINT('',#13999);
#4137=VERTEX_POINT('',#14000);
#4138=VERTEX_POINT('',#14002);
#4139=VERTEX_POINT('',#14004);
#4140=VERTEX_POINT('',#14008);
#4141=VERTEX_POINT('',#14009);
#4142=VERTEX_POINT('',#14011);
#4143=VERTEX_POINT('',#14013);
#4144=VERTEX_POINT('',#14017);
#4145=VERTEX_POINT('',#14018);
#4146=VERTEX_POINT('',#14020);
#4147=VERTEX_POINT('',#14022);
#4148=VERTEX_POINT('',#14026);
#4149=VERTEX_POINT('',#14027);
#4150=VERTEX_POINT('',#14029);
#4151=VERTEX_POINT('',#14031);
#4152=VERTEX_POINT('',#14035);
#4153=VERTEX_POINT('',#14036);
#4154=VERTEX_POINT('',#14038);
#4155=VERTEX_POINT('',#14040);
#4156=VERTEX_POINT('',#14044);
#4157=VERTEX_POINT('',#14045);
#4158=VERTEX_POINT('',#14047);
#4159=VERTEX_POINT('',#14049);
#4160=VERTEX_POINT('',#14053);
#4161=VERTEX_POINT('',#14054);
#4162=VERTEX_POINT('',#14056);
#4163=VERTEX_POINT('',#14058);
#4164=VERTEX_POINT('',#14062);
#4165=VERTEX_POINT('',#14063);
#4166=VERTEX_POINT('',#14065);
#4167=VERTEX_POINT('',#14067);
#4168=VERTEX_POINT('',#14071);
#4169=VERTEX_POINT('',#14072);
#4170=VERTEX_POINT('',#14074);
#4171=VERTEX_POINT('',#14076);
#4172=VERTEX_POINT('',#14080);
#4173=VERTEX_POINT('',#14081);
#4174=VERTEX_POINT('',#14083);
#4175=VERTEX_POINT('',#14085);
#4176=VERTEX_POINT('',#14089);
#4177=VERTEX_POINT('',#14090);
#4178=VERTEX_POINT('',#14092);
#4179=VERTEX_POINT('',#14094);
#4180=VERTEX_POINT('',#14098);
#4181=VERTEX_POINT('',#14099);
#4182=VERTEX_POINT('',#14101);
#4183=VERTEX_POINT('',#14103);
#4184=VERTEX_POINT('',#14107);
#4185=VERTEX_POINT('',#14108);
#4186=VERTEX_POINT('',#14110);
#4187=VERTEX_POINT('',#14112);
#4188=VERTEX_POINT('',#14116);
#4189=VERTEX_POINT('',#14117);
#4190=VERTEX_POINT('',#14119);
#4191=VERTEX_POINT('',#14121);
#4192=VERTEX_POINT('',#14125);
#4193=VERTEX_POINT('',#14126);
#4194=VERTEX_POINT('',#14128);
#4195=VERTEX_POINT('',#14130);
#4196=VERTEX_POINT('',#14134);
#4197=VERTEX_POINT('',#14135);
#4198=VERTEX_POINT('',#14137);
#4199=VERTEX_POINT('',#14139);
#4200=VERTEX_POINT('',#14143);
#4201=VERTEX_POINT('',#14144);
#4202=VERTEX_POINT('',#14146);
#4203=VERTEX_POINT('',#14148);
#4204=VERTEX_POINT('',#14152);
#4205=VERTEX_POINT('',#14153);
#4206=VERTEX_POINT('',#14155);
#4207=VERTEX_POINT('',#14157);
#4208=VERTEX_POINT('',#14161);
#4209=VERTEX_POINT('',#14162);
#4210=VERTEX_POINT('',#14164);
#4211=VERTEX_POINT('',#14166);
#4212=VERTEX_POINT('',#14170);
#4213=VERTEX_POINT('',#14171);
#4214=VERTEX_POINT('',#14173);
#4215=VERTEX_POINT('',#14175);
#4216=VERTEX_POINT('',#14179);
#4217=VERTEX_POINT('',#14180);
#4218=VERTEX_POINT('',#14182);
#4219=VERTEX_POINT('',#14184);
#4220=VERTEX_POINT('',#14188);
#4221=VERTEX_POINT('',#14189);
#4222=VERTEX_POINT('',#14191);
#4223=VERTEX_POINT('',#14193);
#4224=VERTEX_POINT('',#14197);
#4225=VERTEX_POINT('',#14198);
#4226=VERTEX_POINT('',#14200);
#4227=VERTEX_POINT('',#14202);
#4228=VERTEX_POINT('',#14206);
#4229=VERTEX_POINT('',#14207);
#4230=VERTEX_POINT('',#14209);
#4231=VERTEX_POINT('',#14211);
#4232=VERTEX_POINT('',#14215);
#4233=VERTEX_POINT('',#14216);
#4234=VERTEX_POINT('',#14218);
#4235=VERTEX_POINT('',#14220);
#4236=VERTEX_POINT('',#14224);
#4237=VERTEX_POINT('',#14225);
#4238=VERTEX_POINT('',#14227);
#4239=VERTEX_POINT('',#14229);
#4240=VERTEX_POINT('',#14233);
#4241=VERTEX_POINT('',#14234);
#4242=VERTEX_POINT('',#14236);
#4243=VERTEX_POINT('',#14238);
#4244=VERTEX_POINT('',#14242);
#4245=VERTEX_POINT('',#14243);
#4246=VERTEX_POINT('',#14245);
#4247=VERTEX_POINT('',#14247);
#4248=VERTEX_POINT('',#14251);
#4249=VERTEX_POINT('',#14252);
#4250=VERTEX_POINT('',#14254);
#4251=VERTEX_POINT('',#14256);
#4252=VERTEX_POINT('',#14260);
#4253=VERTEX_POINT('',#14261);
#4254=VERTEX_POINT('',#14263);
#4255=VERTEX_POINT('',#14265);
#4256=VERTEX_POINT('',#14269);
#4257=VERTEX_POINT('',#14270);
#4258=VERTEX_POINT('',#14272);
#4259=VERTEX_POINT('',#14274);
#4260=VERTEX_POINT('',#14278);
#4261=VERTEX_POINT('',#14280);
#4262=VERTEX_POINT('',#14287);
#4263=VERTEX_POINT('',#14289);
#4264=VERTEX_POINT('',#14296);
#4265=VERTEX_POINT('',#14298);
#4266=VERTEX_POINT('',#14305);
#4267=VERTEX_POINT('',#14307);
#4268=VERTEX_POINT('',#14314);
#4269=VERTEX_POINT('',#14316);
#4270=VERTEX_POINT('',#14323);
#4271=VERTEX_POINT('',#14325);
#4272=VERTEX_POINT('',#14332);
#4273=VERTEX_POINT('',#14334);
#4274=VERTEX_POINT('',#14341);
#4275=VERTEX_POINT('',#14343);
#4276=VERTEX_POINT('',#14350);
#4277=VERTEX_POINT('',#14352);
#4278=VERTEX_POINT('',#14359);
#4279=VERTEX_POINT('',#14361);
#4280=VERTEX_POINT('',#14368);
#4281=VERTEX_POINT('',#14370);
#4282=VERTEX_POINT('',#14377);
#4283=VERTEX_POINT('',#14379);
#4284=VERTEX_POINT('',#14386);
#4285=VERTEX_POINT('',#14388);
#4286=VERTEX_POINT('',#14395);
#4287=VERTEX_POINT('',#14397);
#4288=VERTEX_POINT('',#14404);
#4289=VERTEX_POINT('',#14406);
#4290=VERTEX_POINT('',#14413);
#4291=VERTEX_POINT('',#14415);
#4292=VERTEX_POINT('',#14422);
#4293=VERTEX_POINT('',#14424);
#4294=VERTEX_POINT('',#14431);
#4295=VERTEX_POINT('',#14433);
#4296=VERTEX_POINT('',#14440);
#4297=VERTEX_POINT('',#14442);
#4298=VERTEX_POINT('',#14449);
#4299=VERTEX_POINT('',#14451);
#4300=VERTEX_POINT('',#14458);
#4301=VERTEX_POINT('',#14460);
#4302=VERTEX_POINT('',#14467);
#4303=VERTEX_POINT('',#14469);
#4304=VERTEX_POINT('',#14476);
#4305=VERTEX_POINT('',#14478);
#4306=VERTEX_POINT('',#14485);
#4307=VERTEX_POINT('',#14487);
#4308=VERTEX_POINT('',#14494);
#4309=VERTEX_POINT('',#14496);
#4310=VERTEX_POINT('',#14503);
#4311=VERTEX_POINT('',#14505);
#4312=VERTEX_POINT('',#14512);
#4313=VERTEX_POINT('',#14514);
#4314=VERTEX_POINT('',#14521);
#4315=VERTEX_POINT('',#14523);
#4316=VERTEX_POINT('',#14530);
#4317=VERTEX_POINT('',#14532);
#4318=VERTEX_POINT('',#14539);
#4319=VERTEX_POINT('',#14541);
#4320=VERTEX_POINT('',#14548);
#4321=VERTEX_POINT('',#14550);
#4322=VERTEX_POINT('',#14557);
#4323=VERTEX_POINT('',#14559);
#4324=VERTEX_POINT('',#14566);
#4325=VERTEX_POINT('',#14568);
#4326=VERTEX_POINT('',#14575);
#4327=VERTEX_POINT('',#14577);
#4328=VERTEX_POINT('',#14584);
#4329=VERTEX_POINT('',#14586);
#4330=VERTEX_POINT('',#14593);
#4331=VERTEX_POINT('',#14595);
#4332=VERTEX_POINT('',#14602);
#4333=VERTEX_POINT('',#14604);
#4334=VERTEX_POINT('',#14611);
#4335=VERTEX_POINT('',#14613);
#4336=VERTEX_POINT('',#14620);
#4337=VERTEX_POINT('',#14622);
#4338=VERTEX_POINT('',#14629);
#4339=VERTEX_POINT('',#14631);
#4340=VERTEX_POINT('',#14638);
#4341=VERTEX_POINT('',#14639);
#4342=VERTEX_POINT('',#14674);
#4343=VERTEX_POINT('',#14676);
#4344=VERTEX_POINT('',#14713);
#4345=VERTEX_POINT('',#14714);
#4346=VERTEX_POINT('',#14719);
#4347=VERTEX_POINT('',#14799);
#4348=VERTEX_POINT('',#14864);
#4349=VERTEX_POINT('',#14871);
#4350=VERTEX_POINT('',#14872);
#4351=VERTEX_POINT('',#14874);
#4352=VERTEX_POINT('',#14879);
#4353=VERTEX_POINT('',#14968);
#4354=VERTEX_POINT('',#15037);
#4355=VERTEX_POINT('',#15040);
#4356=VERTEX_POINT('',#15042);
#4357=VERTEX_POINT('',#15044);
#4358=VERTEX_POINT('',#15299);
#4359=VERTEX_POINT('',#15502);
#4360=VERTEX_POINT('',#15802);
#4361=VERTEX_POINT('',#16162);
#4362=VERTEX_POINT('',#16230);
#4363=VERTEX_POINT('',#16470);
#4364=VERTEX_POINT('',#16535);
#4365=VERTEX_POINT('',#16671);
#4366=VERTEX_POINT('',#16986);
#4367=VERTEX_POINT('',#16989);
#4368=VERTEX_POINT('',#16991);
#4369=VERTEX_POINT('',#17021);
#4370=VERTEX_POINT('',#17024);
#4371=VERTEX_POINT('',#17025);
#4372=VERTEX_POINT('',#17325);
#4373=VERTEX_POINT('',#17326);
#4374=VERTEX_POINT('',#17627);
#4375=VERTEX_POINT('',#17635);
#4376=VERTEX_POINT('',#17636);
#4377=VERTEX_POINT('',#17638);
#4378=VERTEX_POINT('',#17640);
#4379=VERTEX_POINT('',#17644);
#4380=VERTEX_POINT('',#17646);
#4381=VERTEX_POINT('',#17650);
#4382=VERTEX_POINT('',#17654);
#5025=EDGE_CURVE('',#4100,#4101,#2600,.T.);
#5026=EDGE_CURVE('',#4101,#4102,#2212,.T.);
#5027=EDGE_CURVE('',#4103,#4102,#2601,.T.);
#5028=EDGE_CURVE('',#4103,#4100,#2213,.T.);
#5029=EDGE_CURVE('',#4104,#4105,#2602,.T.);
#5030=EDGE_CURVE('',#4105,#4106,#2214,.T.);
#5031=EDGE_CURVE('',#4107,#4106,#2603,.T.);
#5032=EDGE_CURVE('',#4107,#4104,#2215,.T.);
#5033=EDGE_CURVE('',#4108,#4109,#2604,.T.);
#5034=EDGE_CURVE('',#4109,#4110,#2216,.T.);
#5035=EDGE_CURVE('',#4111,#4110,#2605,.T.);
#5036=EDGE_CURVE('',#4111,#4108,#2217,.T.);
#5037=EDGE_CURVE('',#4112,#4113,#2606,.T.);
#5038=EDGE_CURVE('',#4113,#4114,#2218,.T.);
#5039=EDGE_CURVE('',#4115,#4114,#2607,.T.);
#5040=EDGE_CURVE('',#4115,#4112,#2219,.T.);
#5041=EDGE_CURVE('',#4116,#4117,#2608,.T.);
#5042=EDGE_CURVE('',#4117,#4118,#2220,.T.);
#5043=EDGE_CURVE('',#4119,#4118,#2609,.T.);
#5044=EDGE_CURVE('',#4119,#4116,#2221,.T.);
#5045=EDGE_CURVE('',#4120,#4121,#2610,.T.);
#5046=EDGE_CURVE('',#4121,#4122,#2222,.T.);
#5047=EDGE_CURVE('',#4123,#4122,#2611,.T.);
#5048=EDGE_CURVE('',#4123,#4120,#2223,.T.);
#5049=EDGE_CURVE('',#4124,#4125,#2612,.T.);
#5050=EDGE_CURVE('',#4125,#4126,#2224,.T.);
#5051=EDGE_CURVE('',#4127,#4126,#2613,.T.);
#5052=EDGE_CURVE('',#4127,#4124,#2225,.T.);
#5053=EDGE_CURVE('',#4128,#4129,#2614,.T.);
#5054=EDGE_CURVE('',#4129,#4130,#2226,.T.);
#5055=EDGE_CURVE('',#4131,#4130,#2615,.T.);
#5056=EDGE_CURVE('',#4131,#4128,#2227,.T.);
#5057=EDGE_CURVE('',#4132,#4133,#2616,.T.);
#5058=EDGE_CURVE('',#4133,#4134,#2228,.T.);
#5059=EDGE_CURVE('',#4135,#4134,#2617,.T.);
#5060=EDGE_CURVE('',#4135,#4132,#2229,.T.);
#5061=EDGE_CURVE('',#4136,#4137,#2618,.T.);
#5062=EDGE_CURVE('',#4137,#4138,#2230,.T.);
#5063=EDGE_CURVE('',#4139,#4138,#2619,.T.);
#5064=EDGE_CURVE('',#4139,#4136,#2231,.T.);
#5065=EDGE_CURVE('',#4140,#4141,#2620,.T.);
#5066=EDGE_CURVE('',#4141,#4142,#2232,.T.);
#5067=EDGE_CURVE('',#4143,#4142,#2621,.T.);
#5068=EDGE_CURVE('',#4143,#4140,#2233,.T.);
#5069=EDGE_CURVE('',#4144,#4145,#2622,.T.);
#5070=EDGE_CURVE('',#4145,#4146,#2234,.T.);
#5071=EDGE_CURVE('',#4147,#4146,#2623,.T.);
#5072=EDGE_CURVE('',#4147,#4144,#2235,.T.);
#5073=EDGE_CURVE('',#4148,#4149,#2624,.T.);
#5074=EDGE_CURVE('',#4149,#4150,#2236,.T.);
#5075=EDGE_CURVE('',#4151,#4150,#2625,.T.);
#5076=EDGE_CURVE('',#4151,#4148,#2237,.T.);
#5077=EDGE_CURVE('',#4152,#4153,#2626,.T.);
#5078=EDGE_CURVE('',#4153,#4154,#2238,.T.);
#5079=EDGE_CURVE('',#4155,#4154,#2627,.T.);
#5080=EDGE_CURVE('',#4155,#4152,#2239,.T.);
#5081=EDGE_CURVE('',#4156,#4157,#2628,.T.);
#5082=EDGE_CURVE('',#4157,#4158,#2240,.T.);
#5083=EDGE_CURVE('',#4159,#4158,#2629,.T.);
#5084=EDGE_CURVE('',#4159,#4156,#2241,.T.);
#5085=EDGE_CURVE('',#4160,#4161,#2630,.T.);
#5086=EDGE_CURVE('',#4161,#4162,#2242,.T.);
#5087=EDGE_CURVE('',#4163,#4162,#2631,.T.);
#5088=EDGE_CURVE('',#4163,#4160,#2243,.T.);
#5089=EDGE_CURVE('',#4164,#4165,#2632,.T.);
#5090=EDGE_CURVE('',#4165,#4166,#2244,.T.);
#5091=EDGE_CURVE('',#4167,#4166,#2633,.T.);
#5092=EDGE_CURVE('',#4167,#4164,#2245,.T.);
#5093=EDGE_CURVE('',#4168,#4169,#2634,.T.);
#5094=EDGE_CURVE('',#4169,#4170,#2246,.T.);
#5095=EDGE_CURVE('',#4171,#4170,#2635,.T.);
#5096=EDGE_CURVE('',#4171,#4168,#2247,.T.);
#5097=EDGE_CURVE('',#4172,#4173,#2636,.T.);
#5098=EDGE_CURVE('',#4173,#4174,#2248,.T.);
#5099=EDGE_CURVE('',#4175,#4174,#2637,.T.);
#5100=EDGE_CURVE('',#4175,#4172,#2249,.T.);
#5101=EDGE_CURVE('',#4176,#4177,#2638,.T.);
#5102=EDGE_CURVE('',#4177,#4178,#2250,.T.);
#5103=EDGE_CURVE('',#4179,#4178,#2639,.T.);
#5104=EDGE_CURVE('',#4179,#4176,#2251,.T.);
#5105=EDGE_CURVE('',#4180,#4181,#2640,.T.);
#5106=EDGE_CURVE('',#4181,#4182,#2252,.T.);
#5107=EDGE_CURVE('',#4183,#4182,#2641,.T.);
#5108=EDGE_CURVE('',#4183,#4180,#2253,.T.);
#5109=EDGE_CURVE('',#4184,#4185,#2642,.T.);
#5110=EDGE_CURVE('',#4185,#4186,#2254,.T.);
#5111=EDGE_CURVE('',#4187,#4186,#2643,.T.);
#5112=EDGE_CURVE('',#4187,#4184,#2255,.T.);
#5113=EDGE_CURVE('',#4188,#4189,#2644,.T.);
#5114=EDGE_CURVE('',#4189,#4190,#2256,.T.);
#5115=EDGE_CURVE('',#4191,#4190,#2645,.T.);
#5116=EDGE_CURVE('',#4191,#4188,#2257,.T.);
#5117=EDGE_CURVE('',#4192,#4193,#2646,.T.);
#5118=EDGE_CURVE('',#4193,#4194,#2258,.T.);
#5119=EDGE_CURVE('',#4195,#4194,#2647,.T.);
#5120=EDGE_CURVE('',#4195,#4192,#2259,.T.);
#5121=EDGE_CURVE('',#4196,#4197,#2648,.T.);
#5122=EDGE_CURVE('',#4197,#4198,#2260,.T.);
#5123=EDGE_CURVE('',#4199,#4198,#2649,.T.);
#5124=EDGE_CURVE('',#4199,#4196,#2261,.T.);
#5125=EDGE_CURVE('',#4200,#4201,#2650,.T.);
#5126=EDGE_CURVE('',#4201,#4202,#2262,.T.);
#5127=EDGE_CURVE('',#4203,#4202,#2651,.T.);
#5128=EDGE_CURVE('',#4203,#4200,#2263,.T.);
#5129=EDGE_CURVE('',#4204,#4205,#2652,.T.);
#5130=EDGE_CURVE('',#4205,#4206,#2264,.T.);
#5131=EDGE_CURVE('',#4207,#4206,#2653,.T.);
#5132=EDGE_CURVE('',#4207,#4204,#2265,.T.);
#5133=EDGE_CURVE('',#4208,#4209,#2654,.T.);
#5134=EDGE_CURVE('',#4209,#4210,#2266,.T.);
#5135=EDGE_CURVE('',#4211,#4210,#2655,.T.);
#5136=EDGE_CURVE('',#4211,#4208,#2267,.T.);
#5137=EDGE_CURVE('',#4212,#4213,#2656,.T.);
#5138=EDGE_CURVE('',#4213,#4214,#2268,.T.);
#5139=EDGE_CURVE('',#4215,#4214,#2657,.T.);
#5140=EDGE_CURVE('',#4215,#4212,#2269,.T.);
#5141=EDGE_CURVE('',#4216,#4217,#2658,.T.);
#5142=EDGE_CURVE('',#4217,#4218,#2270,.T.);
#5143=EDGE_CURVE('',#4219,#4218,#2659,.T.);
#5144=EDGE_CURVE('',#4219,#4216,#2271,.T.);
#5145=EDGE_CURVE('',#4220,#4221,#2660,.T.);
#5146=EDGE_CURVE('',#4221,#4222,#2272,.T.);
#5147=EDGE_CURVE('',#4223,#4222,#2661,.T.);
#5148=EDGE_CURVE('',#4223,#4220,#2273,.T.);
#5149=EDGE_CURVE('',#4224,#4225,#2662,.T.);
#5150=EDGE_CURVE('',#4225,#4226,#2274,.T.);
#5151=EDGE_CURVE('',#4227,#4226,#2663,.T.);
#5152=EDGE_CURVE('',#4227,#4224,#2275,.T.);
#5153=EDGE_CURVE('',#4228,#4229,#2664,.T.);
#5154=EDGE_CURVE('',#4229,#4230,#2276,.T.);
#5155=EDGE_CURVE('',#4231,#4230,#2665,.T.);
#5156=EDGE_CURVE('',#4231,#4228,#2277,.T.);
#5157=EDGE_CURVE('',#4232,#4233,#2666,.T.);
#5158=EDGE_CURVE('',#4233,#4234,#2278,.T.);
#5159=EDGE_CURVE('',#4235,#4234,#2667,.T.);
#5160=EDGE_CURVE('',#4235,#4232,#2279,.T.);
#5161=EDGE_CURVE('',#4236,#4237,#2668,.T.);
#5162=EDGE_CURVE('',#4237,#4238,#2280,.T.);
#5163=EDGE_CURVE('',#4239,#4238,#2669,.T.);
#5164=EDGE_CURVE('',#4239,#4236,#2281,.T.);
#5165=EDGE_CURVE('',#4240,#4241,#2670,.T.);
#5166=EDGE_CURVE('',#4241,#4242,#2282,.T.);
#5167=EDGE_CURVE('',#4243,#4242,#2671,.T.);
#5168=EDGE_CURVE('',#4243,#4240,#2283,.T.);
#5169=EDGE_CURVE('',#4244,#4245,#2672,.T.);
#5170=EDGE_CURVE('',#4245,#4246,#2284,.T.);
#5171=EDGE_CURVE('',#4247,#4246,#2673,.T.);
#5172=EDGE_CURVE('',#4247,#4244,#2285,.T.);
#5173=EDGE_CURVE('',#4248,#4249,#2674,.T.);
#5174=EDGE_CURVE('',#4249,#4250,#2286,.T.);
#5175=EDGE_CURVE('',#4251,#4250,#2675,.T.);
#5176=EDGE_CURVE('',#4251,#4248,#2287,.T.);
#5177=EDGE_CURVE('',#4252,#4253,#2676,.T.);
#5178=EDGE_CURVE('',#4253,#4254,#2288,.T.);
#5179=EDGE_CURVE('',#4255,#4254,#2677,.T.);
#5180=EDGE_CURVE('',#4255,#4252,#2289,.T.);
#5181=EDGE_CURVE('',#4256,#4257,#2678,.T.);
#5182=EDGE_CURVE('',#4257,#4258,#2290,.T.);
#5183=EDGE_CURVE('',#4259,#4258,#2679,.T.);
#5184=EDGE_CURVE('',#4259,#4256,#2291,.T.);
#5185=EDGE_CURVE('',#4260,#4254,#2680,.T.);
#5186=EDGE_CURVE('',#4261,#4260,#2681,.T.);
#5187=EDGE_CURVE('',#4261,#4255,#2682,.T.);
#5188=EDGE_CURVE('',#4257,#4260,#2683,.T.);
#5189=EDGE_CURVE('',#4256,#4261,#2684,.T.);
#5190=EDGE_CURVE('',#4262,#4250,#2685,.T.);
#5191=EDGE_CURVE('',#4263,#4262,#2686,.T.);
#5192=EDGE_CURVE('',#4263,#4251,#2687,.T.);
#5193=EDGE_CURVE('',#4253,#4262,#2688,.T.);
#5194=EDGE_CURVE('',#4252,#4263,#2689,.T.);
#5195=EDGE_CURVE('',#4264,#4246,#2690,.T.);
#5196=EDGE_CURVE('',#4265,#4264,#2691,.T.);
#5197=EDGE_CURVE('',#4265,#4247,#2692,.T.);
#5198=EDGE_CURVE('',#4249,#4264,#2693,.T.);
#5199=EDGE_CURVE('',#4248,#4265,#2694,.T.);
#5200=EDGE_CURVE('',#4266,#4242,#2695,.T.);
#5201=EDGE_CURVE('',#4267,#4266,#2696,.T.);
#5202=EDGE_CURVE('',#4267,#4243,#2697,.T.);
#5203=EDGE_CURVE('',#4245,#4266,#2698,.T.);
#5204=EDGE_CURVE('',#4244,#4267,#2699,.T.);
#5205=EDGE_CURVE('',#4268,#4238,#2700,.T.);
#5206=EDGE_CURVE('',#4269,#4268,#2701,.T.);
#5207=EDGE_CURVE('',#4269,#4239,#2702,.T.);
#5208=EDGE_CURVE('',#4241,#4268,#2703,.T.);
#5209=EDGE_CURVE('',#4240,#4269,#2704,.T.);
#5210=EDGE_CURVE('',#4270,#4234,#2705,.T.);
#5211=EDGE_CURVE('',#4271,#4270,#2706,.T.);
#5212=EDGE_CURVE('',#4271,#4235,#2707,.T.);
#5213=EDGE_CURVE('',#4237,#4270,#2708,.T.);
#5214=EDGE_CURVE('',#4236,#4271,#2709,.T.);
#5215=EDGE_CURVE('',#4272,#4230,#2710,.T.);
#5216=EDGE_CURVE('',#4273,#4272,#2711,.T.);
#5217=EDGE_CURVE('',#4273,#4231,#2712,.T.);
#5218=EDGE_CURVE('',#4233,#4272,#2713,.T.);
#5219=EDGE_CURVE('',#4232,#4273,#2714,.T.);
#5220=EDGE_CURVE('',#4274,#4226,#2715,.T.);
#5221=EDGE_CURVE('',#4275,#4274,#2716,.T.);
#5222=EDGE_CURVE('',#4275,#4227,#2717,.T.);
#5223=EDGE_CURVE('',#4229,#4274,#2718,.T.);
#5224=EDGE_CURVE('',#4228,#4275,#2719,.T.);
#5225=EDGE_CURVE('',#4276,#4222,#2720,.T.);
#5226=EDGE_CURVE('',#4277,#4276,#2721,.T.);
#5227=EDGE_CURVE('',#4277,#4223,#2722,.T.);
#5228=EDGE_CURVE('',#4225,#4276,#2723,.T.);
#5229=EDGE_CURVE('',#4224,#4277,#2724,.T.);
#5230=EDGE_CURVE('',#4278,#4218,#2725,.T.);
#5231=EDGE_CURVE('',#4279,#4278,#2726,.T.);
#5232=EDGE_CURVE('',#4279,#4219,#2727,.T.);
#5233=EDGE_CURVE('',#4221,#4278,#2728,.T.);
#5234=EDGE_CURVE('',#4220,#4279,#2729,.T.);
#5235=EDGE_CURVE('',#4280,#4214,#2730,.T.);
#5236=EDGE_CURVE('',#4281,#4280,#2731,.T.);
#5237=EDGE_CURVE('',#4281,#4215,#2732,.T.);
#5238=EDGE_CURVE('',#4217,#4280,#2733,.T.);
#5239=EDGE_CURVE('',#4216,#4281,#2734,.T.);
#5240=EDGE_CURVE('',#4282,#4210,#2735,.T.);
#5241=EDGE_CURVE('',#4283,#4282,#2736,.T.);
#5242=EDGE_CURVE('',#4283,#4211,#2737,.T.);
#5243=EDGE_CURVE('',#4213,#4282,#2738,.T.);
#5244=EDGE_CURVE('',#4212,#4283,#2739,.T.);
#5245=EDGE_CURVE('',#4284,#4206,#2740,.T.);
#5246=EDGE_CURVE('',#4285,#4284,#2741,.T.);
#5247=EDGE_CURVE('',#4285,#4207,#2742,.T.);
#5248=EDGE_CURVE('',#4209,#4284,#2743,.T.);
#5249=EDGE_CURVE('',#4208,#4285,#2744,.T.);
#5250=EDGE_CURVE('',#4286,#4202,#2745,.T.);
#5251=EDGE_CURVE('',#4287,#4286,#2746,.T.);
#5252=EDGE_CURVE('',#4287,#4203,#2747,.T.);
#5253=EDGE_CURVE('',#4205,#4286,#2748,.T.);
#5254=EDGE_CURVE('',#4204,#4287,#2749,.T.);
#5255=EDGE_CURVE('',#4288,#4198,#2750,.T.);
#5256=EDGE_CURVE('',#4289,#4288,#2751,.T.);
#5257=EDGE_CURVE('',#4289,#4199,#2752,.T.);
#5258=EDGE_CURVE('',#4201,#4288,#2753,.T.);
#5259=EDGE_CURVE('',#4200,#4289,#2754,.T.);
#5260=EDGE_CURVE('',#4290,#4194,#2755,.T.);
#5261=EDGE_CURVE('',#4291,#4290,#2756,.T.);
#5262=EDGE_CURVE('',#4291,#4195,#2757,.T.);
#5263=EDGE_CURVE('',#4197,#4290,#2758,.T.);
#5264=EDGE_CURVE('',#4196,#4291,#2759,.T.);
#5265=EDGE_CURVE('',#4292,#4190,#2760,.T.);
#5266=EDGE_CURVE('',#4293,#4292,#2761,.T.);
#5267=EDGE_CURVE('',#4293,#4191,#2762,.T.);
#5268=EDGE_CURVE('',#4193,#4292,#2763,.T.);
#5269=EDGE_CURVE('',#4192,#4293,#2764,.T.);
#5270=EDGE_CURVE('',#4294,#4186,#2765,.T.);
#5271=EDGE_CURVE('',#4295,#4294,#2766,.T.);
#5272=EDGE_CURVE('',#4295,#4187,#2767,.T.);
#5273=EDGE_CURVE('',#4189,#4294,#2768,.T.);
#5274=EDGE_CURVE('',#4188,#4295,#2769,.T.);
#5275=EDGE_CURVE('',#4296,#4182,#2770,.T.);
#5276=EDGE_CURVE('',#4297,#4296,#2771,.T.);
#5277=EDGE_CURVE('',#4297,#4183,#2772,.T.);
#5278=EDGE_CURVE('',#4185,#4296,#2773,.T.);
#5279=EDGE_CURVE('',#4184,#4297,#2774,.T.);
#5280=EDGE_CURVE('',#4298,#4178,#2775,.T.);
#5281=EDGE_CURVE('',#4299,#4298,#2776,.T.);
#5282=EDGE_CURVE('',#4299,#4179,#2777,.T.);
#5283=EDGE_CURVE('',#4181,#4298,#2778,.T.);
#5284=EDGE_CURVE('',#4180,#4299,#2779,.T.);
#5285=EDGE_CURVE('',#4300,#4174,#2780,.T.);
#5286=EDGE_CURVE('',#4301,#4300,#2781,.T.);
#5287=EDGE_CURVE('',#4301,#4175,#2782,.T.);
#5288=EDGE_CURVE('',#4177,#4300,#2783,.T.);
#5289=EDGE_CURVE('',#4176,#4301,#2784,.T.);
#5290=EDGE_CURVE('',#4302,#4170,#2785,.T.);
#5291=EDGE_CURVE('',#4303,#4302,#2786,.T.);
#5292=EDGE_CURVE('',#4303,#4171,#2787,.T.);
#5293=EDGE_CURVE('',#4173,#4302,#2788,.T.);
#5294=EDGE_CURVE('',#4172,#4303,#2789,.T.);
#5295=EDGE_CURVE('',#4304,#4166,#2790,.T.);
#5296=EDGE_CURVE('',#4305,#4304,#2791,.T.);
#5297=EDGE_CURVE('',#4305,#4167,#2792,.T.);
#5298=EDGE_CURVE('',#4169,#4304,#2793,.T.);
#5299=EDGE_CURVE('',#4168,#4305,#2794,.T.);
#5300=EDGE_CURVE('',#4306,#4162,#2795,.T.);
#5301=EDGE_CURVE('',#4307,#4306,#2796,.T.);
#5302=EDGE_CURVE('',#4307,#4163,#2797,.T.);
#5303=EDGE_CURVE('',#4165,#4306,#2798,.T.);
#5304=EDGE_CURVE('',#4164,#4307,#2799,.T.);
#5305=EDGE_CURVE('',#4308,#4158,#2800,.T.);
#5306=EDGE_CURVE('',#4309,#4308,#2801,.T.);
#5307=EDGE_CURVE('',#4309,#4159,#2802,.T.);
#5308=EDGE_CURVE('',#4161,#4308,#2803,.T.);
#5309=EDGE_CURVE('',#4160,#4309,#2804,.T.);
#5310=EDGE_CURVE('',#4310,#4154,#2805,.T.);
#5311=EDGE_CURVE('',#4311,#4310,#2806,.T.);
#5312=EDGE_CURVE('',#4311,#4155,#2807,.T.);
#5313=EDGE_CURVE('',#4157,#4310,#2808,.T.);
#5314=EDGE_CURVE('',#4156,#4311,#2809,.T.);
#5315=EDGE_CURVE('',#4312,#4150,#2810,.T.);
#5316=EDGE_CURVE('',#4313,#4312,#2811,.T.);
#5317=EDGE_CURVE('',#4313,#4151,#2812,.T.);
#5318=EDGE_CURVE('',#4153,#4312,#2813,.T.);
#5319=EDGE_CURVE('',#4152,#4313,#2814,.T.);
#5320=EDGE_CURVE('',#4314,#4146,#2815,.T.);
#5321=EDGE_CURVE('',#4315,#4314,#2816,.T.);
#5322=EDGE_CURVE('',#4315,#4147,#2817,.T.);
#5323=EDGE_CURVE('',#4149,#4314,#2818,.T.);
#5324=EDGE_CURVE('',#4148,#4315,#2819,.T.);
#5325=EDGE_CURVE('',#4316,#4142,#2820,.T.);
#5326=EDGE_CURVE('',#4317,#4316,#2821,.T.);
#5327=EDGE_CURVE('',#4317,#4143,#2822,.T.);
#5328=EDGE_CURVE('',#4145,#4316,#2823,.T.);
#5329=EDGE_CURVE('',#4144,#4317,#2824,.T.);
#5330=EDGE_CURVE('',#4318,#4138,#2825,.T.);
#5331=EDGE_CURVE('',#4319,#4318,#2826,.T.);
#5332=EDGE_CURVE('',#4319,#4139,#2827,.T.);
#5333=EDGE_CURVE('',#4141,#4318,#2828,.T.);
#5334=EDGE_CURVE('',#4140,#4319,#2829,.T.);
#5335=EDGE_CURVE('',#4320,#4134,#2830,.T.);
#5336=EDGE_CURVE('',#4321,#4320,#2831,.T.);
#5337=EDGE_CURVE('',#4321,#4135,#2832,.T.);
#5338=EDGE_CURVE('',#4137,#4320,#2833,.T.);
#5339=EDGE_CURVE('',#4136,#4321,#2834,.T.);
#5340=EDGE_CURVE('',#4322,#4130,#2835,.T.);
#5341=EDGE_CURVE('',#4323,#4322,#2836,.T.);
#5342=EDGE_CURVE('',#4323,#4131,#2837,.T.);
#5343=EDGE_CURVE('',#4133,#4322,#2838,.T.);
#5344=EDGE_CURVE('',#4132,#4323,#2839,.T.);
#5345=EDGE_CURVE('',#4324,#4126,#2840,.T.);
#5346=EDGE_CURVE('',#4325,#4324,#2841,.T.);
#5347=EDGE_CURVE('',#4325,#4127,#2842,.T.);
#5348=EDGE_CURVE('',#4129,#4324,#2843,.T.);
#5349=EDGE_CURVE('',#4128,#4325,#2844,.T.);
#5350=EDGE_CURVE('',#4326,#4122,#2845,.T.);
#5351=EDGE_CURVE('',#4327,#4326,#2846,.T.);
#5352=EDGE_CURVE('',#4327,#4123,#2847,.T.);
#5353=EDGE_CURVE('',#4125,#4326,#2848,.T.);
#5354=EDGE_CURVE('',#4124,#4327,#2849,.T.);
#5355=EDGE_CURVE('',#4328,#4118,#2850,.T.);
#5356=EDGE_CURVE('',#4329,#4328,#2851,.T.);
#5357=EDGE_CURVE('',#4329,#4119,#2852,.T.);
#5358=EDGE_CURVE('',#4121,#4328,#2853,.T.);
#5359=EDGE_CURVE('',#4120,#4329,#2854,.T.);
#5360=EDGE_CURVE('',#4330,#4114,#2855,.T.);
#5361=EDGE_CURVE('',#4331,#4330,#2856,.T.);
#5362=EDGE_CURVE('',#4331,#4115,#2857,.T.);
#5363=EDGE_CURVE('',#4117,#4330,#2858,.T.);
#5364=EDGE_CURVE('',#4116,#4331,#2859,.T.);
#5365=EDGE_CURVE('',#4332,#4110,#2860,.T.);
#5366=EDGE_CURVE('',#4333,#4332,#2861,.T.);
#5367=EDGE_CURVE('',#4333,#4111,#2862,.T.);
#5368=EDGE_CURVE('',#4113,#4332,#2863,.T.);
#5369=EDGE_CURVE('',#4112,#4333,#2864,.T.);
#5370=EDGE_CURVE('',#4334,#4106,#2865,.T.);
#5371=EDGE_CURVE('',#4335,#4334,#2866,.T.);
#5372=EDGE_CURVE('',#4335,#4107,#2867,.T.);
#5373=EDGE_CURVE('',#4109,#4334,#2868,.T.);
#5374=EDGE_CURVE('',#4108,#4335,#2869,.T.);
#5375=EDGE_CURVE('',#4336,#4102,#2870,.T.);
#5376=EDGE_CURVE('',#4337,#4336,#2871,.T.);
#5377=EDGE_CURVE('',#4337,#4103,#2872,.T.);
#5378=EDGE_CURVE('',#4105,#4336,#2873,.T.);
#5379=EDGE_CURVE('',#4104,#4337,#2874,.T.);
#5380=EDGE_CURVE('',#4338,#4258,#2875,.T.);
#5381=EDGE_CURVE('',#4339,#4338,#2876,.T.);
#5382=EDGE_CURVE('',#4339,#4259,#2877,.T.);
#5383=EDGE_CURVE('',#4101,#4338,#2878,.T.);
#5384=EDGE_CURVE('',#4100,#4339,#2879,.T.);
#5385=EDGE_CURVE('',#4340,#4341,#554,.T.);
#5386=EDGE_CURVE('',#4341,#4342,#2292,.T.);
#5387=EDGE_CURVE('',#4342,#4343,#555,.T.);
#5388=EDGE_CURVE('',#4343,#4340,#2293,.T.);
#5389=EDGE_CURVE('',#4344,#4345,#556,.T.);
#5390=EDGE_CURVE('',#4345,#4346,#557,.T.);
#5391=EDGE_CURVE('',#4346,#4347,#558,.T.);
#5392=EDGE_CURVE('',#4347,#4348,#559,.T.);
#5393=EDGE_CURVE('',#4348,#4344,#2294,.T.);
#5394=EDGE_CURVE('',#4349,#4350,#2295,.T.);
#5395=EDGE_CURVE('',#4350,#4351,#560,.T.);
#5396=EDGE_CURVE('',#4351,#4352,#561,.T.);
#5397=EDGE_CURVE('',#4352,#4353,#562,.T.);
#5398=EDGE_CURVE('',#4353,#4349,#563,.T.);
#5399=EDGE_CURVE('',#4354,#4354,#2296,.T.);
#5400=EDGE_CURVE('',#4355,#4355,#2297,.T.);
#5401=EDGE_CURVE('',#4355,#4356,#2880,.T.);
#5402=EDGE_CURVE('',#4356,#4357,#564,.T.);
#5403=EDGE_CURVE('',#4357,#4352,#565,.T.);
#5404=EDGE_CURVE('',#4352,#4358,#566,.T.);
#5405=EDGE_CURVE('',#4358,#4359,#567,.T.);
#5406=EDGE_CURVE('',#4359,#4346,#568,.T.);
#5407=EDGE_CURVE('',#4346,#4360,#569,.T.);
#5408=EDGE_CURVE('',#4360,#4356,#570,.T.);
#5409=EDGE_CURVE('',#4361,#4359,#2298,.T.);
#5410=EDGE_CURVE('',#4361,#4346,#571,.T.);
#5411=EDGE_CURVE('',#4362,#4358,#2299,.T.);
#5412=EDGE_CURVE('',#4362,#4341,#406,.T.);
#5413=EDGE_CURVE('',#4340,#4361,#407,.T.);
#5414=EDGE_CURVE('',#4352,#4362,#572,.T.);
#5415=EDGE_CURVE('',#4346,#4363,#573,.T.);
#5416=EDGE_CURVE('',#4360,#4363,#2300,.T.);
#5417=EDGE_CURVE('',#4363,#4343,#408,.T.);
#5418=EDGE_CURVE('',#4342,#4364,#409,.T.);
#5419=EDGE_CURVE('',#4357,#4364,#2301,.T.);
#5420=EDGE_CURVE('',#4364,#4352,#574,.T.);
#5421=EDGE_CURVE('',#4365,#4365,#2302,.T.);
#5422=EDGE_CURVE('',#4365,#4354,#2881,.T.);
#5423=EDGE_CURVE('',#4353,#4364,#2303,.T.);
#5424=EDGE_CURVE('',#4349,#4342,#2304,.T.);
#5425=EDGE_CURVE('',#4350,#4341,#2305,.T.);
#5426=EDGE_CURVE('',#4351,#4362,#2306,.T.);
#5427=EDGE_CURVE('',#4363,#4345,#2307,.T.);
#5428=EDGE_CURVE('',#4343,#4344,#2308,.T.);
#5429=EDGE_CURVE('',#4340,#4348,#2309,.T.);
#5430=EDGE_CURVE('',#4361,#4347,#2310,.T.);
#5431=EDGE_CURVE('',#4366,#4366,#2311,.T.);
#5432=EDGE_CURVE('',#4367,#4367,#2312,.T.);
#5433=EDGE_CURVE('',#4367,#4368,#2882,.T.);
#5434=EDGE_CURVE('',#4368,#4368,#2313,.T.);
#5435=EDGE_CURVE('',#4368,#4369,#2314,.T.);
#5436=EDGE_CURVE('',#4369,#4369,#2315,.T.);
#5437=EDGE_CURVE('',#4370,#4371,#575,.T.);
#5438=EDGE_CURVE('',#4371,#4370,#576,.T.);
#5439=EDGE_CURVE('',#4372,#4373,#577,.T.);
#5440=EDGE_CURVE('',#4373,#4372,#578,.T.);
#5441=EDGE_CURVE('',#4369,#4374,#2883,.T.);
#5442=EDGE_CURVE('',#4374,#4374,#2316,.T.);
#5443=EDGE_CURVE('',#4366,#4367,#2317,.T.);
#5444=EDGE_CURVE('',#4371,#4373,#2884,.T.);
#5445=EDGE_CURVE('',#4375,#4376,#2885,.T.);
#5446=EDGE_CURVE('',#4377,#4375,#2886,.T.);
#5447=EDGE_CURVE('',#4378,#4377,#2887,.T.);
#5448=EDGE_CURVE('',#4376,#4378,#2888,.T.);
#5449=EDGE_CURVE('',#4379,#4375,#2889,.T.);
#5450=EDGE_CURVE('',#4380,#4379,#2890,.T.);
#5451=EDGE_CURVE('',#4380,#4377,#2891,.T.);
#5452=EDGE_CURVE('',#4381,#4380,#2892,.T.);
#5453=EDGE_CURVE('',#4381,#4378,#2893,.T.);
#5454=EDGE_CURVE('',#4382,#4381,#2894,.T.);
#5455=EDGE_CURVE('',#4382,#4376,#2895,.T.);
#5456=EDGE_CURVE('',#4379,#4382,#2896,.T.);
#6424=ORIENTED_EDGE('',*,*,#5025,.T.);
#6425=ORIENTED_EDGE('',*,*,#5026,.T.);
#6426=ORIENTED_EDGE('',*,*,#5027,.F.);
#6427=ORIENTED_EDGE('',*,*,#5028,.T.);
#6428=ORIENTED_EDGE('',*,*,#5029,.T.);
#6429=ORIENTED_EDGE('',*,*,#5030,.T.);
#6430=ORIENTED_EDGE('',*,*,#5031,.F.);
#6431=ORIENTED_EDGE('',*,*,#5032,.T.);
#6432=ORIENTED_EDGE('',*,*,#5033,.T.);
#6433=ORIENTED_EDGE('',*,*,#5034,.T.);
#6434=ORIENTED_EDGE('',*,*,#5035,.F.);
#6435=ORIENTED_EDGE('',*,*,#5036,.T.);
#6436=ORIENTED_EDGE('',*,*,#5037,.T.);
#6437=ORIENTED_EDGE('',*,*,#5038,.T.);
#6438=ORIENTED_EDGE('',*,*,#5039,.F.);
#6439=ORIENTED_EDGE('',*,*,#5040,.T.);
#6440=ORIENTED_EDGE('',*,*,#5041,.T.);
#6441=ORIENTED_EDGE('',*,*,#5042,.T.);
#6442=ORIENTED_EDGE('',*,*,#5043,.F.);
#6443=ORIENTED_EDGE('',*,*,#5044,.T.);
#6444=ORIENTED_EDGE('',*,*,#5045,.T.);
#6445=ORIENTED_EDGE('',*,*,#5046,.T.);
#6446=ORIENTED_EDGE('',*,*,#5047,.F.);
#6447=ORIENTED_EDGE('',*,*,#5048,.T.);
#6448=ORIENTED_EDGE('',*,*,#5049,.T.);
#6449=ORIENTED_EDGE('',*,*,#5050,.T.);
#6450=ORIENTED_EDGE('',*,*,#5051,.F.);
#6451=ORIENTED_EDGE('',*,*,#5052,.T.);
#6452=ORIENTED_EDGE('',*,*,#5053,.T.);
#6453=ORIENTED_EDGE('',*,*,#5054,.T.);
#6454=ORIENTED_EDGE('',*,*,#5055,.F.);
#6455=ORIENTED_EDGE('',*,*,#5056,.T.);
#6456=ORIENTED_EDGE('',*,*,#5057,.T.);
#6457=ORIENTED_EDGE('',*,*,#5058,.T.);
#6458=ORIENTED_EDGE('',*,*,#5059,.F.);
#6459=ORIENTED_EDGE('',*,*,#5060,.T.);
#6460=ORIENTED_EDGE('',*,*,#5061,.T.);
#6461=ORIENTED_EDGE('',*,*,#5062,.T.);
#6462=ORIENTED_EDGE('',*,*,#5063,.F.);
#6463=ORIENTED_EDGE('',*,*,#5064,.T.);
#6464=ORIENTED_EDGE('',*,*,#5065,.T.);
#6465=ORIENTED_EDGE('',*,*,#5066,.T.);
#6466=ORIENTED_EDGE('',*,*,#5067,.F.);
#6467=ORIENTED_EDGE('',*,*,#5068,.T.);
#6468=ORIENTED_EDGE('',*,*,#5069,.T.);
#6469=ORIENTED_EDGE('',*,*,#5070,.T.);
#6470=ORIENTED_EDGE('',*,*,#5071,.F.);
#6471=ORIENTED_EDGE('',*,*,#5072,.T.);
#6472=ORIENTED_EDGE('',*,*,#5073,.T.);
#6473=ORIENTED_EDGE('',*,*,#5074,.T.);
#6474=ORIENTED_EDGE('',*,*,#5075,.F.);
#6475=ORIENTED_EDGE('',*,*,#5076,.T.);
#6476=ORIENTED_EDGE('',*,*,#5077,.T.);
#6477=ORIENTED_EDGE('',*,*,#5078,.T.);
#6478=ORIENTED_EDGE('',*,*,#5079,.F.);
#6479=ORIENTED_EDGE('',*,*,#5080,.T.);
#6480=ORIENTED_EDGE('',*,*,#5081,.T.);
#6481=ORIENTED_EDGE('',*,*,#5082,.T.);
#6482=ORIENTED_EDGE('',*,*,#5083,.F.);
#6483=ORIENTED_EDGE('',*,*,#5084,.T.);
#6484=ORIENTED_EDGE('',*,*,#5085,.T.);
#6485=ORIENTED_EDGE('',*,*,#5086,.T.);
#6486=ORIENTED_EDGE('',*,*,#5087,.F.);
#6487=ORIENTED_EDGE('',*,*,#5088,.T.);
#6488=ORIENTED_EDGE('',*,*,#5089,.T.);
#6489=ORIENTED_EDGE('',*,*,#5090,.T.);
#6490=ORIENTED_EDGE('',*,*,#5091,.F.);
#6491=ORIENTED_EDGE('',*,*,#5092,.T.);
#6492=ORIENTED_EDGE('',*,*,#5093,.T.);
#6493=ORIENTED_EDGE('',*,*,#5094,.T.);
#6494=ORIENTED_EDGE('',*,*,#5095,.F.);
#6495=ORIENTED_EDGE('',*,*,#5096,.T.);
#6496=ORIENTED_EDGE('',*,*,#5097,.T.);
#6497=ORIENTED_EDGE('',*,*,#5098,.T.);
#6498=ORIENTED_EDGE('',*,*,#5099,.F.);
#6499=ORIENTED_EDGE('',*,*,#5100,.T.);
#6500=ORIENTED_EDGE('',*,*,#5101,.T.);
#6501=ORIENTED_EDGE('',*,*,#5102,.T.);
#6502=ORIENTED_EDGE('',*,*,#5103,.F.);
#6503=ORIENTED_EDGE('',*,*,#5104,.T.);
#6504=ORIENTED_EDGE('',*,*,#5105,.T.);
#6505=ORIENTED_EDGE('',*,*,#5106,.T.);
#6506=ORIENTED_EDGE('',*,*,#5107,.F.);
#6507=ORIENTED_EDGE('',*,*,#5108,.T.);
#6508=ORIENTED_EDGE('',*,*,#5109,.T.);
#6509=ORIENTED_EDGE('',*,*,#5110,.T.);
#6510=ORIENTED_EDGE('',*,*,#5111,.F.);
#6511=ORIENTED_EDGE('',*,*,#5112,.T.);
#6512=ORIENTED_EDGE('',*,*,#5113,.T.);
#6513=ORIENTED_EDGE('',*,*,#5114,.T.);
#6514=ORIENTED_EDGE('',*,*,#5115,.F.);
#6515=ORIENTED_EDGE('',*,*,#5116,.T.);
#6516=ORIENTED_EDGE('',*,*,#5117,.T.);
#6517=ORIENTED_EDGE('',*,*,#5118,.T.);
#6518=ORIENTED_EDGE('',*,*,#5119,.F.);
#6519=ORIENTED_EDGE('',*,*,#5120,.T.);
#6520=ORIENTED_EDGE('',*,*,#5121,.T.);
#6521=ORIENTED_EDGE('',*,*,#5122,.T.);
#6522=ORIENTED_EDGE('',*,*,#5123,.F.);
#6523=ORIENTED_EDGE('',*,*,#5124,.T.);
#6524=ORIENTED_EDGE('',*,*,#5125,.T.);
#6525=ORIENTED_EDGE('',*,*,#5126,.T.);
#6526=ORIENTED_EDGE('',*,*,#5127,.F.);
#6527=ORIENTED_EDGE('',*,*,#5128,.T.);
#6528=ORIENTED_EDGE('',*,*,#5129,.T.);
#6529=ORIENTED_EDGE('',*,*,#5130,.T.);
#6530=ORIENTED_EDGE('',*,*,#5131,.F.);
#6531=ORIENTED_EDGE('',*,*,#5132,.T.);
#6532=ORIENTED_EDGE('',*,*,#5133,.T.);
#6533=ORIENTED_EDGE('',*,*,#5134,.T.);
#6534=ORIENTED_EDGE('',*,*,#5135,.F.);
#6535=ORIENTED_EDGE('',*,*,#5136,.T.);
#6536=ORIENTED_EDGE('',*,*,#5137,.T.);
#6537=ORIENTED_EDGE('',*,*,#5138,.T.);
#6538=ORIENTED_EDGE('',*,*,#5139,.F.);
#6539=ORIENTED_EDGE('',*,*,#5140,.T.);
#6540=ORIENTED_EDGE('',*,*,#5141,.T.);
#6541=ORIENTED_EDGE('',*,*,#5142,.T.);
#6542=ORIENTED_EDGE('',*,*,#5143,.F.);
#6543=ORIENTED_EDGE('',*,*,#5144,.T.);
#6544=ORIENTED_EDGE('',*,*,#5145,.T.);
#6545=ORIENTED_EDGE('',*,*,#5146,.T.);
#6546=ORIENTED_EDGE('',*,*,#5147,.F.);
#6547=ORIENTED_EDGE('',*,*,#5148,.T.);
#6548=ORIENTED_EDGE('',*,*,#5149,.T.);
#6549=ORIENTED_EDGE('',*,*,#5150,.T.);
#6550=ORIENTED_EDGE('',*,*,#5151,.F.);
#6551=ORIENTED_EDGE('',*,*,#5152,.T.);
#6552=ORIENTED_EDGE('',*,*,#5153,.T.);
#6553=ORIENTED_EDGE('',*,*,#5154,.T.);
#6554=ORIENTED_EDGE('',*,*,#5155,.F.);
#6555=ORIENTED_EDGE('',*,*,#5156,.T.);
#6556=ORIENTED_EDGE('',*,*,#5157,.T.);
#6557=ORIENTED_EDGE('',*,*,#5158,.T.);
#6558=ORIENTED_EDGE('',*,*,#5159,.F.);
#6559=ORIENTED_EDGE('',*,*,#5160,.T.);
#6560=ORIENTED_EDGE('',*,*,#5161,.T.);
#6561=ORIENTED_EDGE('',*,*,#5162,.T.);
#6562=ORIENTED_EDGE('',*,*,#5163,.F.);
#6563=ORIENTED_EDGE('',*,*,#5164,.T.);
#6564=ORIENTED_EDGE('',*,*,#5165,.T.);
#6565=ORIENTED_EDGE('',*,*,#5166,.T.);
#6566=ORIENTED_EDGE('',*,*,#5167,.F.);
#6567=ORIENTED_EDGE('',*,*,#5168,.T.);
#6568=ORIENTED_EDGE('',*,*,#5169,.T.);
#6569=ORIENTED_EDGE('',*,*,#5170,.T.);
#6570=ORIENTED_EDGE('',*,*,#5171,.F.);
#6571=ORIENTED_EDGE('',*,*,#5172,.T.);
#6572=ORIENTED_EDGE('',*,*,#5173,.T.);
#6573=ORIENTED_EDGE('',*,*,#5174,.T.);
#6574=ORIENTED_EDGE('',*,*,#5175,.F.);
#6575=ORIENTED_EDGE('',*,*,#5176,.T.);
#6576=ORIENTED_EDGE('',*,*,#5177,.T.);
#6577=ORIENTED_EDGE('',*,*,#5178,.T.);
#6578=ORIENTED_EDGE('',*,*,#5179,.F.);
#6579=ORIENTED_EDGE('',*,*,#5180,.T.);
#6580=ORIENTED_EDGE('',*,*,#5181,.T.);
#6581=ORIENTED_EDGE('',*,*,#5182,.T.);
#6582=ORIENTED_EDGE('',*,*,#5183,.F.);
#6583=ORIENTED_EDGE('',*,*,#5184,.T.);
#6584=ORIENTED_EDGE('',*,*,#5185,.F.);
#6585=ORIENTED_EDGE('',*,*,#5186,.F.);
#6586=ORIENTED_EDGE('',*,*,#5187,.T.);
#6587=ORIENTED_EDGE('',*,*,#5179,.T.);
#6588=ORIENTED_EDGE('',*,*,#5188,.F.);
#6589=ORIENTED_EDGE('',*,*,#5181,.F.);
#6590=ORIENTED_EDGE('',*,*,#5189,.T.);
#6591=ORIENTED_EDGE('',*,*,#5186,.T.);
#6592=ORIENTED_EDGE('',*,*,#5190,.F.);
#6593=ORIENTED_EDGE('',*,*,#5191,.F.);
#6594=ORIENTED_EDGE('',*,*,#5192,.T.);
#6595=ORIENTED_EDGE('',*,*,#5175,.T.);
#6596=ORIENTED_EDGE('',*,*,#5193,.F.);
#6597=ORIENTED_EDGE('',*,*,#5177,.F.);
#6598=ORIENTED_EDGE('',*,*,#5194,.T.);
#6599=ORIENTED_EDGE('',*,*,#5191,.T.);
#6600=ORIENTED_EDGE('',*,*,#5195,.F.);
#6601=ORIENTED_EDGE('',*,*,#5196,.F.);
#6602=ORIENTED_EDGE('',*,*,#5197,.T.);
#6603=ORIENTED_EDGE('',*,*,#5171,.T.);
#6604=ORIENTED_EDGE('',*,*,#5198,.F.);
#6605=ORIENTED_EDGE('',*,*,#5173,.F.);
#6606=ORIENTED_EDGE('',*,*,#5199,.T.);
#6607=ORIENTED_EDGE('',*,*,#5196,.T.);
#6608=ORIENTED_EDGE('',*,*,#5200,.F.);
#6609=ORIENTED_EDGE('',*,*,#5201,.F.);
#6610=ORIENTED_EDGE('',*,*,#5202,.T.);
#6611=ORIENTED_EDGE('',*,*,#5167,.T.);
#6612=ORIENTED_EDGE('',*,*,#5203,.F.);
#6613=ORIENTED_EDGE('',*,*,#5169,.F.);
#6614=ORIENTED_EDGE('',*,*,#5204,.T.);
#6615=ORIENTED_EDGE('',*,*,#5201,.T.);
#6616=ORIENTED_EDGE('',*,*,#5205,.F.);
#6617=ORIENTED_EDGE('',*,*,#5206,.F.);
#6618=ORIENTED_EDGE('',*,*,#5207,.T.);
#6619=ORIENTED_EDGE('',*,*,#5163,.T.);
#6620=ORIENTED_EDGE('',*,*,#5208,.F.);
#6621=ORIENTED_EDGE('',*,*,#5165,.F.);
#6622=ORIENTED_EDGE('',*,*,#5209,.T.);
#6623=ORIENTED_EDGE('',*,*,#5206,.T.);
#6624=ORIENTED_EDGE('',*,*,#5210,.F.);
#6625=ORIENTED_EDGE('',*,*,#5211,.F.);
#6626=ORIENTED_EDGE('',*,*,#5212,.T.);
#6627=ORIENTED_EDGE('',*,*,#5159,.T.);
#6628=ORIENTED_EDGE('',*,*,#5213,.F.);
#6629=ORIENTED_EDGE('',*,*,#5161,.F.);
#6630=ORIENTED_EDGE('',*,*,#5214,.T.);
#6631=ORIENTED_EDGE('',*,*,#5211,.T.);
#6632=ORIENTED_EDGE('',*,*,#5215,.F.);
#6633=ORIENTED_EDGE('',*,*,#5216,.F.);
#6634=ORIENTED_EDGE('',*,*,#5217,.T.);
#6635=ORIENTED_EDGE('',*,*,#5155,.T.);
#6636=ORIENTED_EDGE('',*,*,#5218,.F.);
#6637=ORIENTED_EDGE('',*,*,#5157,.F.);
#6638=ORIENTED_EDGE('',*,*,#5219,.T.);
#6639=ORIENTED_EDGE('',*,*,#5216,.T.);
#6640=ORIENTED_EDGE('',*,*,#5220,.F.);
#6641=ORIENTED_EDGE('',*,*,#5221,.F.);
#6642=ORIENTED_EDGE('',*,*,#5222,.T.);
#6643=ORIENTED_EDGE('',*,*,#5151,.T.);
#6644=ORIENTED_EDGE('',*,*,#5223,.F.);
#6645=ORIENTED_EDGE('',*,*,#5153,.F.);
#6646=ORIENTED_EDGE('',*,*,#5224,.T.);
#6647=ORIENTED_EDGE('',*,*,#5221,.T.);
#6648=ORIENTED_EDGE('',*,*,#5225,.F.);
#6649=ORIENTED_EDGE('',*,*,#5226,.F.);
#6650=ORIENTED_EDGE('',*,*,#5227,.T.);
#6651=ORIENTED_EDGE('',*,*,#5147,.T.);
#6652=ORIENTED_EDGE('',*,*,#5228,.F.);
#6653=ORIENTED_EDGE('',*,*,#5149,.F.);
#6654=ORIENTED_EDGE('',*,*,#5229,.T.);
#6655=ORIENTED_EDGE('',*,*,#5226,.T.);
#6656=ORIENTED_EDGE('',*,*,#5230,.F.);
#6657=ORIENTED_EDGE('',*,*,#5231,.F.);
#6658=ORIENTED_EDGE('',*,*,#5232,.T.);
#6659=ORIENTED_EDGE('',*,*,#5143,.T.);
#6660=ORIENTED_EDGE('',*,*,#5233,.F.);
#6661=ORIENTED_EDGE('',*,*,#5145,.F.);
#6662=ORIENTED_EDGE('',*,*,#5234,.T.);
#6663=ORIENTED_EDGE('',*,*,#5231,.T.);
#6664=ORIENTED_EDGE('',*,*,#5235,.F.);
#6665=ORIENTED_EDGE('',*,*,#5236,.F.);
#6666=ORIENTED_EDGE('',*,*,#5237,.T.);
#6667=ORIENTED_EDGE('',*,*,#5139,.T.);
#6668=ORIENTED_EDGE('',*,*,#5238,.F.);
#6669=ORIENTED_EDGE('',*,*,#5141,.F.);
#6670=ORIENTED_EDGE('',*,*,#5239,.T.);
#6671=ORIENTED_EDGE('',*,*,#5236,.T.);
#6672=ORIENTED_EDGE('',*,*,#5240,.F.);
#6673=ORIENTED_EDGE('',*,*,#5241,.F.);
#6674=ORIENTED_EDGE('',*,*,#5242,.T.);
#6675=ORIENTED_EDGE('',*,*,#5135,.T.);
#6676=ORIENTED_EDGE('',*,*,#5243,.F.);
#6677=ORIENTED_EDGE('',*,*,#5137,.F.);
#6678=ORIENTED_EDGE('',*,*,#5244,.T.);
#6679=ORIENTED_EDGE('',*,*,#5241,.T.);
#6680=ORIENTED_EDGE('',*,*,#5245,.F.);
#6681=ORIENTED_EDGE('',*,*,#5246,.F.);
#6682=ORIENTED_EDGE('',*,*,#5247,.T.);
#6683=ORIENTED_EDGE('',*,*,#5131,.T.);
#6684=ORIENTED_EDGE('',*,*,#5248,.F.);
#6685=ORIENTED_EDGE('',*,*,#5133,.F.);
#6686=ORIENTED_EDGE('',*,*,#5249,.T.);
#6687=ORIENTED_EDGE('',*,*,#5246,.T.);
#6688=ORIENTED_EDGE('',*,*,#5250,.F.);
#6689=ORIENTED_EDGE('',*,*,#5251,.F.);
#6690=ORIENTED_EDGE('',*,*,#5252,.T.);
#6691=ORIENTED_EDGE('',*,*,#5127,.T.);
#6692=ORIENTED_EDGE('',*,*,#5253,.F.);
#6693=ORIENTED_EDGE('',*,*,#5129,.F.);
#6694=ORIENTED_EDGE('',*,*,#5254,.T.);
#6695=ORIENTED_EDGE('',*,*,#5251,.T.);
#6696=ORIENTED_EDGE('',*,*,#5255,.F.);
#6697=ORIENTED_EDGE('',*,*,#5256,.F.);
#6698=ORIENTED_EDGE('',*,*,#5257,.T.);
#6699=ORIENTED_EDGE('',*,*,#5123,.T.);
#6700=ORIENTED_EDGE('',*,*,#5258,.F.);
#6701=ORIENTED_EDGE('',*,*,#5125,.F.);
#6702=ORIENTED_EDGE('',*,*,#5259,.T.);
#6703=ORIENTED_EDGE('',*,*,#5256,.T.);
#6704=ORIENTED_EDGE('',*,*,#5260,.F.);
#6705=ORIENTED_EDGE('',*,*,#5261,.F.);
#6706=ORIENTED_EDGE('',*,*,#5262,.T.);
#6707=ORIENTED_EDGE('',*,*,#5119,.T.);
#6708=ORIENTED_EDGE('',*,*,#5263,.F.);
#6709=ORIENTED_EDGE('',*,*,#5121,.F.);
#6710=ORIENTED_EDGE('',*,*,#5264,.T.);
#6711=ORIENTED_EDGE('',*,*,#5261,.T.);
#6712=ORIENTED_EDGE('',*,*,#5265,.F.);
#6713=ORIENTED_EDGE('',*,*,#5266,.F.);
#6714=ORIENTED_EDGE('',*,*,#5267,.T.);
#6715=ORIENTED_EDGE('',*,*,#5115,.T.);
#6716=ORIENTED_EDGE('',*,*,#5268,.F.);
#6717=ORIENTED_EDGE('',*,*,#5117,.F.);
#6718=ORIENTED_EDGE('',*,*,#5269,.T.);
#6719=ORIENTED_EDGE('',*,*,#5266,.T.);
#6720=ORIENTED_EDGE('',*,*,#5270,.F.);
#6721=ORIENTED_EDGE('',*,*,#5271,.F.);
#6722=ORIENTED_EDGE('',*,*,#5272,.T.);
#6723=ORIENTED_EDGE('',*,*,#5111,.T.);
#6724=ORIENTED_EDGE('',*,*,#5273,.F.);
#6725=ORIENTED_EDGE('',*,*,#5113,.F.);
#6726=ORIENTED_EDGE('',*,*,#5274,.T.);
#6727=ORIENTED_EDGE('',*,*,#5271,.T.);
#6728=ORIENTED_EDGE('',*,*,#5275,.F.);
#6729=ORIENTED_EDGE('',*,*,#5276,.F.);
#6730=ORIENTED_EDGE('',*,*,#5277,.T.);
#6731=ORIENTED_EDGE('',*,*,#5107,.T.);
#6732=ORIENTED_EDGE('',*,*,#5278,.F.);
#6733=ORIENTED_EDGE('',*,*,#5109,.F.);
#6734=ORIENTED_EDGE('',*,*,#5279,.T.);
#6735=ORIENTED_EDGE('',*,*,#5276,.T.);
#6736=ORIENTED_EDGE('',*,*,#5280,.F.);
#6737=ORIENTED_EDGE('',*,*,#5281,.F.);
#6738=ORIENTED_EDGE('',*,*,#5282,.T.);
#6739=ORIENTED_EDGE('',*,*,#5103,.T.);
#6740=ORIENTED_EDGE('',*,*,#5283,.F.);
#6741=ORIENTED_EDGE('',*,*,#5105,.F.);
#6742=ORIENTED_EDGE('',*,*,#5284,.T.);
#6743=ORIENTED_EDGE('',*,*,#5281,.T.);
#6744=ORIENTED_EDGE('',*,*,#5285,.F.);
#6745=ORIENTED_EDGE('',*,*,#5286,.F.);
#6746=ORIENTED_EDGE('',*,*,#5287,.T.);
#6747=ORIENTED_EDGE('',*,*,#5099,.T.);
#6748=ORIENTED_EDGE('',*,*,#5288,.F.);
#6749=ORIENTED_EDGE('',*,*,#5101,.F.);
#6750=ORIENTED_EDGE('',*,*,#5289,.T.);
#6751=ORIENTED_EDGE('',*,*,#5286,.T.);
#6752=ORIENTED_EDGE('',*,*,#5290,.F.);
#6753=ORIENTED_EDGE('',*,*,#5291,.F.);
#6754=ORIENTED_EDGE('',*,*,#5292,.T.);
#6755=ORIENTED_EDGE('',*,*,#5095,.T.);
#6756=ORIENTED_EDGE('',*,*,#5293,.F.);
#6757=ORIENTED_EDGE('',*,*,#5097,.F.);
#6758=ORIENTED_EDGE('',*,*,#5294,.T.);
#6759=ORIENTED_EDGE('',*,*,#5291,.T.);
#6760=ORIENTED_EDGE('',*,*,#5295,.F.);
#6761=ORIENTED_EDGE('',*,*,#5296,.F.);
#6762=ORIENTED_EDGE('',*,*,#5297,.T.);
#6763=ORIENTED_EDGE('',*,*,#5091,.T.);
#6764=ORIENTED_EDGE('',*,*,#5298,.F.);
#6765=ORIENTED_EDGE('',*,*,#5093,.F.);
#6766=ORIENTED_EDGE('',*,*,#5299,.T.);
#6767=ORIENTED_EDGE('',*,*,#5296,.T.);
#6768=ORIENTED_EDGE('',*,*,#5300,.F.);
#6769=ORIENTED_EDGE('',*,*,#5301,.F.);
#6770=ORIENTED_EDGE('',*,*,#5302,.T.);
#6771=ORIENTED_EDGE('',*,*,#5087,.T.);
#6772=ORIENTED_EDGE('',*,*,#5303,.F.);
#6773=ORIENTED_EDGE('',*,*,#5089,.F.);
#6774=ORIENTED_EDGE('',*,*,#5304,.T.);
#6775=ORIENTED_EDGE('',*,*,#5301,.T.);
#6776=ORIENTED_EDGE('',*,*,#5305,.F.);
#6777=ORIENTED_EDGE('',*,*,#5306,.F.);
#6778=ORIENTED_EDGE('',*,*,#5307,.T.);
#6779=ORIENTED_EDGE('',*,*,#5083,.T.);
#6780=ORIENTED_EDGE('',*,*,#5308,.F.);
#6781=ORIENTED_EDGE('',*,*,#5085,.F.);
#6782=ORIENTED_EDGE('',*,*,#5309,.T.);
#6783=ORIENTED_EDGE('',*,*,#5306,.T.);
#6784=ORIENTED_EDGE('',*,*,#5310,.F.);
#6785=ORIENTED_EDGE('',*,*,#5311,.F.);
#6786=ORIENTED_EDGE('',*,*,#5312,.T.);
#6787=ORIENTED_EDGE('',*,*,#5079,.T.);
#6788=ORIENTED_EDGE('',*,*,#5313,.F.);
#6789=ORIENTED_EDGE('',*,*,#5081,.F.);
#6790=ORIENTED_EDGE('',*,*,#5314,.T.);
#6791=ORIENTED_EDGE('',*,*,#5311,.T.);
#6792=ORIENTED_EDGE('',*,*,#5315,.F.);
#6793=ORIENTED_EDGE('',*,*,#5316,.F.);
#6794=ORIENTED_EDGE('',*,*,#5317,.T.);
#6795=ORIENTED_EDGE('',*,*,#5075,.T.);
#6796=ORIENTED_EDGE('',*,*,#5318,.F.);
#6797=ORIENTED_EDGE('',*,*,#5077,.F.);
#6798=ORIENTED_EDGE('',*,*,#5319,.T.);
#6799=ORIENTED_EDGE('',*,*,#5316,.T.);
#6800=ORIENTED_EDGE('',*,*,#5320,.F.);
#6801=ORIENTED_EDGE('',*,*,#5321,.F.);
#6802=ORIENTED_EDGE('',*,*,#5322,.T.);
#6803=ORIENTED_EDGE('',*,*,#5071,.T.);
#6804=ORIENTED_EDGE('',*,*,#5323,.F.);
#6805=ORIENTED_EDGE('',*,*,#5073,.F.);
#6806=ORIENTED_EDGE('',*,*,#5324,.T.);
#6807=ORIENTED_EDGE('',*,*,#5321,.T.);
#6808=ORIENTED_EDGE('',*,*,#5325,.F.);
#6809=ORIENTED_EDGE('',*,*,#5326,.F.);
#6810=ORIENTED_EDGE('',*,*,#5327,.T.);
#6811=ORIENTED_EDGE('',*,*,#5067,.T.);
#6812=ORIENTED_EDGE('',*,*,#5328,.F.);
#6813=ORIENTED_EDGE('',*,*,#5069,.F.);
#6814=ORIENTED_EDGE('',*,*,#5329,.T.);
#6815=ORIENTED_EDGE('',*,*,#5326,.T.);
#6816=ORIENTED_EDGE('',*,*,#5330,.F.);
#6817=ORIENTED_EDGE('',*,*,#5331,.F.);
#6818=ORIENTED_EDGE('',*,*,#5332,.T.);
#6819=ORIENTED_EDGE('',*,*,#5063,.T.);
#6820=ORIENTED_EDGE('',*,*,#5333,.F.);
#6821=ORIENTED_EDGE('',*,*,#5065,.F.);
#6822=ORIENTED_EDGE('',*,*,#5334,.T.);
#6823=ORIENTED_EDGE('',*,*,#5331,.T.);
#6824=ORIENTED_EDGE('',*,*,#5335,.F.);
#6825=ORIENTED_EDGE('',*,*,#5336,.F.);
#6826=ORIENTED_EDGE('',*,*,#5337,.T.);
#6827=ORIENTED_EDGE('',*,*,#5059,.T.);
#6828=ORIENTED_EDGE('',*,*,#5338,.F.);
#6829=ORIENTED_EDGE('',*,*,#5061,.F.);
#6830=ORIENTED_EDGE('',*,*,#5339,.T.);
#6831=ORIENTED_EDGE('',*,*,#5336,.T.);
#6832=ORIENTED_EDGE('',*,*,#5340,.F.);
#6833=ORIENTED_EDGE('',*,*,#5341,.F.);
#6834=ORIENTED_EDGE('',*,*,#5342,.T.);
#6835=ORIENTED_EDGE('',*,*,#5055,.T.);
#6836=ORIENTED_EDGE('',*,*,#5343,.F.);
#6837=ORIENTED_EDGE('',*,*,#5057,.F.);
#6838=ORIENTED_EDGE('',*,*,#5344,.T.);
#6839=ORIENTED_EDGE('',*,*,#5341,.T.);
#6840=ORIENTED_EDGE('',*,*,#5345,.F.);
#6841=ORIENTED_EDGE('',*,*,#5346,.F.);
#6842=ORIENTED_EDGE('',*,*,#5347,.T.);
#6843=ORIENTED_EDGE('',*,*,#5051,.T.);
#6844=ORIENTED_EDGE('',*,*,#5348,.F.);
#6845=ORIENTED_EDGE('',*,*,#5053,.F.);
#6846=ORIENTED_EDGE('',*,*,#5349,.T.);
#6847=ORIENTED_EDGE('',*,*,#5346,.T.);
#6848=ORIENTED_EDGE('',*,*,#5350,.F.);
#6849=ORIENTED_EDGE('',*,*,#5351,.F.);
#6850=ORIENTED_EDGE('',*,*,#5352,.T.);
#6851=ORIENTED_EDGE('',*,*,#5047,.T.);
#6852=ORIENTED_EDGE('',*,*,#5353,.F.);
#6853=ORIENTED_EDGE('',*,*,#5049,.F.);
#6854=ORIENTED_EDGE('',*,*,#5354,.T.);
#6855=ORIENTED_EDGE('',*,*,#5351,.T.);
#6856=ORIENTED_EDGE('',*,*,#5355,.F.);
#6857=ORIENTED_EDGE('',*,*,#5356,.F.);
#6858=ORIENTED_EDGE('',*,*,#5357,.T.);
#6859=ORIENTED_EDGE('',*,*,#5043,.T.);
#6860=ORIENTED_EDGE('',*,*,#5358,.F.);
#6861=ORIENTED_EDGE('',*,*,#5045,.F.);
#6862=ORIENTED_EDGE('',*,*,#5359,.T.);
#6863=ORIENTED_EDGE('',*,*,#5356,.T.);
#6864=ORIENTED_EDGE('',*,*,#5360,.F.);
#6865=ORIENTED_EDGE('',*,*,#5361,.F.);
#6866=ORIENTED_EDGE('',*,*,#5362,.T.);
#6867=ORIENTED_EDGE('',*,*,#5039,.T.);
#6868=ORIENTED_EDGE('',*,*,#5363,.F.);
#6869=ORIENTED_EDGE('',*,*,#5041,.F.);
#6870=ORIENTED_EDGE('',*,*,#5364,.T.);
#6871=ORIENTED_EDGE('',*,*,#5361,.T.);
#6872=ORIENTED_EDGE('',*,*,#5365,.F.);
#6873=ORIENTED_EDGE('',*,*,#5366,.F.);
#6874=ORIENTED_EDGE('',*,*,#5367,.T.);
#6875=ORIENTED_EDGE('',*,*,#5035,.T.);
#6876=ORIENTED_EDGE('',*,*,#5368,.F.);
#6877=ORIENTED_EDGE('',*,*,#5037,.F.);
#6878=ORIENTED_EDGE('',*,*,#5369,.T.);
#6879=ORIENTED_EDGE('',*,*,#5366,.T.);
#6880=ORIENTED_EDGE('',*,*,#5370,.F.);
#6881=ORIENTED_EDGE('',*,*,#5371,.F.);
#6882=ORIENTED_EDGE('',*,*,#5372,.T.);
#6883=ORIENTED_EDGE('',*,*,#5031,.T.);
#6884=ORIENTED_EDGE('',*,*,#5373,.F.);
#6885=ORIENTED_EDGE('',*,*,#5033,.F.);
#6886=ORIENTED_EDGE('',*,*,#5374,.T.);
#6887=ORIENTED_EDGE('',*,*,#5371,.T.);
#6888=ORIENTED_EDGE('',*,*,#5375,.F.);
#6889=ORIENTED_EDGE('',*,*,#5376,.F.);
#6890=ORIENTED_EDGE('',*,*,#5377,.T.);
#6891=ORIENTED_EDGE('',*,*,#5027,.T.);
#6892=ORIENTED_EDGE('',*,*,#5378,.F.);
#6893=ORIENTED_EDGE('',*,*,#5029,.F.);
#6894=ORIENTED_EDGE('',*,*,#5379,.T.);
#6895=ORIENTED_EDGE('',*,*,#5376,.T.);
#6896=ORIENTED_EDGE('',*,*,#5380,.F.);
#6897=ORIENTED_EDGE('',*,*,#5381,.F.);
#6898=ORIENTED_EDGE('',*,*,#5382,.T.);
#6899=ORIENTED_EDGE('',*,*,#5183,.T.);
#6900=ORIENTED_EDGE('',*,*,#5383,.F.);
#6901=ORIENTED_EDGE('',*,*,#5025,.F.);
#6902=ORIENTED_EDGE('',*,*,#5384,.T.);
#6903=ORIENTED_EDGE('',*,*,#5381,.T.);
#6904=ORIENTED_EDGE('',*,*,#5385,.T.);
#6905=ORIENTED_EDGE('',*,*,#5386,.T.);
#6906=ORIENTED_EDGE('',*,*,#5387,.T.);
#6907=ORIENTED_EDGE('',*,*,#5388,.T.);
#6908=ORIENTED_EDGE('',*,*,#5389,.T.);
#6909=ORIENTED_EDGE('',*,*,#5390,.T.);
#6910=ORIENTED_EDGE('',*,*,#5391,.T.);
#6911=ORIENTED_EDGE('',*,*,#5392,.T.);
#6912=ORIENTED_EDGE('',*,*,#5393,.T.);
#6913=ORIENTED_EDGE('',*,*,#5382,.F.);
#6914=ORIENTED_EDGE('',*,*,#5384,.F.);
#6915=ORIENTED_EDGE('',*,*,#5028,.F.);
#6916=ORIENTED_EDGE('',*,*,#5377,.F.);
#6917=ORIENTED_EDGE('',*,*,#5379,.F.);
#6918=ORIENTED_EDGE('',*,*,#5032,.F.);
#6919=ORIENTED_EDGE('',*,*,#5372,.F.);
#6920=ORIENTED_EDGE('',*,*,#5374,.F.);
#6921=ORIENTED_EDGE('',*,*,#5036,.F.);
#6922=ORIENTED_EDGE('',*,*,#5367,.F.);
#6923=ORIENTED_EDGE('',*,*,#5369,.F.);
#6924=ORIENTED_EDGE('',*,*,#5040,.F.);
#6925=ORIENTED_EDGE('',*,*,#5362,.F.);
#6926=ORIENTED_EDGE('',*,*,#5364,.F.);
#6927=ORIENTED_EDGE('',*,*,#5044,.F.);
#6928=ORIENTED_EDGE('',*,*,#5357,.F.);
#6929=ORIENTED_EDGE('',*,*,#5359,.F.);
#6930=ORIENTED_EDGE('',*,*,#5048,.F.);
#6931=ORIENTED_EDGE('',*,*,#5352,.F.);
#6932=ORIENTED_EDGE('',*,*,#5354,.F.);
#6933=ORIENTED_EDGE('',*,*,#5052,.F.);
#6934=ORIENTED_EDGE('',*,*,#5347,.F.);
#6935=ORIENTED_EDGE('',*,*,#5349,.F.);
#6936=ORIENTED_EDGE('',*,*,#5056,.F.);
#6937=ORIENTED_EDGE('',*,*,#5342,.F.);
#6938=ORIENTED_EDGE('',*,*,#5344,.F.);
#6939=ORIENTED_EDGE('',*,*,#5060,.F.);
#6940=ORIENTED_EDGE('',*,*,#5337,.F.);
#6941=ORIENTED_EDGE('',*,*,#5339,.F.);
#6942=ORIENTED_EDGE('',*,*,#5064,.F.);
#6943=ORIENTED_EDGE('',*,*,#5332,.F.);
#6944=ORIENTED_EDGE('',*,*,#5334,.F.);
#6945=ORIENTED_EDGE('',*,*,#5068,.F.);
#6946=ORIENTED_EDGE('',*,*,#5327,.F.);
#6947=ORIENTED_EDGE('',*,*,#5329,.F.);
#6948=ORIENTED_EDGE('',*,*,#5072,.F.);
#6949=ORIENTED_EDGE('',*,*,#5322,.F.);
#6950=ORIENTED_EDGE('',*,*,#5324,.F.);
#6951=ORIENTED_EDGE('',*,*,#5076,.F.);
#6952=ORIENTED_EDGE('',*,*,#5317,.F.);
#6953=ORIENTED_EDGE('',*,*,#5319,.F.);
#6954=ORIENTED_EDGE('',*,*,#5080,.F.);
#6955=ORIENTED_EDGE('',*,*,#5312,.F.);
#6956=ORIENTED_EDGE('',*,*,#5314,.F.);
#6957=ORIENTED_EDGE('',*,*,#5084,.F.);
#6958=ORIENTED_EDGE('',*,*,#5307,.F.);
#6959=ORIENTED_EDGE('',*,*,#5309,.F.);
#6960=ORIENTED_EDGE('',*,*,#5088,.F.);
#6961=ORIENTED_EDGE('',*,*,#5302,.F.);
#6962=ORIENTED_EDGE('',*,*,#5304,.F.);
#6963=ORIENTED_EDGE('',*,*,#5092,.F.);
#6964=ORIENTED_EDGE('',*,*,#5297,.F.);
#6965=ORIENTED_EDGE('',*,*,#5299,.F.);
#6966=ORIENTED_EDGE('',*,*,#5096,.F.);
#6967=ORIENTED_EDGE('',*,*,#5292,.F.);
#6968=ORIENTED_EDGE('',*,*,#5294,.F.);
#6969=ORIENTED_EDGE('',*,*,#5100,.F.);
#6970=ORIENTED_EDGE('',*,*,#5287,.F.);
#6971=ORIENTED_EDGE('',*,*,#5289,.F.);
#6972=ORIENTED_EDGE('',*,*,#5104,.F.);
#6973=ORIENTED_EDGE('',*,*,#5282,.F.);
#6974=ORIENTED_EDGE('',*,*,#5284,.F.);
#6975=ORIENTED_EDGE('',*,*,#5108,.F.);
#6976=ORIENTED_EDGE('',*,*,#5277,.F.);
#6977=ORIENTED_EDGE('',*,*,#5279,.F.);
#6978=ORIENTED_EDGE('',*,*,#5112,.F.);
#6979=ORIENTED_EDGE('',*,*,#5272,.F.);
#6980=ORIENTED_EDGE('',*,*,#5274,.F.);
#6981=ORIENTED_EDGE('',*,*,#5116,.F.);
#6982=ORIENTED_EDGE('',*,*,#5267,.F.);
#6983=ORIENTED_EDGE('',*,*,#5269,.F.);
#6984=ORIENTED_EDGE('',*,*,#5120,.F.);
#6985=ORIENTED_EDGE('',*,*,#5262,.F.);
#6986=ORIENTED_EDGE('',*,*,#5264,.F.);
#6987=ORIENTED_EDGE('',*,*,#5124,.F.);
#6988=ORIENTED_EDGE('',*,*,#5257,.F.);
#6989=ORIENTED_EDGE('',*,*,#5259,.F.);
#6990=ORIENTED_EDGE('',*,*,#5128,.F.);
#6991=ORIENTED_EDGE('',*,*,#5252,.F.);
#6992=ORIENTED_EDGE('',*,*,#5254,.F.);
#6993=ORIENTED_EDGE('',*,*,#5132,.F.);
#6994=ORIENTED_EDGE('',*,*,#5247,.F.);
#6995=ORIENTED_EDGE('',*,*,#5249,.F.);
#6996=ORIENTED_EDGE('',*,*,#5136,.F.);
#6997=ORIENTED_EDGE('',*,*,#5242,.F.);
#6998=ORIENTED_EDGE('',*,*,#5244,.F.);
#6999=ORIENTED_EDGE('',*,*,#5140,.F.);
#7000=ORIENTED_EDGE('',*,*,#5237,.F.);
#7001=ORIENTED_EDGE('',*,*,#5239,.F.);
#7002=ORIENTED_EDGE('',*,*,#5144,.F.);
#7003=ORIENTED_EDGE('',*,*,#5232,.F.);
#7004=ORIENTED_EDGE('',*,*,#5234,.F.);
#7005=ORIENTED_EDGE('',*,*,#5148,.F.);
#7006=ORIENTED_EDGE('',*,*,#5227,.F.);
#7007=ORIENTED_EDGE('',*,*,#5229,.F.);
#7008=ORIENTED_EDGE('',*,*,#5152,.F.);
#7009=ORIENTED_EDGE('',*,*,#5222,.F.);
#7010=ORIENTED_EDGE('',*,*,#5224,.F.);
#7011=ORIENTED_EDGE('',*,*,#5156,.F.);
#7012=ORIENTED_EDGE('',*,*,#5217,.F.);
#7013=ORIENTED_EDGE('',*,*,#5219,.F.);
#7014=ORIENTED_EDGE('',*,*,#5160,.F.);
#7015=ORIENTED_EDGE('',*,*,#5212,.F.);
#7016=ORIENTED_EDGE('',*,*,#5214,.F.);
#7017=ORIENTED_EDGE('',*,*,#5164,.F.);
#7018=ORIENTED_EDGE('',*,*,#5207,.F.);
#7019=ORIENTED_EDGE('',*,*,#5209,.F.);
#7020=ORIENTED_EDGE('',*,*,#5168,.F.);
#7021=ORIENTED_EDGE('',*,*,#5202,.F.);
#7022=ORIENTED_EDGE('',*,*,#5204,.F.);
#7023=ORIENTED_EDGE('',*,*,#5172,.F.);
#7024=ORIENTED_EDGE('',*,*,#5197,.F.);
#7025=ORIENTED_EDGE('',*,*,#5199,.F.);
#7026=ORIENTED_EDGE('',*,*,#5176,.F.);
#7027=ORIENTED_EDGE('',*,*,#5192,.F.);
#7028=ORIENTED_EDGE('',*,*,#5194,.F.);
#7029=ORIENTED_EDGE('',*,*,#5180,.F.);
#7030=ORIENTED_EDGE('',*,*,#5187,.F.);
#7031=ORIENTED_EDGE('',*,*,#5189,.F.);
#7032=ORIENTED_EDGE('',*,*,#5184,.F.);
#7033=ORIENTED_EDGE('',*,*,#5394,.T.);
#7034=ORIENTED_EDGE('',*,*,#5395,.T.);
#7035=ORIENTED_EDGE('',*,*,#5396,.T.);
#7036=ORIENTED_EDGE('',*,*,#5397,.T.);
#7037=ORIENTED_EDGE('',*,*,#5398,.T.);
#7038=ORIENTED_EDGE('',*,*,#5399,.F.);
#7039=ORIENTED_EDGE('',*,*,#5400,.T.);
#7040=ORIENTED_EDGE('',*,*,#5401,.T.);
#7041=ORIENTED_EDGE('',*,*,#5402,.T.);
#7042=ORIENTED_EDGE('',*,*,#5403,.T.);
#7043=ORIENTED_EDGE('',*,*,#5404,.T.);
#7044=ORIENTED_EDGE('',*,*,#5405,.T.);
#7045=ORIENTED_EDGE('',*,*,#5406,.T.);
#7046=ORIENTED_EDGE('',*,*,#5407,.T.);
#7047=ORIENTED_EDGE('',*,*,#5408,.T.);
#7048=ORIENTED_EDGE('',*,*,#5401,.F.);
#7049=ORIENTED_EDGE('',*,*,#5409,.F.);
#7050=ORIENTED_EDGE('',*,*,#5410,.T.);
#7051=ORIENTED_EDGE('',*,*,#5406,.F.);
#7052=ORIENTED_EDGE('',*,*,#5411,.F.);
#7053=ORIENTED_EDGE('',*,*,#5412,.T.);
#7054=ORIENTED_EDGE('',*,*,#5385,.F.);
#7055=ORIENTED_EDGE('',*,*,#5413,.T.);
#7056=ORIENTED_EDGE('',*,*,#5409,.T.);
#7057=ORIENTED_EDGE('',*,*,#5405,.F.);
#7058=ORIENTED_EDGE('',*,*,#5404,.F.);
#7059=ORIENTED_EDGE('',*,*,#5414,.T.);
#7060=ORIENTED_EDGE('',*,*,#5411,.T.);
#7061=ORIENTED_EDGE('',*,*,#5407,.F.);
#7062=ORIENTED_EDGE('',*,*,#5415,.T.);
#7063=ORIENTED_EDGE('',*,*,#5416,.F.);
#7064=ORIENTED_EDGE('',*,*,#5416,.T.);
#7065=ORIENTED_EDGE('',*,*,#5417,.T.);
#7066=ORIENTED_EDGE('',*,*,#5387,.F.);
#7067=ORIENTED_EDGE('',*,*,#5418,.T.);
#7068=ORIENTED_EDGE('',*,*,#5419,.F.);
#7069=ORIENTED_EDGE('',*,*,#5402,.F.);
#7070=ORIENTED_EDGE('',*,*,#5408,.F.);
#7071=ORIENTED_EDGE('',*,*,#5419,.T.);
#7072=ORIENTED_EDGE('',*,*,#5420,.T.);
#7073=ORIENTED_EDGE('',*,*,#5403,.F.);
#7074=ORIENTED_EDGE('',*,*,#5421,.F.);
#7075=ORIENTED_EDGE('',*,*,#5422,.T.);
#7076=ORIENTED_EDGE('',*,*,#5399,.T.);
#7077=ORIENTED_EDGE('',*,*,#5422,.F.);
#7078=ORIENTED_EDGE('',*,*,#5421,.T.);
#7079=ORIENTED_EDGE('',*,*,#5318,.T.);
#7080=ORIENTED_EDGE('',*,*,#5315,.T.);
#7081=ORIENTED_EDGE('',*,*,#5074,.F.);
#7082=ORIENTED_EDGE('',*,*,#5323,.T.);
#7083=ORIENTED_EDGE('',*,*,#5320,.T.);
#7084=ORIENTED_EDGE('',*,*,#5070,.F.);
#7085=ORIENTED_EDGE('',*,*,#5328,.T.);
#7086=ORIENTED_EDGE('',*,*,#5325,.T.);
#7087=ORIENTED_EDGE('',*,*,#5066,.F.);
#7088=ORIENTED_EDGE('',*,*,#5333,.T.);
#7089=ORIENTED_EDGE('',*,*,#5330,.T.);
#7090=ORIENTED_EDGE('',*,*,#5062,.F.);
#7091=ORIENTED_EDGE('',*,*,#5338,.T.);
#7092=ORIENTED_EDGE('',*,*,#5335,.T.);
#7093=ORIENTED_EDGE('',*,*,#5058,.F.);
#7094=ORIENTED_EDGE('',*,*,#5343,.T.);
#7095=ORIENTED_EDGE('',*,*,#5340,.T.);
#7096=ORIENTED_EDGE('',*,*,#5054,.F.);
#7097=ORIENTED_EDGE('',*,*,#5348,.T.);
#7098=ORIENTED_EDGE('',*,*,#5345,.T.);
#7099=ORIENTED_EDGE('',*,*,#5050,.F.);
#7100=ORIENTED_EDGE('',*,*,#5353,.T.);
#7101=ORIENTED_EDGE('',*,*,#5350,.T.);
#7102=ORIENTED_EDGE('',*,*,#5046,.F.);
#7103=ORIENTED_EDGE('',*,*,#5358,.T.);
#7104=ORIENTED_EDGE('',*,*,#5355,.T.);
#7105=ORIENTED_EDGE('',*,*,#5042,.F.);
#7106=ORIENTED_EDGE('',*,*,#5363,.T.);
#7107=ORIENTED_EDGE('',*,*,#5360,.T.);
#7108=ORIENTED_EDGE('',*,*,#5038,.F.);
#7109=ORIENTED_EDGE('',*,*,#5368,.T.);
#7110=ORIENTED_EDGE('',*,*,#5365,.T.);
#7111=ORIENTED_EDGE('',*,*,#5034,.F.);
#7112=ORIENTED_EDGE('',*,*,#5373,.T.);
#7113=ORIENTED_EDGE('',*,*,#5370,.T.);
#7114=ORIENTED_EDGE('',*,*,#5030,.F.);
#7115=ORIENTED_EDGE('',*,*,#5378,.T.);
#7116=ORIENTED_EDGE('',*,*,#5375,.T.);
#7117=ORIENTED_EDGE('',*,*,#5026,.F.);
#7118=ORIENTED_EDGE('',*,*,#5383,.T.);
#7119=ORIENTED_EDGE('',*,*,#5380,.T.);
#7120=ORIENTED_EDGE('',*,*,#5182,.F.);
#7121=ORIENTED_EDGE('',*,*,#5188,.T.);
#7122=ORIENTED_EDGE('',*,*,#5185,.T.);
#7123=ORIENTED_EDGE('',*,*,#5178,.F.);
#7124=ORIENTED_EDGE('',*,*,#5193,.T.);
#7125=ORIENTED_EDGE('',*,*,#5190,.T.);
#7126=ORIENTED_EDGE('',*,*,#5174,.F.);
#7127=ORIENTED_EDGE('',*,*,#5198,.T.);
#7128=ORIENTED_EDGE('',*,*,#5195,.T.);
#7129=ORIENTED_EDGE('',*,*,#5170,.F.);
#7130=ORIENTED_EDGE('',*,*,#5203,.T.);
#7131=ORIENTED_EDGE('',*,*,#5200,.T.);
#7132=ORIENTED_EDGE('',*,*,#5166,.F.);
#7133=ORIENTED_EDGE('',*,*,#5208,.T.);
#7134=ORIENTED_EDGE('',*,*,#5205,.T.);
#7135=ORIENTED_EDGE('',*,*,#5162,.F.);
#7136=ORIENTED_EDGE('',*,*,#5213,.T.);
#7137=ORIENTED_EDGE('',*,*,#5210,.T.);
#7138=ORIENTED_EDGE('',*,*,#5158,.F.);
#7139=ORIENTED_EDGE('',*,*,#5218,.T.);
#7140=ORIENTED_EDGE('',*,*,#5215,.T.);
#7141=ORIENTED_EDGE('',*,*,#5154,.F.);
#7142=ORIENTED_EDGE('',*,*,#5223,.T.);
#7143=ORIENTED_EDGE('',*,*,#5220,.T.);
#7144=ORIENTED_EDGE('',*,*,#5150,.F.);
#7145=ORIENTED_EDGE('',*,*,#5228,.T.);
#7146=ORIENTED_EDGE('',*,*,#5225,.T.);
#7147=ORIENTED_EDGE('',*,*,#5146,.F.);
#7148=ORIENTED_EDGE('',*,*,#5233,.T.);
#7149=ORIENTED_EDGE('',*,*,#5230,.T.);
#7150=ORIENTED_EDGE('',*,*,#5142,.F.);
#7151=ORIENTED_EDGE('',*,*,#5238,.T.);
#7152=ORIENTED_EDGE('',*,*,#5235,.T.);
#7153=ORIENTED_EDGE('',*,*,#5138,.F.);
#7154=ORIENTED_EDGE('',*,*,#5243,.T.);
#7155=ORIENTED_EDGE('',*,*,#5240,.T.);
#7156=ORIENTED_EDGE('',*,*,#5134,.F.);
#7157=ORIENTED_EDGE('',*,*,#5248,.T.);
#7158=ORIENTED_EDGE('',*,*,#5245,.T.);
#7159=ORIENTED_EDGE('',*,*,#5130,.F.);
#7160=ORIENTED_EDGE('',*,*,#5253,.T.);
#7161=ORIENTED_EDGE('',*,*,#5250,.T.);
#7162=ORIENTED_EDGE('',*,*,#5126,.F.);
#7163=ORIENTED_EDGE('',*,*,#5258,.T.);
#7164=ORIENTED_EDGE('',*,*,#5255,.T.);
#7165=ORIENTED_EDGE('',*,*,#5122,.F.);
#7166=ORIENTED_EDGE('',*,*,#5263,.T.);
#7167=ORIENTED_EDGE('',*,*,#5260,.T.);
#7168=ORIENTED_EDGE('',*,*,#5118,.F.);
#7169=ORIENTED_EDGE('',*,*,#5268,.T.);
#7170=ORIENTED_EDGE('',*,*,#5265,.T.);
#7171=ORIENTED_EDGE('',*,*,#5114,.F.);
#7172=ORIENTED_EDGE('',*,*,#5273,.T.);
#7173=ORIENTED_EDGE('',*,*,#5270,.T.);
#7174=ORIENTED_EDGE('',*,*,#5110,.F.);
#7175=ORIENTED_EDGE('',*,*,#5278,.T.);
#7176=ORIENTED_EDGE('',*,*,#5275,.T.);
#7177=ORIENTED_EDGE('',*,*,#5106,.F.);
#7178=ORIENTED_EDGE('',*,*,#5283,.T.);
#7179=ORIENTED_EDGE('',*,*,#5280,.T.);
#7180=ORIENTED_EDGE('',*,*,#5102,.F.);
#7181=ORIENTED_EDGE('',*,*,#5288,.T.);
#7182=ORIENTED_EDGE('',*,*,#5285,.T.);
#7183=ORIENTED_EDGE('',*,*,#5098,.F.);
#7184=ORIENTED_EDGE('',*,*,#5293,.T.);
#7185=ORIENTED_EDGE('',*,*,#5290,.T.);
#7186=ORIENTED_EDGE('',*,*,#5094,.F.);
#7187=ORIENTED_EDGE('',*,*,#5298,.T.);
#7188=ORIENTED_EDGE('',*,*,#5295,.T.);
#7189=ORIENTED_EDGE('',*,*,#5090,.F.);
#7190=ORIENTED_EDGE('',*,*,#5303,.T.);
#7191=ORIENTED_EDGE('',*,*,#5300,.T.);
#7192=ORIENTED_EDGE('',*,*,#5086,.F.);
#7193=ORIENTED_EDGE('',*,*,#5308,.T.);
#7194=ORIENTED_EDGE('',*,*,#5305,.T.);
#7195=ORIENTED_EDGE('',*,*,#5082,.F.);
#7196=ORIENTED_EDGE('',*,*,#5313,.T.);
#7197=ORIENTED_EDGE('',*,*,#5310,.T.);
#7198=ORIENTED_EDGE('',*,*,#5078,.F.);
#7199=ORIENTED_EDGE('',*,*,#5397,.F.);
#7200=ORIENTED_EDGE('',*,*,#5420,.F.);
#7201=ORIENTED_EDGE('',*,*,#5423,.F.);
#7202=ORIENTED_EDGE('',*,*,#5423,.T.);
#7203=ORIENTED_EDGE('',*,*,#5418,.F.);
#7204=ORIENTED_EDGE('',*,*,#5424,.F.);
#7205=ORIENTED_EDGE('',*,*,#5398,.F.);
#7206=ORIENTED_EDGE('',*,*,#5424,.T.);
#7207=ORIENTED_EDGE('',*,*,#5386,.F.);
#7208=ORIENTED_EDGE('',*,*,#5425,.F.);
#7209=ORIENTED_EDGE('',*,*,#5394,.F.);
#7210=ORIENTED_EDGE('',*,*,#5425,.T.);
#7211=ORIENTED_EDGE('',*,*,#5412,.F.);
#7212=ORIENTED_EDGE('',*,*,#5426,.F.);
#7213=ORIENTED_EDGE('',*,*,#5395,.F.);
#7214=ORIENTED_EDGE('',*,*,#5414,.F.);
#7215=ORIENTED_EDGE('',*,*,#5396,.F.);
#7216=ORIENTED_EDGE('',*,*,#5426,.T.);
#7217=ORIENTED_EDGE('',*,*,#5415,.F.);
#7218=ORIENTED_EDGE('',*,*,#5390,.F.);
#7219=ORIENTED_EDGE('',*,*,#5427,.F.);
#7220=ORIENTED_EDGE('',*,*,#5427,.T.);
#7221=ORIENTED_EDGE('',*,*,#5389,.F.);
#7222=ORIENTED_EDGE('',*,*,#5428,.F.);
#7223=ORIENTED_EDGE('',*,*,#5417,.F.);
#7224=ORIENTED_EDGE('',*,*,#5428,.T.);
#7225=ORIENTED_EDGE('',*,*,#5393,.F.);
#7226=ORIENTED_EDGE('',*,*,#5429,.F.);
#7227=ORIENTED_EDGE('',*,*,#5388,.F.);
#7228=ORIENTED_EDGE('',*,*,#5429,.T.);
#7229=ORIENTED_EDGE('',*,*,#5392,.F.);
#7230=ORIENTED_EDGE('',*,*,#5430,.F.);
#7231=ORIENTED_EDGE('',*,*,#5413,.F.);
#7232=ORIENTED_EDGE('',*,*,#5391,.F.);
#7233=ORIENTED_EDGE('',*,*,#5410,.F.);
#7234=ORIENTED_EDGE('',*,*,#5430,.T.);
#7235=ORIENTED_EDGE('',*,*,#5400,.F.);
#7236=ORIENTED_EDGE('',*,*,#5431,.T.);
#7237=ORIENTED_EDGE('',*,*,#5432,.T.);
#7238=ORIENTED_EDGE('',*,*,#5433,.T.);
#7239=ORIENTED_EDGE('',*,*,#5434,.T.);
#7240=ORIENTED_EDGE('',*,*,#5433,.F.);
#7241=ORIENTED_EDGE('',*,*,#5434,.F.);
#7242=ORIENTED_EDGE('',*,*,#5435,.T.);
#7243=ORIENTED_EDGE('',*,*,#5436,.T.);
#7244=ORIENTED_EDGE('',*,*,#5435,.F.);
#7245=ORIENTED_EDGE('',*,*,#5437,.F.);
#7246=ORIENTED_EDGE('',*,*,#5438,.F.);
#7247=ORIENTED_EDGE('',*,*,#5439,.F.);
#7248=ORIENTED_EDGE('',*,*,#5440,.F.);
#7249=ORIENTED_EDGE('',*,*,#5436,.F.);
#7250=ORIENTED_EDGE('',*,*,#5441,.T.);
#7251=ORIENTED_EDGE('',*,*,#5442,.T.);
#7252=ORIENTED_EDGE('',*,*,#5441,.F.);
#7253=ORIENTED_EDGE('',*,*,#5431,.F.);
#7254=ORIENTED_EDGE('',*,*,#5443,.T.);
#7255=ORIENTED_EDGE('',*,*,#5432,.F.);
#7256=ORIENTED_EDGE('',*,*,#5443,.F.);
#7257=ORIENTED_EDGE('',*,*,#5437,.T.);
#7258=ORIENTED_EDGE('',*,*,#5444,.T.);
#7259=ORIENTED_EDGE('',*,*,#5440,.T.);
#7260=ORIENTED_EDGE('',*,*,#5439,.T.);
#7261=ORIENTED_EDGE('',*,*,#5444,.F.);
#7262=ORIENTED_EDGE('',*,*,#5438,.T.);
#7263=ORIENTED_EDGE('',*,*,#5442,.F.);
#7264=ORIENTED_EDGE('',*,*,#5445,.F.);
#7265=ORIENTED_EDGE('',*,*,#5446,.F.);
#7266=ORIENTED_EDGE('',*,*,#5447,.F.);
#7267=ORIENTED_EDGE('',*,*,#5448,.F.);
#7268=ORIENTED_EDGE('',*,*,#5446,.T.);
#7269=ORIENTED_EDGE('',*,*,#5449,.F.);
#7270=ORIENTED_EDGE('',*,*,#5450,.F.);
#7271=ORIENTED_EDGE('',*,*,#5451,.T.);
#7272=ORIENTED_EDGE('',*,*,#5447,.T.);
#7273=ORIENTED_EDGE('',*,*,#5451,.F.);
#7274=ORIENTED_EDGE('',*,*,#5452,.F.);
#7275=ORIENTED_EDGE('',*,*,#5453,.T.);
#7276=ORIENTED_EDGE('',*,*,#5448,.T.);
#7277=ORIENTED_EDGE('',*,*,#5453,.F.);
#7278=ORIENTED_EDGE('',*,*,#5454,.F.);
#7279=ORIENTED_EDGE('',*,*,#5455,.T.);
#7280=ORIENTED_EDGE('',*,*,#5445,.T.);
#7281=ORIENTED_EDGE('',*,*,#5455,.F.);
#7282=ORIENTED_EDGE('',*,*,#5456,.F.);
#7283=ORIENTED_EDGE('',*,*,#5449,.T.);
#7284=ORIENTED_EDGE('',*,*,#5450,.T.);
#7285=ORIENTED_EDGE('',*,*,#5456,.T.);
#7286=ORIENTED_EDGE('',*,*,#5454,.T.);
#7287=ORIENTED_EDGE('',*,*,#5452,.T.);
#9222=CYLINDRICAL_SURFACE('',#10269,18.);
#9223=CYLINDRICAL_SURFACE('',#10272,18.);
#9224=CYLINDRICAL_SURFACE('',#10275,18.);
#9225=CYLINDRICAL_SURFACE('',#10278,18.);
#9226=CYLINDRICAL_SURFACE('',#10281,18.);
#9227=CYLINDRICAL_SURFACE('',#10284,18.);
#9228=CYLINDRICAL_SURFACE('',#10287,18.);
#9229=CYLINDRICAL_SURFACE('',#10290,18.);
#9230=CYLINDRICAL_SURFACE('',#10293,18.);
#9231=CYLINDRICAL_SURFACE('',#10296,18.);
#9232=CYLINDRICAL_SURFACE('',#10299,18.);
#9233=CYLINDRICAL_SURFACE('',#10302,18.);
#9234=CYLINDRICAL_SURFACE('',#10305,18.);
#9235=CYLINDRICAL_SURFACE('',#10308,18.);
#9236=CYLINDRICAL_SURFACE('',#10311,18.);
#9237=CYLINDRICAL_SURFACE('',#10314,18.);
#9238=CYLINDRICAL_SURFACE('',#10317,18.);
#9239=CYLINDRICAL_SURFACE('',#10320,18.);
#9240=CYLINDRICAL_SURFACE('',#10323,18.);
#9241=CYLINDRICAL_SURFACE('',#10326,18.);
#9242=CYLINDRICAL_SURFACE('',#10329,18.);
#9243=CYLINDRICAL_SURFACE('',#10332,18.);
#9244=CYLINDRICAL_SURFACE('',#10335,18.);
#9245=CYLINDRICAL_SURFACE('',#10338,18.);
#9246=CYLINDRICAL_SURFACE('',#10341,18.);
#9247=CYLINDRICAL_SURFACE('',#10344,18.);
#9248=CYLINDRICAL_SURFACE('',#10347,18.);
#9249=CYLINDRICAL_SURFACE('',#10350,18.);
#9250=CYLINDRICAL_SURFACE('',#10353,18.);
#9251=CYLINDRICAL_SURFACE('',#10356,18.);
#9252=CYLINDRICAL_SURFACE('',#10359,18.);
#9253=CYLINDRICAL_SURFACE('',#10362,18.);
#9254=CYLINDRICAL_SURFACE('',#10365,18.);
#9255=CYLINDRICAL_SURFACE('',#10368,18.);
#9256=CYLINDRICAL_SURFACE('',#10371,18.);
#9257=CYLINDRICAL_SURFACE('',#10374,18.);
#9258=CYLINDRICAL_SURFACE('',#10377,18.);
#9259=CYLINDRICAL_SURFACE('',#10380,18.);
#9260=CYLINDRICAL_SURFACE('',#10383,18.);
#9261=CYLINDRICAL_SURFACE('',#10386,18.);
#9262=CYLINDRICAL_SURFACE('',#10469,25.);
#9263=CYLINDRICAL_SURFACE('',#10477,10.75);
#9264=CYLINDRICAL_SURFACE('',#10487,20.);
#9265=CYLINDRICAL_SURFACE('',#10502,8.35);
#9266=CYLINDRICAL_SURFACE('',#10511,3.10000000000001);
#9386=ADVANCED_FACE('',(#1020),#9222,.F.);
#9387=ADVANCED_FACE('',(#1021),#9223,.F.);
#9388=ADVANCED_FACE('',(#1022),#9224,.F.);
#9389=ADVANCED_FACE('',(#1023),#9225,.F.);
#9390=ADVANCED_FACE('',(#1024),#9226,.F.);
#9391=ADVANCED_FACE('',(#1025),#9227,.F.);
#9392=ADVANCED_FACE('',(#1026),#9228,.F.);
#9393=ADVANCED_FACE('',(#1027),#9229,.F.);
#9394=ADVANCED_FACE('',(#1028),#9230,.F.);
#9395=ADVANCED_FACE('',(#1029),#9231,.F.);
#9396=ADVANCED_FACE('',(#1030),#9232,.F.);
#9397=ADVANCED_FACE('',(#1031),#9233,.F.);
#9398=ADVANCED_FACE('',(#1032),#9234,.F.);
#9399=ADVANCED_FACE('',(#1033),#9235,.F.);
#9400=ADVANCED_FACE('',(#1034),#9236,.F.);
#9401=ADVANCED_FACE('',(#1035),#9237,.F.);
#9402=ADVANCED_FACE('',(#1036),#9238,.F.);
#9403=ADVANCED_FACE('',(#1037),#9239,.F.);
#9404=ADVANCED_FACE('',(#1038),#9240,.F.);
#9405=ADVANCED_FACE('',(#1039),#9241,.F.);
#9406=ADVANCED_FACE('',(#1040),#9242,.F.);
#9407=ADVANCED_FACE('',(#1041),#9243,.F.);
#9408=ADVANCED_FACE('',(#1042),#9244,.F.);
#9409=ADVANCED_FACE('',(#1043),#9245,.F.);
#9410=ADVANCED_FACE('',(#1044),#9246,.F.);
#9411=ADVANCED_FACE('',(#1045),#9247,.F.);
#9412=ADVANCED_FACE('',(#1046),#9248,.F.);
#9413=ADVANCED_FACE('',(#1047),#9249,.F.);
#9414=ADVANCED_FACE('',(#1048),#9250,.F.);
#9415=ADVANCED_FACE('',(#1049),#9251,.F.);
#9416=ADVANCED_FACE('',(#1050),#9252,.F.);
#9417=ADVANCED_FACE('',(#1051),#9253,.F.);
#9418=ADVANCED_FACE('',(#1052),#9254,.F.);
#9419=ADVANCED_FACE('',(#1053),#9255,.F.);
#9420=ADVANCED_FACE('',(#1054),#9256,.F.);
#9421=ADVANCED_FACE('',(#1055),#9257,.F.);
#9422=ADVANCED_FACE('',(#1056),#9258,.F.);
#9423=ADVANCED_FACE('',(#1057),#9259,.F.);
#9424=ADVANCED_FACE('',(#1058),#9260,.F.);
#9425=ADVANCED_FACE('',(#1059),#9261,.F.);
#9426=ADVANCED_FACE('',(#1060),#753,.F.);
#9427=ADVANCED_FACE('',(#1061),#754,.F.);
#9428=ADVANCED_FACE('',(#1062),#755,.F.);
#9429=ADVANCED_FACE('',(#1063),#756,.F.);
#9430=ADVANCED_FACE('',(#1064),#757,.F.);
#9431=ADVANCED_FACE('',(#1065),#758,.F.);
#9432=ADVANCED_FACE('',(#1066),#759,.F.);
#9433=ADVANCED_FACE('',(#1067),#760,.F.);
#9434=ADVANCED_FACE('',(#1068),#761,.F.);
#9435=ADVANCED_FACE('',(#1069),#762,.F.);
#9436=ADVANCED_FACE('',(#1070),#763,.F.);
#9437=ADVANCED_FACE('',(#1071),#764,.F.);
#9438=ADVANCED_FACE('',(#1072),#765,.F.);
#9439=ADVANCED_FACE('',(#1073),#766,.F.);
#9440=ADVANCED_FACE('',(#1074),#767,.F.);
#9441=ADVANCED_FACE('',(#1075),#768,.F.);
#9442=ADVANCED_FACE('',(#1076),#769,.F.);
#9443=ADVANCED_FACE('',(#1077),#770,.F.);
#9444=ADVANCED_FACE('',(#1078),#771,.F.);
#9445=ADVANCED_FACE('',(#1079),#772,.F.);
#9446=ADVANCED_FACE('',(#1080),#773,.F.);
#9447=ADVANCED_FACE('',(#1081),#774,.F.);
#9448=ADVANCED_FACE('',(#1082),#775,.F.);
#9449=ADVANCED_FACE('',(#1083),#776,.F.);
#9450=ADVANCED_FACE('',(#1084),#777,.F.);
#9451=ADVANCED_FACE('',(#1085),#778,.F.);
#9452=ADVANCED_FACE('',(#1086),#779,.F.);
#9453=ADVANCED_FACE('',(#1087),#780,.F.);
#9454=ADVANCED_FACE('',(#1088),#781,.F.);
#9455=ADVANCED_FACE('',(#1089),#782,.F.);
#9456=ADVANCED_FACE('',(#1090),#783,.F.);
#9457=ADVANCED_FACE('',(#1091),#784,.F.);
#9458=ADVANCED_FACE('',(#1092),#785,.F.);
#9459=ADVANCED_FACE('',(#1093),#786,.F.);
#9460=ADVANCED_FACE('',(#1094),#787,.F.);
#9461=ADVANCED_FACE('',(#1095),#788,.F.);
#9462=ADVANCED_FACE('',(#1096),#789,.F.);
#9463=ADVANCED_FACE('',(#1097),#790,.F.);
#9464=ADVANCED_FACE('',(#1098),#791,.F.);
#9465=ADVANCED_FACE('',(#1099),#792,.F.);
#9466=ADVANCED_FACE('',(#1100),#793,.F.);
#9467=ADVANCED_FACE('',(#1101),#794,.F.);
#9468=ADVANCED_FACE('',(#1102),#795,.F.);
#9469=ADVANCED_FACE('',(#1103),#796,.F.);
#9470=ADVANCED_FACE('',(#1104),#797,.F.);
#9471=ADVANCED_FACE('',(#1105),#798,.F.);
#9472=ADVANCED_FACE('',(#1106),#799,.F.);
#9473=ADVANCED_FACE('',(#1107),#800,.F.);
#9474=ADVANCED_FACE('',(#1108),#801,.F.);
#9475=ADVANCED_FACE('',(#1109),#802,.F.);
#9476=ADVANCED_FACE('',(#1110),#803,.F.);
#9477=ADVANCED_FACE('',(#1111),#804,.F.);
#9478=ADVANCED_FACE('',(#1112),#805,.F.);
#9479=ADVANCED_FACE('',(#1113),#806,.F.);
#9480=ADVANCED_FACE('',(#1114),#807,.F.);
#9481=ADVANCED_FACE('',(#1115),#808,.F.);
#9482=ADVANCED_FACE('',(#1116),#809,.F.);
#9483=ADVANCED_FACE('',(#1117),#810,.F.);
#9484=ADVANCED_FACE('',(#1118),#811,.F.);
#9485=ADVANCED_FACE('',(#1119),#812,.F.);
#9486=ADVANCED_FACE('',(#1120),#813,.F.);
#9487=ADVANCED_FACE('',(#1121),#814,.F.);
#9488=ADVANCED_FACE('',(#1122),#815,.F.);
#9489=ADVANCED_FACE('',(#1123),#816,.F.);
#9490=ADVANCED_FACE('',(#1124),#817,.F.);
#9491=ADVANCED_FACE('',(#1125),#818,.F.);
#9492=ADVANCED_FACE('',(#1126),#819,.F.);
#9493=ADVANCED_FACE('',(#1127),#820,.F.);
#9494=ADVANCED_FACE('',(#1128),#821,.F.);
#9495=ADVANCED_FACE('',(#1129),#822,.F.);
#9496=ADVANCED_FACE('',(#1130),#823,.F.);
#9497=ADVANCED_FACE('',(#1131),#824,.F.);
#9498=ADVANCED_FACE('',(#1132),#825,.F.);
#9499=ADVANCED_FACE('',(#1133),#826,.F.);
#9500=ADVANCED_FACE('',(#1134),#827,.F.);
#9501=ADVANCED_FACE('',(#1135),#828,.F.);
#9502=ADVANCED_FACE('',(#1136),#829,.F.);
#9503=ADVANCED_FACE('',(#1137),#830,.F.);
#9504=ADVANCED_FACE('',(#1138),#831,.F.);
#9505=ADVANCED_FACE('',(#1139),#832,.F.);
#9506=ADVANCED_FACE('',(#1140),#9262,.T.);
#9507=ADVANCED_FACE('',(#1141,#474),#833,.T.);
#9508=ADVANCED_FACE('',(#1142,#475),#834,.F.);
#9509=ADVANCED_FACE('',(#1143),#9263,.T.);
#9510=ADVANCED_FACE('',(#1144),#416,.F.);
#9511=ADVANCED_FACE('',(#1145),#417,.F.);
#9512=ADVANCED_FACE('',(#1146),#418,.F.);
#9513=ADVANCED_FACE('',(#1147),#419,.F.);
#9514=ADVANCED_FACE('',(#1148),#420,.F.);
#9515=ADVANCED_FACE('',(#1149),#421,.F.);
#9516=ADVANCED_FACE('',(#1150),#9264,.F.);
#9517=ADVANCED_FACE('',(#1151,#476),#835,.T.);
#9518=ADVANCED_FACE('',(#1152),#422,.T.);
#9519=ADVANCED_FACE('',(#1153),#423,.T.);
#9520=ADVANCED_FACE('',(#1154),#384,.T.);
#9521=ADVANCED_FACE('',(#1155),#424,.T.);
#9522=ADVANCED_FACE('',(#1156),#425,.T.);
#9523=ADVANCED_FACE('',(#1157),#426,.T.);
#9524=ADVANCED_FACE('',(#1158),#427,.T.);
#9525=ADVANCED_FACE('',(#1159),#385,.T.);
#9526=ADVANCED_FACE('',(#1160),#428,.T.);
#9527=ADVANCED_FACE('',(#1161),#429,.T.);
#9528=ADVANCED_FACE('',(#1162,#477),#836,.F.);
#9529=ADVANCED_FACE('',(#1163),#9265,.T.);
#9530=ADVANCED_FACE('',(#1164,#478,#479),#430,.F.);
#9531=ADVANCED_FACE('',(#1165),#345,.T.);
#9532=ADVANCED_FACE('',(#1166),#386,.F.);
#9533=ADVANCED_FACE('',(#1167),#9266,.F.);
#9534=ADVANCED_FACE('',(#1168,#480),#837,.F.);
#9535=ADVANCED_FACE('',(#1169),#838,.T.);
#9536=ADVANCED_FACE('',(#1170),#839,.F.);
#9537=ADVANCED_FACE('',(#1171),#840,.T.);
#9538=ADVANCED_FACE('',(#1172),#841,.F.);
#9539=ADVANCED_FACE('',(#1173),#842,.T.);
#9942=CLOSED_SHELL('',(#9386,#9387,#9388,#9389,#9390,#9391,#9392,#9393,
#9394,#9395,#9396,#9397,#9398,#9399,#9400,#9401,#9402,#9403,#9404,#9405,
#9406,#9407,#9408,#9409,#9410,#9411,#9412,#9413,#9414,#9415,#9416,#9417,
#9418,#9419,#9420,#9421,#9422,#9423,#9424,#9425,#9426,#9427,#9428,#9429,
#9430,#9431,#9432,#9433,#9434,#9435,#9436,#9437,#9438,#9439,#9440,#9441,
#9442,#9443,#9444,#9445,#9446,#9447,#9448,#9449,#9450,#9451,#9452,#9453,
#9454,#9455,#9456,#9457,#9458,#9459,#9460,#9461,#9462,#9463,#9464,#9465,
#9466,#9467,#9468,#9469,#9470,#9471,#9472,#9473,#9474,#9475,#9476,#9477,
#9478,#9479,#9480,#9481,#9482,#9483,#9484,#9485,#9486,#9487,#9488,#9489,
#9490,#9491,#9492,#9493,#9494,#9495,#9496,#9497,#9498,#9499,#9500,#9501,
#9502,#9503,#9504,#9505,#9506,#9507,#9508,#9509,#9510,#9511,#9512,#9513,
#9514,#9515,#9516,#9517,#9518,#9519,#9520,#9521,#9522,#9523,#9524,#9525,
#9526,#9527,#9528,#9529,#9530,#9531,#9532,#9533,#9534,#9535,#9536,#9537,
#9538,#9539));
#10268=AXIS2_PLACEMENT_3D('',#13916,#11235,#11236);
#10269=AXIS2_PLACEMENT_3D('',#13917,#11237,#11238);
#10270=AXIS2_PLACEMENT_3D('',#13922,#11240,#11241);
#10271=AXIS2_PLACEMENT_3D('',#13925,#11243,#11244);
#10272=AXIS2_PLACEMENT_3D('',#13926,#11245,#11246);
#10273=AXIS2_PLACEMENT_3D('',#13931,#11248,#11249);
#10274=AXIS2_PLACEMENT_3D('',#13934,#11251,#11252);
#10275=AXIS2_PLACEMENT_3D('',#13935,#11253,#11254);
#10276=AXIS2_PLACEMENT_3D('',#13940,#11256,#11257);
#10277=AXIS2_PLACEMENT_3D('',#13943,#11259,#11260);
#10278=AXIS2_PLACEMENT_3D('',#13944,#11261,#11262);
#10279=AXIS2_PLACEMENT_3D('',#13949,#11264,#11265);
#10280=AXIS2_PLACEMENT_3D('',#13952,#11267,#11268);
#10281=AXIS2_PLACEMENT_3D('',#13953,#11269,#11270);
#10282=AXIS2_PLACEMENT_3D('',#13958,#11272,#11273);
#10283=AXIS2_PLACEMENT_3D('',#13961,#11275,#11276);
#10284=AXIS2_PLACEMENT_3D('',#13962,#11277,#11278);
#10285=AXIS2_PLACEMENT_3D('',#13967,#11280,#11281);
#10286=AXIS2_PLACEMENT_3D('',#13970,#11283,#11284);
#10287=AXIS2_PLACEMENT_3D('',#13971,#11285,#11286);
#10288=AXIS2_PLACEMENT_3D('',#13976,#11288,#11289);
#10289=AXIS2_PLACEMENT_3D('',#13979,#11291,#11292);
#10290=AXIS2_PLACEMENT_3D('',#13980,#11293,#11294);
#10291=AXIS2_PLACEMENT_3D('',#13985,#11296,#11297);
#10292=AXIS2_PLACEMENT_3D('',#13988,#11299,#11300);
#10293=AXIS2_PLACEMENT_3D('',#13989,#11301,#11302);
#10294=AXIS2_PLACEMENT_3D('',#13994,#11304,#11305);
#10295=AXIS2_PLACEMENT_3D('',#13997,#11307,#11308);
#10296=AXIS2_PLACEMENT_3D('',#13998,#11309,#11310);
#10297=AXIS2_PLACEMENT_3D('',#14003,#11312,#11313);
#10298=AXIS2_PLACEMENT_3D('',#14006,#11315,#11316);
#10299=AXIS2_PLACEMENT_3D('',#14007,#11317,#11318);
#10300=AXIS2_PLACEMENT_3D('',#14012,#11320,#11321);
#10301=AXIS2_PLACEMENT_3D('',#14015,#11323,#11324);
#10302=AXIS2_PLACEMENT_3D('',#14016,#11325,#11326);
#10303=AXIS2_PLACEMENT_3D('',#14021,#11328,#11329);
#10304=AXIS2_PLACEMENT_3D('',#14024,#11331,#11332);
#10305=AXIS2_PLACEMENT_3D('',#14025,#11333,#11334);
#10306=AXIS2_PLACEMENT_3D('',#14030,#11336,#11337);
#10307=AXIS2_PLACEMENT_3D('',#14033,#11339,#11340);
#10308=AXIS2_PLACEMENT_3D('',#14034,#11341,#11342);
#10309=AXIS2_PLACEMENT_3D('',#14039,#11344,#11345);
#10310=AXIS2_PLACEMENT_3D('',#14042,#11347,#11348);
#10311=AXIS2_PLACEMENT_3D('',#14043,#11349,#11350);
#10312=AXIS2_PLACEMENT_3D('',#14048,#11352,#11353);
#10313=AXIS2_PLACEMENT_3D('',#14051,#11355,#11356);
#10314=AXIS2_PLACEMENT_3D('',#14052,#11357,#11358);
#10315=AXIS2_PLACEMENT_3D('',#14057,#11360,#11361);
#10316=AXIS2_PLACEMENT_3D('',#14060,#11363,#11364);
#10317=AXIS2_PLACEMENT_3D('',#14061,#11365,#11366);
#10318=AXIS2_PLACEMENT_3D('',#14066,#11368,#11369);
#10319=AXIS2_PLACEMENT_3D('',#14069,#11371,#11372);
#10320=AXIS2_PLACEMENT_3D('',#14070,#11373,#11374);
#10321=AXIS2_PLACEMENT_3D('',#14075,#11376,#11377);
#10322=AXIS2_PLACEMENT_3D('',#14078,#11379,#11380);
#10323=AXIS2_PLACEMENT_3D('',#14079,#11381,#11382);
#10324=AXIS2_PLACEMENT_3D('',#14084,#11384,#11385);
#10325=AXIS2_PLACEMENT_3D('',#14087,#11387,#11388);
#10326=AXIS2_PLACEMENT_3D('',#14088,#11389,#11390);
#10327=AXIS2_PLACEMENT_3D('',#14093,#11392,#11393);
#10328=AXIS2_PLACEMENT_3D('',#14096,#11395,#11396);
#10329=AXIS2_PLACEMENT_3D('',#14097,#11397,#11398);
#10330=AXIS2_PLACEMENT_3D('',#14102,#11400,#11401);
#10331=AXIS2_PLACEMENT_3D('',#14105,#11403,#11404);
#10332=AXIS2_PLACEMENT_3D('',#14106,#11405,#11406);
#10333=AXIS2_PLACEMENT_3D('',#14111,#11408,#11409);
#10334=AXIS2_PLACEMENT_3D('',#14114,#11411,#11412);
#10335=AXIS2_PLACEMENT_3D('',#14115,#11413,#11414);
#10336=AXIS2_PLACEMENT_3D('',#14120,#11416,#11417);
#10337=AXIS2_PLACEMENT_3D('',#14123,#11419,#11420);
#10338=AXIS2_PLACEMENT_3D('',#14124,#11421,#11422);
#10339=AXIS2_PLACEMENT_3D('',#14129,#11424,#11425);
#10340=AXIS2_PLACEMENT_3D('',#14132,#11427,#11428);
#10341=AXIS2_PLACEMENT_3D('',#14133,#11429,#11430);
#10342=AXIS2_PLACEMENT_3D('',#14138,#11432,#11433);
#10343=AXIS2_PLACEMENT_3D('',#14141,#11435,#11436);
#10344=AXIS2_PLACEMENT_3D('',#14142,#11437,#11438);
#10345=AXIS2_PLACEMENT_3D('',#14147,#11440,#11441);
#10346=AXIS2_PLACEMENT_3D('',#14150,#11443,#11444);
#10347=AXIS2_PLACEMENT_3D('',#14151,#11445,#11446);
#10348=AXIS2_PLACEMENT_3D('',#14156,#11448,#11449);
#10349=AXIS2_PLACEMENT_3D('',#14159,#11451,#11452);
#10350=AXIS2_PLACEMENT_3D('',#14160,#11453,#11454);
#10351=AXIS2_PLACEMENT_3D('',#14165,#11456,#11457);
#10352=AXIS2_PLACEMENT_3D('',#14168,#11459,#11460);
#10353=AXIS2_PLACEMENT_3D('',#14169,#11461,#11462);
#10354=AXIS2_PLACEMENT_3D('',#14174,#11464,#11465);
#10355=AXIS2_PLACEMENT_3D('',#14177,#11467,#11468);
#10356=AXIS2_PLACEMENT_3D('',#14178,#11469,#11470);
#10357=AXIS2_PLACEMENT_3D('',#14183,#11472,#11473);
#10358=AXIS2_PLACEMENT_3D('',#14186,#11475,#11476);
#10359=AXIS2_PLACEMENT_3D('',#14187,#11477,#11478);
#10360=AXIS2_PLACEMENT_3D('',#14192,#11480,#11481);
#10361=AXIS2_PLACEMENT_3D('',#14195,#11483,#11484);
#10362=AXIS2_PLACEMENT_3D('',#14196,#11485,#11486);
#10363=AXIS2_PLACEMENT_3D('',#14201,#11488,#11489);
#10364=AXIS2_PLACEMENT_3D('',#14204,#11491,#11492);
#10365=AXIS2_PLACEMENT_3D('',#14205,#11493,#11494);
#10366=AXIS2_PLACEMENT_3D('',#14210,#11496,#11497);
#10367=AXIS2_PLACEMENT_3D('',#14213,#11499,#11500);
#10368=AXIS2_PLACEMENT_3D('',#14214,#11501,#11502);
#10369=AXIS2_PLACEMENT_3D('',#14219,#11504,#11505);
#10370=AXIS2_PLACEMENT_3D('',#14222,#11507,#11508);
#10371=AXIS2_PLACEMENT_3D('',#14223,#11509,#11510);
#10372=AXIS2_PLACEMENT_3D('',#14228,#11512,#11513);
#10373=AXIS2_PLACEMENT_3D('',#14231,#11515,#11516);
#10374=AXIS2_PLACEMENT_3D('',#14232,#11517,#11518);
#10375=AXIS2_PLACEMENT_3D('',#14237,#11520,#11521);
#10376=AXIS2_PLACEMENT_3D('',#14240,#11523,#11524);
#10377=AXIS2_PLACEMENT_3D('',#14241,#11525,#11526);
#10378=AXIS2_PLACEMENT_3D('',#14246,#11528,#11529);
#10379=AXIS2_PLACEMENT_3D('',#14249,#11531,#11532);
#10380=AXIS2_PLACEMENT_3D('',#14250,#11533,#11534);
#10381=AXIS2_PLACEMENT_3D('',#14255,#11536,#11537);
#10382=AXIS2_PLACEMENT_3D('',#14258,#11539,#11540);
#10383=AXIS2_PLACEMENT_3D('',#14259,#11541,#11542);
#10384=AXIS2_PLACEMENT_3D('',#14264,#11544,#11545);
#10385=AXIS2_PLACEMENT_3D('',#14267,#11547,#11548);
#10386=AXIS2_PLACEMENT_3D('',#14268,#11549,#11550);
#10387=AXIS2_PLACEMENT_3D('',#14273,#11552,#11553);
#10388=AXIS2_PLACEMENT_3D('',#14276,#11555,#11556);
#10389=AXIS2_PLACEMENT_3D('',#14277,#11557,#11558);
#10390=AXIS2_PLACEMENT_3D('',#14283,#11562,#11563);
#10391=AXIS2_PLACEMENT_3D('',#14286,#11566,#11567);
#10392=AXIS2_PLACEMENT_3D('',#14292,#11571,#11572);
#10393=AXIS2_PLACEMENT_3D('',#14295,#11575,#11576);
#10394=AXIS2_PLACEMENT_3D('',#14301,#11580,#11581);
#10395=AXIS2_PLACEMENT_3D('',#14304,#11584,#11585);
#10396=AXIS2_PLACEMENT_3D('',#14310,#11589,#11590);
#10397=AXIS2_PLACEMENT_3D('',#14313,#11593,#11594);
#10398=AXIS2_PLACEMENT_3D('',#14319,#11598,#11599);
#10399=AXIS2_PLACEMENT_3D('',#14322,#11602,#11603);
#10400=AXIS2_PLACEMENT_3D('',#14328,#11607,#11608);
#10401=AXIS2_PLACEMENT_3D('',#14331,#11611,#11612);
#10402=AXIS2_PLACEMENT_3D('',#14337,#11616,#11617);
#10403=AXIS2_PLACEMENT_3D('',#14340,#11620,#11621);
#10404=AXIS2_PLACEMENT_3D('',#14346,#11625,#11626);
#10405=AXIS2_PLACEMENT_3D('',#14349,#11629,#11630);
#10406=AXIS2_PLACEMENT_3D('',#14355,#11634,#11635);
#10407=AXIS2_PLACEMENT_3D('',#14358,#11638,#11639);
#10408=AXIS2_PLACEMENT_3D('',#14364,#11643,#11644);
#10409=AXIS2_PLACEMENT_3D('',#14367,#11647,#11648);
#10410=AXIS2_PLACEMENT_3D('',#14373,#11652,#11653);
#10411=AXIS2_PLACEMENT_3D('',#14376,#11656,#11657);
#10412=AXIS2_PLACEMENT_3D('',#14382,#11661,#11662);
#10413=AXIS2_PLACEMENT_3D('',#14385,#11665,#11666);
#10414=AXIS2_PLACEMENT_3D('',#14391,#11670,#11671);
#10415=AXIS2_PLACEMENT_3D('',#14394,#11674,#11675);
#10416=AXIS2_PLACEMENT_3D('',#14400,#11679,#11680);
#10417=AXIS2_PLACEMENT_3D('',#14403,#11683,#11684);
#10418=AXIS2_PLACEMENT_3D('',#14409,#11688,#11689);
#10419=AXIS2_PLACEMENT_3D('',#14412,#11692,#11693);
#10420=AXIS2_PLACEMENT_3D('',#14418,#11697,#11698);
#10421=AXIS2_PLACEMENT_3D('',#14421,#11701,#11702);
#10422=AXIS2_PLACEMENT_3D('',#14427,#11706,#11707);
#10423=AXIS2_PLACEMENT_3D('',#14430,#11710,#11711);
#10424=AXIS2_PLACEMENT_3D('',#14436,#11715,#11716);
#10425=AXIS2_PLACEMENT_3D('',#14439,#11719,#11720);
#10426=AXIS2_PLACEMENT_3D('',#14445,#11724,#11725);
#10427=AXIS2_PLACEMENT_3D('',#14448,#11728,#11729);
#10428=AXIS2_PLACEMENT_3D('',#14454,#11733,#11734);
#10429=AXIS2_PLACEMENT_3D('',#14457,#11737,#11738);
#10430=AXIS2_PLACEMENT_3D('',#14463,#11742,#11743);
#10431=AXIS2_PLACEMENT_3D('',#14466,#11746,#11747);
#10432=AXIS2_PLACEMENT_3D('',#14472,#11751,#11752);
#10433=AXIS2_PLACEMENT_3D('',#14475,#11755,#11756);
#10434=AXIS2_PLACEMENT_3D('',#14481,#11760,#11761);
#10435=AXIS2_PLACEMENT_3D('',#14484,#11764,#11765);
#10436=AXIS2_PLACEMENT_3D('',#14490,#11769,#11770);
#10437=AXIS2_PLACEMENT_3D('',#14493,#11773,#11774);
#10438=AXIS2_PLACEMENT_3D('',#14499,#11778,#11779);
#10439=AXIS2_PLACEMENT_3D('',#14502,#11782,#11783);
#10440=AXIS2_PLACEMENT_3D('',#14508,#11787,#11788);
#10441=AXIS2_PLACEMENT_3D('',#14511,#11791,#11792);
#10442=AXIS2_PLACEMENT_3D('',#14517,#11796,#11797);
#10443=AXIS2_PLACEMENT_3D('',#14520,#11800,#11801);
#10444=AXIS2_PLACEMENT_3D('',#14526,#11805,#11806);
#10445=AXIS2_PLACEMENT_3D('',#14529,#11809,#11810);
#10446=AXIS2_PLACEMENT_3D('',#14535,#11814,#11815);
#10447=AXIS2_PLACEMENT_3D('',#14538,#11818,#11819);
#10448=AXIS2_PLACEMENT_3D('',#14544,#11823,#11824);
#10449=AXIS2_PLACEMENT_3D('',#14547,#11827,#11828);
#10450=AXIS2_PLACEMENT_3D('',#14553,#11832,#11833);
#10451=AXIS2_PLACEMENT_3D('',#14556,#11836,#11837);
#10452=AXIS2_PLACEMENT_3D('',#14562,#11841,#11842);
#10453=AXIS2_PLACEMENT_3D('',#14565,#11845,#11846);
#10454=AXIS2_PLACEMENT_3D('',#14571,#11850,#11851);
#10455=AXIS2_PLACEMENT_3D('',#14574,#11854,#11855);
#10456=AXIS2_PLACEMENT_3D('',#14580,#11859,#11860);
#10457=AXIS2_PLACEMENT_3D('',#14583,#11863,#11864);
#10458=AXIS2_PLACEMENT_3D('',#14589,#11868,#11869);
#10459=AXIS2_PLACEMENT_3D('',#14592,#11872,#11873);
#10460=AXIS2_PLACEMENT_3D('',#14598,#11877,#11878);
#10461=AXIS2_PLACEMENT_3D('',#14601,#11881,#11882);
#10462=AXIS2_PLACEMENT_3D('',#14607,#11886,#11887);
#10463=AXIS2_PLACEMENT_3D('',#14610,#11890,#11891);
#10464=AXIS2_PLACEMENT_3D('',#14616,#11895,#11896);
#10465=AXIS2_PLACEMENT_3D('',#14619,#11899,#11900);
#10466=AXIS2_PLACEMENT_3D('',#14625,#11904,#11905);
#10467=AXIS2_PLACEMENT_3D('',#14628,#11908,#11909);
#10468=AXIS2_PLACEMENT_3D('',#14634,#11913,#11914);
#10469=AXIS2_PLACEMENT_3D('',#14637,#11917,#11918);
#10470=AXIS2_PLACEMENT_3D('',#14675,#11919,#11920);
#10471=AXIS2_PLACEMENT_3D('',#14711,#11921,#11922);
#10472=AXIS2_PLACEMENT_3D('',#14712,#11923,#11924);
#10473=AXIS2_PLACEMENT_3D('',#14869,#11925,#11926);
#10474=AXIS2_PLACEMENT_3D('',#14870,#11927,#11928);
#10475=AXIS2_PLACEMENT_3D('',#14873,#11929,#11930);
#10476=AXIS2_PLACEMENT_3D('',#15038,#11931,#11932);
#10477=AXIS2_PLACEMENT_3D('',#15039,#11933,#11934);
#10478=AXIS2_PLACEMENT_3D('',#15041,#11935,#11936);
#10479=AXIS2_PLACEMENT_3D('',#16163,#11938,#11939);
#10480=AXIS2_PLACEMENT_3D('',#16231,#11940,#11941);
#10481=AXIS2_PLACEMENT_3D('',#16232,#11942,#11943);
#10482=AXIS2_PLACEMENT_3D('',#16233,#11944,#11945);
#10483=AXIS2_PLACEMENT_3D('',#16491,#11946,#11947);
#10484=AXIS2_PLACEMENT_3D('',#16534,#11948,#11949);
#10485=AXIS2_PLACEMENT_3D('',#16536,#11950,#11951);
#10486=AXIS2_PLACEMENT_3D('',#16537,#11952,#11953);
#10487=AXIS2_PLACEMENT_3D('',#16670,#11954,#11955);
#10488=AXIS2_PLACEMENT_3D('',#16672,#11956,#11957);
#10489=AXIS2_PLACEMENT_3D('',#16674,#11959,#11960);
#10490=AXIS2_PLACEMENT_3D('',#16735,#11961,#11962);
#10491=AXIS2_PLACEMENT_3D('',#16748,#11963,#11964);
#10492=AXIS2_PLACEMENT_3D('',#16749,#11965,#11966);
#10493=AXIS2_PLACEMENT_3D('',#16750,#11967,#11968);
#10494=AXIS2_PLACEMENT_3D('',#16763,#11969,#11970);
#10495=AXIS2_PLACEMENT_3D('',#16896,#11971,#11972);
#10496=AXIS2_PLACEMENT_3D('',#16909,#11973,#11974);
#10497=AXIS2_PLACEMENT_3D('',#16910,#11975,#11976);
#10498=AXIS2_PLACEMENT_3D('',#16911,#11977,#11978);
#10499=AXIS2_PLACEMENT_3D('',#16924,#11979,#11980);
#10500=AXIS2_PLACEMENT_3D('',#16985,#11981,#11982);
#10501=AXIS2_PLACEMENT_3D('',#16987,#11983,#11984);
#10502=AXIS2_PLACEMENT_3D('',#16988,#11985,#11986);
#10503=AXIS2_PLACEMENT_3D('',#16990,#11987,#11988);
#10504=AXIS2_PLACEMENT_3D('',#16993,#11990,#11991);
#10505=AXIS2_PLACEMENT_3D('',#17022,#11992,#11993);
#10506=AXIS2_PLACEMENT_3D('',#17023,#11994,#11995);
#10507=AXIS2_PLACEMENT_3D('',#17626,#11996,#11997);
#10508=AXIS2_PLACEMENT_3D('',#17629,#11999,#12000);
#10509=AXIS2_PLACEMENT_3D('',#17630,#12001,#12002);
#10510=AXIS2_PLACEMENT_3D('',#17631,#12003,#12004);
#10511=AXIS2_PLACEMENT_3D('',#17632,#12005,#12006);
#10512=AXIS2_PLACEMENT_3D('',#17634,#12008,#12009);
#10513=AXIS2_PLACEMENT_3D('',#17643,#12014,#12015);
#10514=AXIS2_PLACEMENT_3D('',#17649,#12019,#12020);
#10515=AXIS2_PLACEMENT_3D('',#17653,#12023,#12024);
#10516=AXIS2_PLACEMENT_3D('',#17657,#12027,#12028);
#10517=AXIS2_PLACEMENT_3D('',#17659,#12030,#12031);
#11235=DIRECTION('axis',(0.,0.,1.));
#11236=DIRECTION('refdir',(1.,0.,0.));
#11237=DIRECTION('center_axis',(0.,-1.,0.));
#11238=DIRECTION('ref_axis',(0.,0.,-1.));
#11239=DIRECTION('',(0.,-1.,0.));
#11240=DIRECTION('center_axis',(0.,-1.,0.));
#11241=DIRECTION('ref_axis',(0.,0.,-1.));
#11242=DIRECTION('',(0.,-1.,0.));
#11243=DIRECTION('center_axis',(0.,1.,0.));
#11244=DIRECTION('ref_axis',(0.,0.,1.));
#11245=DIRECTION('center_axis',(0.,-1.,0.));
#11246=DIRECTION('ref_axis',(0.,0.,-1.));
#11247=DIRECTION('',(0.,-1.,0.));
#11248=DIRECTION('center_axis',(0.,-1.,0.));
#11249=DIRECTION('ref_axis',(0.,0.,-1.));
#11250=DIRECTION('',(0.,-1.,0.));
#11251=DIRECTION('center_axis',(0.,1.,0.));
#11252=DIRECTION('ref_axis',(0.,0.,1.));
#11253=DIRECTION('center_axis',(0.,-1.,0.));
#11254=DIRECTION('ref_axis',(0.,0.,-1.));
#11255=DIRECTION('',(0.,-1.,0.));
#11256=DIRECTION('center_axis',(0.,-1.,0.));
#11257=DIRECTION('ref_axis',(0.,0.,-1.));
#11258=DIRECTION('',(0.,-1.,0.));
#11259=DIRECTION('center_axis',(0.,1.,0.));
#11260=DIRECTION('ref_axis',(0.,0.,1.));
#11261=DIRECTION('center_axis',(0.,-1.,0.));
#11262=DIRECTION('ref_axis',(0.,0.,-1.));
#11263=DIRECTION('',(0.,-1.,0.));
#11264=DIRECTION('center_axis',(0.,-1.,0.));
#11265=DIRECTION('ref_axis',(0.,0.,-1.));
#11266=DIRECTION('',(0.,-1.,0.));
#11267=DIRECTION('center_axis',(0.,1.,0.));
#11268=DIRECTION('ref_axis',(0.,0.,1.));
#11269=DIRECTION('center_axis',(0.,-1.,0.));
#11270=DIRECTION('ref_axis',(0.,0.,-1.));
#11271=DIRECTION('',(0.,-1.,0.));
#11272=DIRECTION('center_axis',(0.,-1.,0.));
#11273=DIRECTION('ref_axis',(0.,0.,-1.));
#11274=DIRECTION('',(0.,-1.,0.));
#11275=DIRECTION('center_axis',(0.,1.,0.));
#11276=DIRECTION('ref_axis',(0.,0.,1.));
#11277=DIRECTION('center_axis',(0.,-1.,0.));
#11278=DIRECTION('ref_axis',(0.,0.,-1.));
#11279=DIRECTION('',(0.,-1.,0.));
#11280=DIRECTION('center_axis',(0.,-1.,0.));
#11281=DIRECTION('ref_axis',(0.,0.,-1.));
#11282=DIRECTION('',(0.,-1.,0.));
#11283=DIRECTION('center_axis',(0.,1.,0.));
#11284=DIRECTION('ref_axis',(0.,0.,1.));
#11285=DIRECTION('center_axis',(0.,-1.,0.));
#11286=DIRECTION('ref_axis',(0.,0.,-1.));
#11287=DIRECTION('',(0.,-1.,0.));
#11288=DIRECTION('center_axis',(0.,-1.,0.));
#11289=DIRECTION('ref_axis',(0.,0.,-1.));
#11290=DIRECTION('',(0.,-1.,0.));
#11291=DIRECTION('center_axis',(0.,1.,0.));
#11292=DIRECTION('ref_axis',(0.,0.,1.));
#11293=DIRECTION('center_axis',(0.,-1.,0.));
#11294=DIRECTION('ref_axis',(0.,0.,-1.));
#11295=DIRECTION('',(0.,-1.,0.));
#11296=DIRECTION('center_axis',(0.,-1.,0.));
#11297=DIRECTION('ref_axis',(0.,0.,-1.));
#11298=DIRECTION('',(0.,-1.,0.));
#11299=DIRECTION('center_axis',(0.,1.,0.));
#11300=DIRECTION('ref_axis',(0.,0.,1.));
#11301=DIRECTION('center_axis',(0.,-1.,0.));
#11302=DIRECTION('ref_axis',(0.,0.,-1.));
#11303=DIRECTION('',(0.,-1.,0.));
#11304=DIRECTION('center_axis',(0.,-1.,0.));
#11305=DIRECTION('ref_axis',(0.,0.,-1.));
#11306=DIRECTION('',(0.,-1.,0.));
#11307=DIRECTION('center_axis',(0.,1.,0.));
#11308=DIRECTION('ref_axis',(0.,0.,1.));
#11309=DIRECTION('center_axis',(0.,-1.,0.));
#11310=DIRECTION('ref_axis',(0.,0.,-1.));
#11311=DIRECTION('',(0.,-1.,0.));
#11312=DIRECTION('center_axis',(0.,-1.,0.));
#11313=DIRECTION('ref_axis',(0.,0.,-1.));
#11314=DIRECTION('',(0.,-1.,0.));
#11315=DIRECTION('center_axis',(0.,1.,0.));
#11316=DIRECTION('ref_axis',(0.,0.,1.));
#11317=DIRECTION('center_axis',(0.,-1.,0.));
#11318=DIRECTION('ref_axis',(0.,0.,-1.));
#11319=DIRECTION('',(0.,-1.,0.));
#11320=DIRECTION('center_axis',(0.,-1.,0.));
#11321=DIRECTION('ref_axis',(0.,0.,-1.));
#11322=DIRECTION('',(0.,-1.,0.));
#11323=DIRECTION('center_axis',(0.,1.,0.));
#11324=DIRECTION('ref_axis',(0.,0.,1.));
#11325=DIRECTION('center_axis',(0.,-1.,0.));
#11326=DIRECTION('ref_axis',(0.,0.,-1.));
#11327=DIRECTION('',(0.,-1.,0.));
#11328=DIRECTION('center_axis',(0.,-1.,0.));
#11329=DIRECTION('ref_axis',(0.,0.,-1.));
#11330=DIRECTION('',(0.,-1.,0.));
#11331=DIRECTION('center_axis',(0.,1.,0.));
#11332=DIRECTION('ref_axis',(0.,0.,1.));
#11333=DIRECTION('center_axis',(0.,-1.,0.));
#11334=DIRECTION('ref_axis',(0.,0.,-1.));
#11335=DIRECTION('',(0.,-1.,0.));
#11336=DIRECTION('center_axis',(0.,-1.,0.));
#11337=DIRECTION('ref_axis',(0.,0.,-1.));
#11338=DIRECTION('',(0.,-1.,0.));
#11339=DIRECTION('center_axis',(0.,1.,0.));
#11340=DIRECTION('ref_axis',(0.,0.,1.));
#11341=DIRECTION('center_axis',(0.,-1.,0.));
#11342=DIRECTION('ref_axis',(0.,0.,-1.));
#11343=DIRECTION('',(0.,-1.,0.));
#11344=DIRECTION('center_axis',(0.,-1.,0.));
#11345=DIRECTION('ref_axis',(0.,0.,-1.));
#11346=DIRECTION('',(0.,-1.,0.));
#11347=DIRECTION('center_axis',(0.,1.,0.));
#11348=DIRECTION('ref_axis',(0.,0.,1.));
#11349=DIRECTION('center_axis',(0.,-1.,0.));
#11350=DIRECTION('ref_axis',(0.,0.,-1.));
#11351=DIRECTION('',(0.,-1.,0.));
#11352=DIRECTION('center_axis',(0.,-1.,0.));
#11353=DIRECTION('ref_axis',(0.,0.,-1.));
#11354=DIRECTION('',(0.,-1.,0.));
#11355=DIRECTION('center_axis',(0.,1.,0.));
#11356=DIRECTION('ref_axis',(0.,0.,1.));
#11357=DIRECTION('center_axis',(0.,-1.,0.));
#11358=DIRECTION('ref_axis',(0.,0.,-1.));
#11359=DIRECTION('',(0.,-1.,0.));
#11360=DIRECTION('center_axis',(0.,-1.,0.));
#11361=DIRECTION('ref_axis',(0.,0.,-1.));
#11362=DIRECTION('',(0.,-1.,0.));
#11363=DIRECTION('center_axis',(0.,1.,0.));
#11364=DIRECTION('ref_axis',(0.,0.,1.));
#11365=DIRECTION('center_axis',(0.,-1.,0.));
#11366=DIRECTION('ref_axis',(0.,0.,-1.));
#11367=DIRECTION('',(0.,-1.,0.));
#11368=DIRECTION('center_axis',(0.,-1.,0.));
#11369=DIRECTION('ref_axis',(0.,0.,-1.));
#11370=DIRECTION('',(0.,-1.,0.));
#11371=DIRECTION('center_axis',(0.,1.,0.));
#11372=DIRECTION('ref_axis',(0.,0.,1.));
#11373=DIRECTION('center_axis',(0.,-1.,0.));
#11374=DIRECTION('ref_axis',(0.,0.,-1.));
#11375=DIRECTION('',(0.,-1.,0.));
#11376=DIRECTION('center_axis',(0.,-1.,0.));
#11377=DIRECTION('ref_axis',(0.,0.,-1.));
#11378=DIRECTION('',(0.,-1.,0.));
#11379=DIRECTION('center_axis',(0.,1.,0.));
#11380=DIRECTION('ref_axis',(0.,0.,1.));
#11381=DIRECTION('center_axis',(0.,-1.,0.));
#11382=DIRECTION('ref_axis',(0.,0.,-1.));
#11383=DIRECTION('',(0.,-1.,0.));
#11384=DIRECTION('center_axis',(0.,-1.,0.));
#11385=DIRECTION('ref_axis',(0.,0.,-1.));
#11386=DIRECTION('',(0.,-1.,0.));
#11387=DIRECTION('center_axis',(0.,1.,0.));
#11388=DIRECTION('ref_axis',(0.,0.,1.));
#11389=DIRECTION('center_axis',(0.,-1.,0.));
#11390=DIRECTION('ref_axis',(0.,0.,-1.));
#11391=DIRECTION('',(0.,-1.,0.));
#11392=DIRECTION('center_axis',(0.,-1.,0.));
#11393=DIRECTION('ref_axis',(0.,0.,-1.));
#11394=DIRECTION('',(0.,-1.,0.));
#11395=DIRECTION('center_axis',(0.,1.,0.));
#11396=DIRECTION('ref_axis',(0.,0.,1.));
#11397=DIRECTION('center_axis',(0.,-1.,0.));
#11398=DIRECTION('ref_axis',(0.,0.,-1.));
#11399=DIRECTION('',(0.,-1.,0.));
#11400=DIRECTION('center_axis',(0.,-1.,0.));
#11401=DIRECTION('ref_axis',(0.,0.,-1.));
#11402=DIRECTION('',(0.,-1.,0.));
#11403=DIRECTION('center_axis',(0.,1.,0.));
#11404=DIRECTION('ref_axis',(0.,0.,1.));
#11405=DIRECTION('center_axis',(0.,-1.,0.));
#11406=DIRECTION('ref_axis',(0.,0.,-1.));
#11407=DIRECTION('',(0.,-1.,0.));
#11408=DIRECTION('center_axis',(0.,-1.,0.));
#11409=DIRECTION('ref_axis',(0.,0.,-1.));
#11410=DIRECTION('',(0.,-1.,0.));
#11411=DIRECTION('center_axis',(0.,1.,0.));
#11412=DIRECTION('ref_axis',(0.,0.,1.));
#11413=DIRECTION('center_axis',(0.,-1.,0.));
#11414=DIRECTION('ref_axis',(0.,0.,-1.));
#11415=DIRECTION('',(0.,-1.,0.));
#11416=DIRECTION('center_axis',(0.,-1.,0.));
#11417=DIRECTION('ref_axis',(0.,0.,-1.));
#11418=DIRECTION('',(0.,-1.,0.));
#11419=DIRECTION('center_axis',(0.,1.,0.));
#11420=DIRECTION('ref_axis',(0.,0.,1.));
#11421=DIRECTION('center_axis',(0.,-1.,0.));
#11422=DIRECTION('ref_axis',(0.,0.,-1.));
#11423=DIRECTION('',(0.,-1.,0.));
#11424=DIRECTION('center_axis',(0.,-1.,0.));
#11425=DIRECTION('ref_axis',(0.,0.,-1.));
#11426=DIRECTION('',(0.,-1.,0.));
#11427=DIRECTION('center_axis',(0.,1.,0.));
#11428=DIRECTION('ref_axis',(0.,0.,1.));
#11429=DIRECTION('center_axis',(0.,-1.,0.));
#11430=DIRECTION('ref_axis',(0.,0.,-1.));
#11431=DIRECTION('',(0.,-1.,0.));
#11432=DIRECTION('center_axis',(0.,-1.,0.));
#11433=DIRECTION('ref_axis',(0.,0.,-1.));
#11434=DIRECTION('',(0.,-1.,0.));
#11435=DIRECTION('center_axis',(0.,1.,0.));
#11436=DIRECTION('ref_axis',(0.,0.,1.));
#11437=DIRECTION('center_axis',(0.,-1.,0.));
#11438=DIRECTION('ref_axis',(0.,0.,-1.));
#11439=DIRECTION('',(0.,-1.,0.));
#11440=DIRECTION('center_axis',(0.,-1.,0.));
#11441=DIRECTION('ref_axis',(0.,0.,-1.));
#11442=DIRECTION('',(0.,-1.,0.));
#11443=DIRECTION('center_axis',(0.,1.,0.));
#11444=DIRECTION('ref_axis',(0.,0.,1.));
#11445=DIRECTION('center_axis',(0.,-1.,0.));
#11446=DIRECTION('ref_axis',(0.,0.,-1.));
#11447=DIRECTION('',(0.,-1.,0.));
#11448=DIRECTION('center_axis',(0.,-1.,0.));
#11449=DIRECTION('ref_axis',(0.,0.,-1.));
#11450=DIRECTION('',(0.,-1.,0.));
#11451=DIRECTION('center_axis',(0.,1.,0.));
#11452=DIRECTION('ref_axis',(0.,0.,1.));
#11453=DIRECTION('center_axis',(0.,-1.,0.));
#11454=DIRECTION('ref_axis',(0.,0.,-1.));
#11455=DIRECTION('',(0.,-1.,0.));
#11456=DIRECTION('center_axis',(0.,-1.,0.));
#11457=DIRECTION('ref_axis',(0.,0.,-1.));
#11458=DIRECTION('',(0.,-1.,0.));
#11459=DIRECTION('center_axis',(0.,1.,0.));
#11460=DIRECTION('ref_axis',(0.,0.,1.));
#11461=DIRECTION('center_axis',(0.,-1.,0.));
#11462=DIRECTION('ref_axis',(0.,0.,-1.));
#11463=DIRECTION('',(0.,-1.,0.));
#11464=DIRECTION('center_axis',(0.,-1.,0.));
#11465=DIRECTION('ref_axis',(0.,0.,-1.));
#11466=DIRECTION('',(0.,-1.,0.));
#11467=DIRECTION('center_axis',(0.,1.,0.));
#11468=DIRECTION('ref_axis',(0.,0.,1.));
#11469=DIRECTION('center_axis',(0.,-1.,0.));
#11470=DIRECTION('ref_axis',(0.,0.,-1.));
#11471=DIRECTION('',(0.,-1.,0.));
#11472=DIRECTION('center_axis',(0.,-1.,0.));
#11473=DIRECTION('ref_axis',(0.,0.,-1.));
#11474=DIRECTION('',(0.,-1.,0.));
#11475=DIRECTION('center_axis',(0.,1.,0.));
#11476=DIRECTION('ref_axis',(0.,0.,1.));
#11477=DIRECTION('center_axis',(0.,-1.,0.));
#11478=DIRECTION('ref_axis',(0.,0.,-1.));
#11479=DIRECTION('',(0.,-1.,0.));
#11480=DIRECTION('center_axis',(0.,-1.,0.));
#11481=DIRECTION('ref_axis',(0.,0.,-1.));
#11482=DIRECTION('',(0.,-1.,0.));
#11483=DIRECTION('center_axis',(0.,1.,0.));
#11484=DIRECTION('ref_axis',(0.,0.,1.));
#11485=DIRECTION('center_axis',(0.,-1.,0.));
#11486=DIRECTION('ref_axis',(0.,0.,-1.));
#11487=DIRECTION('',(0.,-1.,0.));
#11488=DIRECTION('center_axis',(0.,-1.,0.));
#11489=DIRECTION('ref_axis',(0.,0.,-1.));
#11490=DIRECTION('',(0.,-1.,0.));
#11491=DIRECTION('center_axis',(0.,1.,0.));
#11492=DIRECTION('ref_axis',(0.,0.,1.));
#11493=DIRECTION('center_axis',(0.,-1.,0.));
#11494=DIRECTION('ref_axis',(0.,0.,-1.));
#11495=DIRECTION('',(0.,-1.,0.));
#11496=DIRECTION('center_axis',(0.,-1.,0.));
#11497=DIRECTION('ref_axis',(0.,0.,-1.));
#11498=DIRECTION('',(0.,-1.,0.));
#11499=DIRECTION('center_axis',(0.,1.,0.));
#11500=DIRECTION('ref_axis',(0.,0.,1.));
#11501=DIRECTION('center_axis',(0.,-1.,0.));
#11502=DIRECTION('ref_axis',(0.,0.,-1.));
#11503=DIRECTION('',(0.,-1.,0.));
#11504=DIRECTION('center_axis',(0.,-1.,0.));
#11505=DIRECTION('ref_axis',(0.,0.,-1.));
#11506=DIRECTION('',(0.,-1.,0.));
#11507=DIRECTION('center_axis',(0.,1.,0.));
#11508=DIRECTION('ref_axis',(0.,0.,1.));
#11509=DIRECTION('center_axis',(0.,-1.,0.));
#11510=DIRECTION('ref_axis',(0.,0.,-1.));
#11511=DIRECTION('',(0.,-1.,0.));
#11512=DIRECTION('center_axis',(0.,-1.,0.));
#11513=DIRECTION('ref_axis',(0.,0.,-1.));
#11514=DIRECTION('',(0.,-1.,0.));
#11515=DIRECTION('center_axis',(0.,1.,0.));
#11516=DIRECTION('ref_axis',(0.,0.,1.));
#11517=DIRECTION('center_axis',(0.,-1.,0.));
#11518=DIRECTION('ref_axis',(0.,0.,-1.));
#11519=DIRECTION('',(0.,-1.,0.));
#11520=DIRECTION('center_axis',(0.,-1.,0.));
#11521=DIRECTION('ref_axis',(0.,0.,-1.));
#11522=DIRECTION('',(0.,-1.,0.));
#11523=DIRECTION('center_axis',(0.,1.,0.));
#11524=DIRECTION('ref_axis',(0.,0.,1.));
#11525=DIRECTION('center_axis',(0.,-1.,0.));
#11526=DIRECTION('ref_axis',(0.,0.,-1.));
#11527=DIRECTION('',(0.,-1.,0.));
#11528=DIRECTION('center_axis',(0.,-1.,0.));
#11529=DIRECTION('ref_axis',(0.,0.,-1.));
#11530=DIRECTION('',(0.,-1.,0.));
#11531=DIRECTION('center_axis',(0.,1.,0.));
#11532=DIRECTION('ref_axis',(0.,0.,1.));
#11533=DIRECTION('center_axis',(0.,-1.,0.));
#11534=DIRECTION('ref_axis',(0.,0.,-1.));
#11535=DIRECTION('',(0.,-1.,0.));
#11536=DIRECTION('center_axis',(0.,-1.,0.));
#11537=DIRECTION('ref_axis',(0.,0.,-1.));
#11538=DIRECTION('',(0.,-1.,0.));
#11539=DIRECTION('center_axis',(0.,1.,0.));
#11540=DIRECTION('ref_axis',(0.,0.,1.));
#11541=DIRECTION('center_axis',(0.,-1.,0.));
#11542=DIRECTION('ref_axis',(0.,0.,-1.));
#11543=DIRECTION('',(0.,-1.,0.));
#11544=DIRECTION('center_axis',(0.,-1.,0.));
#11545=DIRECTION('ref_axis',(0.,0.,-1.));
#11546=DIRECTION('',(0.,-1.,0.));
#11547=DIRECTION('center_axis',(0.,1.,0.));
#11548=DIRECTION('ref_axis',(0.,0.,1.));
#11549=DIRECTION('center_axis',(0.,-1.,0.));
#11550=DIRECTION('ref_axis',(0.,0.,-1.));
#11551=DIRECTION('',(0.,-1.,0.));
#11552=DIRECTION('center_axis',(0.,-1.,0.));
#11553=DIRECTION('ref_axis',(0.,0.,-1.));
#11554=DIRECTION('',(0.,-1.,0.));
#11555=DIRECTION('center_axis',(0.,1.,0.));
#11556=DIRECTION('ref_axis',(0.,0.,1.));
#11557=DIRECTION('center_axis',(0.598674156532674,0.,0.800992668068748));
#11558=DIRECTION('ref_axis',(0.800992668068748,0.,-0.598674156532674));
#11559=DIRECTION('',(0.800992668068748,0.,-0.598674156532674));
#11560=DIRECTION('',(0.,-1.,0.));
#11561=DIRECTION('',(0.800992668068748,0.,-0.598674156532674));
#11562=DIRECTION('center_axis',(-0.598674156532673,0.,0.800992668068749));
#11563=DIRECTION('ref_axis',(0.800992668068749,0.,0.598674156532673));
#11564=DIRECTION('',(0.800992668068749,0.,0.598674156532673));
#11565=DIRECTION('',(0.800992668068749,0.,0.598674156532673));
#11566=DIRECTION('center_axis',(0.716606343753432,0.,0.697477847743093));
#11567=DIRECTION('ref_axis',(0.697477847743093,0.,-0.716606343753432));
#11568=DIRECTION('',(0.697477847743093,0.,-0.716606343753432));
#11569=DIRECTION('',(0.,-1.,0.));
#11570=DIRECTION('',(0.697477847743093,0.,-0.716606343753432));
#11571=DIRECTION('center_axis',(-0.466000624692467,0.,0.884784390564295));
#11572=DIRECTION('ref_axis',(0.884784390564295,0.,0.466000624692467));
#11573=DIRECTION('',(0.884784390564295,0.,0.466000624692467));
#11574=DIRECTION('',(0.884784390564295,0.,0.466000624692467));
#11575=DIRECTION('center_axis',(0.816893304510879,0.,0.57678880800974));
#11576=DIRECTION('ref_axis',(0.57678880800974,0.,-0.816893304510879));
#11577=DIRECTION('',(0.57678880800974,0.,-0.816893304510879));
#11578=DIRECTION('',(0.,-1.,0.));
#11579=DIRECTION('',(0.57678880800974,0.,-0.816893304510879));
#11580=DIRECTION('center_axis',(-0.321852610904928,0.,0.946789784933108));
#11581=DIRECTION('ref_axis',(0.946789784933108,0.,0.321852610904928));
#11582=DIRECTION('',(0.946789784933108,0.,0.321852610904928));
#11583=DIRECTION('',(0.946789784933108,0.,0.321852610904928));
#11584=DIRECTION('center_axis',(0.897065640997825,0.,0.441897313570881));
#11585=DIRECTION('ref_axis',(0.441897313570881,0.,-0.897065640997825));
#11586=DIRECTION('',(0.441897313570881,0.,-0.897065640997825));
#11587=DIRECTION('',(0.,-1.,0.));
#11588=DIRECTION('',(0.441897313570881,0.,-0.897065640997825));
#11589=DIRECTION('center_axis',(-0.169779517669335,0.,0.985482072581723));
#11590=DIRECTION('ref_axis',(0.985482072581723,0.,0.169779517669335));
#11591=DIRECTION('',(0.985482072581723,0.,0.169779517669335));
#11592=DIRECTION('',(0.985482072581723,0.,0.169779517669335));
#11593=DIRECTION('center_axis',(0.955149244213231,0.,0.296124840698806));
#11594=DIRECTION('ref_axis',(0.296124840698806,0.,-0.955149244213231));
#11595=DIRECTION('',(0.296124840698806,0.,-0.955149244213231));
#11596=DIRECTION('',(0.,-1.,0.));
#11597=DIRECTION('',(0.296124840698806,0.,-0.955149244213231));
#11598=DIRECTION('center_axis',(-0.013525889242808,0.,0.99990852097589));
#11599=DIRECTION('ref_axis',(0.99990852097589,0.,0.013525889242808));
#11600=DIRECTION('',(0.99990852097589,0.,0.013525889242808));
#11601=DIRECTION('',(0.99990852097589,0.,0.013525889242808));
#11602=DIRECTION('center_axis',(0.989713903077508,0.,0.143060791466725));
#11603=DIRECTION('ref_axis',(0.143060791466725,0.,-0.989713903077508));
#11604=DIRECTION('',(0.143060791466725,0.,-0.989713903077508));
#11605=DIRECTION('',(0.,-1.,0.));
#11606=DIRECTION('',(0.143060791466725,0.,-0.989713903077508));
#11607=DIRECTION('center_axis',(0.143060791466729,0.,0.989713903077507));
#11608=DIRECTION('ref_axis',(0.989713903077507,0.,-0.143060791466729));
#11609=DIRECTION('',(0.989713903077507,0.,-0.143060791466729));
#11610=DIRECTION('',(0.989713903077507,0.,-0.143060791466729));
#11611=DIRECTION('center_axis',(0.99990852097589,0.,-0.0135258892428123));
#11612=DIRECTION('ref_axis',(-0.0135258892428123,0.,-0.99990852097589));
#11613=DIRECTION('',(-0.0135258892428123,0.,-0.99990852097589));
#11614=DIRECTION('',(0.,-1.,0.));
#11615=DIRECTION('',(-0.0135258892428123,0.,-0.99990852097589));
#11616=DIRECTION('center_axis',(0.29612484069881,0.,0.95514924421323));
#11617=DIRECTION('ref_axis',(0.95514924421323,0.,-0.29612484069881));
#11618=DIRECTION('',(0.95514924421323,0.,-0.29612484069881));
#11619=DIRECTION('',(0.95514924421323,0.,-0.29612484069881));
#11620=DIRECTION('center_axis',(0.985482072581722,0.,-0.169779517669339));
#11621=DIRECTION('ref_axis',(-0.169779517669339,0.,-0.985482072581722));
#11622=DIRECTION('',(-0.169779517669339,0.,-0.985482072581722));
#11623=DIRECTION('',(0.,-1.,0.));
#11624=DIRECTION('',(-0.169779517669339,0.,-0.985482072581722));
#11625=DIRECTION('center_axis',(0.441897313570885,0.,0.897065640997823));
#11626=DIRECTION('ref_axis',(0.897065640997823,0.,-0.441897313570885));
#11627=DIRECTION('',(0.897065640997823,0.,-0.441897313570885));
#11628=DIRECTION('',(0.897065640997823,0.,-0.441897313570885));
#11629=DIRECTION('center_axis',(0.946789784933107,0.,-0.321852610904932));
#11630=DIRECTION('ref_axis',(-0.321852610904932,0.,-0.946789784933107));
#11631=DIRECTION('',(-0.321852610904932,0.,-0.946789784933107));
#11632=DIRECTION('',(0.,-1.,0.));
#11633=DIRECTION('',(-0.321852610904932,0.,-0.946789784933107));
#11634=DIRECTION('center_axis',(0.576788808009743,0.,0.816893304510877));
#11635=DIRECTION('ref_axis',(0.816893304510876,0.,-0.576788808009743));
#11636=DIRECTION('',(0.816893304510877,0.,-0.576788808009743));
#11637=DIRECTION('',(0.816893304510877,0.,-0.576788808009743));
#11638=DIRECTION('center_axis',(0.884784390564293,0.,-0.466000624692471));
#11639=DIRECTION('ref_axis',(-0.466000624692471,0.,-0.884784390564292));
#11640=DIRECTION('',(-0.466000624692471,0.,-0.884784390564293));
#11641=DIRECTION('',(0.,-1.,0.));
#11642=DIRECTION('',(-0.466000624692471,0.,-0.884784390564293));
#11643=DIRECTION('center_axis',(0.697477847743097,0.,0.716606343753429));
#11644=DIRECTION('ref_axis',(0.716606343753429,0.,-0.697477847743097));
#11645=DIRECTION('',(0.716606343753429,0.,-0.697477847743097));
#11646=DIRECTION('',(0.716606343753429,0.,-0.697477847743097));
#11647=DIRECTION('center_axis',(0.800992668068746,0.,-0.598674156532677));
#11648=DIRECTION('ref_axis',(-0.598674156532677,0.,-0.800992668068746));
#11649=DIRECTION('',(-0.598674156532677,0.,-0.800992668068746));
#11650=DIRECTION('',(0.,-1.,0.));
#11651=DIRECTION('',(-0.598674156532677,0.,-0.800992668068746));
#11652=DIRECTION('center_axis',(0.800992668068751,0.,0.59867415653267));
#11653=DIRECTION('ref_axis',(0.59867415653267,0.,-0.800992668068751));
#11654=DIRECTION('',(0.59867415653267,0.,-0.800992668068751));
#11655=DIRECTION('',(0.59867415653267,0.,-0.800992668068751));
#11656=DIRECTION('center_axis',(0.697477847743091,0.,-0.716606343753435));
#11657=DIRECTION('ref_axis',(-0.716606343753435,0.,-0.697477847743091));
#11658=DIRECTION('',(-0.716606343753435,0.,-0.697477847743091));
#11659=DIRECTION('',(0.,-1.,0.));
#11660=DIRECTION('',(-0.716606343753435,0.,-0.697477847743091));
#11661=DIRECTION('center_axis',(0.884784390564296,0.,0.466000624692464));
#11662=DIRECTION('ref_axis',(0.466000624692464,0.,-0.884784390564296));
#11663=DIRECTION('',(0.466000624692464,0.,-0.884784390564296));
#11664=DIRECTION('',(0.466000624692464,0.,-0.884784390564296));
#11665=DIRECTION('center_axis',(0.576788808009737,0.,-0.816893304510881));
#11666=DIRECTION('ref_axis',(-0.816893304510881,0.,-0.576788808009737));
#11667=DIRECTION('',(-0.816893304510881,0.,-0.576788808009737));
#11668=DIRECTION('',(0.,-1.,0.));
#11669=DIRECTION('',(-0.816893304510881,0.,-0.576788808009737));
#11670=DIRECTION('center_axis',(0.946789784933109,0.,0.321852610904925));
#11671=DIRECTION('ref_axis',(0.321852610904925,0.,-0.946789784933109));
#11672=DIRECTION('',(0.321852610904925,0.,-0.946789784933109));
#11673=DIRECTION('',(0.321852610904925,0.,-0.946789784933109));
#11674=DIRECTION('center_axis',(0.441897313570878,0.,-0.897065640997826));
#11675=DIRECTION('ref_axis',(-0.897065640997827,0.,-0.441897313570878));
#11676=DIRECTION('',(-0.897065640997826,0.,-0.441897313570878));
#11677=DIRECTION('',(0.,-1.,0.));
#11678=DIRECTION('',(-0.897065640997826,0.,-0.441897313570878));
#11679=DIRECTION('center_axis',(0.985482072581723,0.,0.169779517669331));
#11680=DIRECTION('ref_axis',(0.169779517669331,0.,-0.985482072581724));
#11681=DIRECTION('',(0.169779517669331,0.,-0.985482072581723));
#11682=DIRECTION('',(0.169779517669331,0.,-0.985482072581723));
#11683=DIRECTION('center_axis',(0.296124840698803,0.,-0.955149244213232));
#11684=DIRECTION('ref_axis',(-0.955149244213232,0.,-0.296124840698803));
#11685=DIRECTION('',(-0.955149244213232,0.,-0.296124840698803));
#11686=DIRECTION('',(0.,-1.,0.));
#11687=DIRECTION('',(-0.955149244213232,0.,-0.296124840698803));
#11688=DIRECTION('center_axis',(0.99990852097589,0.,0.0135258892428046));
#11689=DIRECTION('ref_axis',(0.0135258892428046,0.,-0.99990852097589));
#11690=DIRECTION('',(0.0135258892428046,0.,-0.99990852097589));
#11691=DIRECTION('',(0.0135258892428046,0.,-0.99990852097589));
#11692=DIRECTION('center_axis',(0.143060791466722,0.,-0.989713903077508));
#11693=DIRECTION('ref_axis',(-0.989713903077508,0.,-0.143060791466722));
#11694=DIRECTION('',(-0.989713903077508,0.,-0.143060791466722));
#11695=DIRECTION('',(0.,-1.,0.));
#11696=DIRECTION('',(-0.989713903077508,0.,-0.143060791466722));
#11697=DIRECTION('center_axis',(0.989713903077507,0.,-0.143060791466733));
#11698=DIRECTION('ref_axis',(-0.143060791466733,0.,-0.989713903077507));
#11699=DIRECTION('',(-0.143060791466733,0.,-0.989713903077507));
#11700=DIRECTION('',(-0.143060791466733,0.,-0.989713903077507));
#11701=DIRECTION('center_axis',(-0.0135258892428158,0.,-0.99990852097589));
#11702=DIRECTION('ref_axis',(-0.99990852097589,0.,0.0135258892428158));
#11703=DIRECTION('',(-0.99990852097589,0.,0.0135258892428158));
#11704=DIRECTION('',(0.,-1.,0.));
#11705=DIRECTION('',(-0.99990852097589,0.,0.0135258892428158));
#11706=DIRECTION('center_axis',(0.955149244213229,0.,-0.296124840698814));
#11707=DIRECTION('ref_axis',(-0.296124840698814,0.,-0.955149244213229));
#11708=DIRECTION('',(-0.296124840698814,0.,-0.955149244213229));
#11709=DIRECTION('',(-0.296124840698814,0.,-0.955149244213229));
#11710=DIRECTION('center_axis',(-0.169779517669343,0.,-0.985482072581721));
#11711=DIRECTION('ref_axis',(-0.985482072581721,0.,0.169779517669343));
#11712=DIRECTION('',(-0.985482072581721,0.,0.169779517669343));
#11713=DIRECTION('',(0.,-1.,0.));
#11714=DIRECTION('',(-0.985482072581721,0.,0.169779517669343));
#11715=DIRECTION('center_axis',(0.897065640997821,0.,-0.441897313570888));
#11716=DIRECTION('ref_axis',(-0.441897313570888,0.,-0.897065640997821));
#11717=DIRECTION('',(-0.441897313570888,0.,-0.897065640997821));
#11718=DIRECTION('',(-0.441897313570888,0.,-0.897065640997821));
#11719=DIRECTION('center_axis',(-0.321852610904936,0.,-0.946789784933105));
#11720=DIRECTION('ref_axis',(-0.946789784933106,0.,0.321852610904936));
#11721=DIRECTION('',(-0.946789784933105,0.,0.321852610904936));
#11722=DIRECTION('',(0.,-1.,0.));
#11723=DIRECTION('',(-0.946789784933105,0.,0.321852610904936));
#11724=DIRECTION('center_axis',(0.816893304510874,0.,-0.576788808009746));
#11725=DIRECTION('ref_axis',(-0.576788808009746,0.,-0.816893304510874));
#11726=DIRECTION('',(-0.576788808009746,0.,-0.816893304510874));
#11727=DIRECTION('',(-0.576788808009746,0.,-0.816893304510874));
#11728=DIRECTION('center_axis',(-0.466000624692474,0.,-0.884784390564291));
#11729=DIRECTION('ref_axis',(-0.884784390564291,0.,0.466000624692474));
#11730=DIRECTION('',(-0.884784390564291,0.,0.466000624692474));
#11731=DIRECTION('',(0.,-1.,0.));
#11732=DIRECTION('',(-0.884784390564291,0.,0.466000624692474));
#11733=DIRECTION('center_axis',(0.716606343753427,0.,-0.697477847743099));
#11734=DIRECTION('ref_axis',(-0.697477847743099,0.,-0.716606343753427));
#11735=DIRECTION('',(-0.697477847743099,0.,-0.716606343753427));
#11736=DIRECTION('',(-0.697477847743099,0.,-0.716606343753427));
#11737=DIRECTION('center_axis',(-0.598674156532674,0.,-0.800992668068748));
#11738=DIRECTION('ref_axis',(-0.800992668068748,0.,0.598674156532674));
#11739=DIRECTION('',(-0.800992668068748,0.,0.598674156532674));
#11740=DIRECTION('',(0.,-1.,0.));
#11741=DIRECTION('',(-0.800992668068748,0.,0.598674156532674));
#11742=DIRECTION('center_axis',(0.598674156532673,0.,-0.800992668068749));
#11743=DIRECTION('ref_axis',(-0.800992668068749,0.,-0.598674156532673));
#11744=DIRECTION('',(-0.800992668068749,0.,-0.598674156532673));
#11745=DIRECTION('',(-0.800992668068749,0.,-0.598674156532673));
#11746=DIRECTION('center_axis',(-0.716606343753437,0.,-0.697477847743088));
#11747=DIRECTION('ref_axis',(-0.697477847743088,0.,0.716606343753437));
#11748=DIRECTION('',(-0.697477847743088,0.,0.716606343753437));
#11749=DIRECTION('',(0.,-1.,0.));
#11750=DIRECTION('',(-0.697477847743088,0.,0.716606343753437));
#11751=DIRECTION('center_axis',(0.466000624692461,0.,-0.884784390564298));
#11752=DIRECTION('ref_axis',(-0.884784390564298,0.,-0.466000624692461));
#11753=DIRECTION('',(-0.884784390564298,0.,-0.466000624692461));
#11754=DIRECTION('',(-0.884784390564298,0.,-0.466000624692461));
#11755=DIRECTION('center_axis',(-0.816893304510883,0.,-0.576788808009734));
#11756=DIRECTION('ref_axis',(-0.576788808009734,0.,0.816893304510883));
#11757=DIRECTION('',(-0.576788808009734,0.,0.816893304510883));
#11758=DIRECTION('',(0.,-1.,0.));
#11759=DIRECTION('',(-0.576788808009734,0.,0.816893304510883));
#11760=DIRECTION('center_axis',(0.321852610904921,0.,-0.94678978493311));
#11761=DIRECTION('ref_axis',(-0.94678978493311,0.,-0.321852610904921));
#11762=DIRECTION('',(-0.94678978493311,0.,-0.321852610904921));
#11763=DIRECTION('',(-0.94678978493311,0.,-0.321852610904921));
#11764=DIRECTION('center_axis',(-0.897065640997828,0.,-0.441897313570875));
#11765=DIRECTION('ref_axis',(-0.441897313570875,0.,0.897065640997828));
#11766=DIRECTION('',(-0.441897313570875,0.,0.897065640997828));
#11767=DIRECTION('',(0.,-1.,0.));
#11768=DIRECTION('',(-0.441897313570875,0.,0.897065640997828));
#11769=DIRECTION('center_axis',(0.169779517669328,0.,-0.985482072581724));
#11770=DIRECTION('ref_axis',(-0.985482072581724,0.,-0.169779517669328));
#11771=DIRECTION('',(-0.985482072581724,0.,-0.169779517669328));
#11772=DIRECTION('',(-0.985482072581724,0.,-0.169779517669328));
#11773=DIRECTION('center_axis',(-0.955149244213233,0.,-0.296124840698799));
#11774=DIRECTION('ref_axis',(-0.296124840698799,0.,0.955149244213233));
#11775=DIRECTION('',(-0.296124840698799,0.,0.955149244213233));
#11776=DIRECTION('',(0.,-1.,0.));
#11777=DIRECTION('',(-0.296124840698799,0.,0.955149244213233));
#11778=DIRECTION('center_axis',(0.0135258892428006,0.,-0.99990852097589));
#11779=DIRECTION('ref_axis',(-0.99990852097589,0.,-0.0135258892428006));
#11780=DIRECTION('',(-0.99990852097589,0.,-0.0135258892428006));
#11781=DIRECTION('',(-0.99990852097589,0.,-0.0135258892428006));
#11782=DIRECTION('center_axis',(-0.989713903077509,0.,-0.143060791466718));
#11783=DIRECTION('ref_axis',(-0.143060791466718,0.,0.989713903077509));
#11784=DIRECTION('',(-0.143060791466718,0.,0.989713903077509));
#11785=DIRECTION('',(0.,-1.,0.));
#11786=DIRECTION('',(-0.143060791466718,0.,0.989713903077509));
#11787=DIRECTION('center_axis',(-0.143060791466736,0.,-0.989713903077506));
#11788=DIRECTION('ref_axis',(-0.989713903077506,0.,0.143060791466736));
#11789=DIRECTION('',(-0.989713903077506,0.,0.143060791466736));
#11790=DIRECTION('',(-0.989713903077506,0.,0.143060791466736));
#11791=DIRECTION('center_axis',(-0.99990852097589,0.,0.0135258892428198));
#11792=DIRECTION('ref_axis',(0.0135258892428198,0.,0.99990852097589));
#11793=DIRECTION('',(0.0135258892428198,0.,0.99990852097589));
#11794=DIRECTION('',(0.,-1.,0.));
#11795=DIRECTION('',(0.0135258892428198,0.,0.99990852097589));
#11796=DIRECTION('center_axis',(-0.296124840698817,0.,-0.955149244213228));
#11797=DIRECTION('ref_axis',(-0.955149244213228,0.,0.296124840698817));
#11798=DIRECTION('',(-0.955149244213228,0.,0.296124840698817));
#11799=DIRECTION('',(-0.955149244213228,0.,0.296124840698817));
#11800=DIRECTION('center_axis',(-0.985482072581721,0.,0.169779517669346));
#11801=DIRECTION('ref_axis',(0.169779517669346,0.,0.985482072581721));
#11802=DIRECTION('',(0.169779517669346,0.,0.985482072581721));
#11803=DIRECTION('',(0.,-1.,0.));
#11804=DIRECTION('',(0.169779517669346,0.,0.985482072581721));
#11805=DIRECTION('center_axis',(-0.441897313570892,0.,-0.89706564099782));
#11806=DIRECTION('ref_axis',(-0.89706564099782,0.,0.441897313570891));
#11807=DIRECTION('',(-0.89706564099782,0.,0.441897313570891));
#11808=DIRECTION('',(-0.89706564099782,0.,0.441897313570891));
#11809=DIRECTION('center_axis',(-0.946789784933104,0.,0.321852610904939));
#11810=DIRECTION('ref_axis',(0.321852610904939,0.,0.946789784933104));
#11811=DIRECTION('',(0.321852610904939,0.,0.946789784933104));
#11812=DIRECTION('',(0.,-1.,0.));
#11813=DIRECTION('',(0.321852610904939,0.,0.946789784933104));
#11814=DIRECTION('center_axis',(-0.576788808009749,0.,-0.816893304510873));
#11815=DIRECTION('ref_axis',(-0.816893304510873,0.,0.576788808009749));
#11816=DIRECTION('',(-0.816893304510873,0.,0.576788808009749));
#11817=DIRECTION('',(-0.816893304510873,0.,0.576788808009749));
#11818=DIRECTION('center_axis',(-0.884784390564289,0.,0.466000624692478));
#11819=DIRECTION('ref_axis',(0.466000624692478,0.,0.884784390564289));
#11820=DIRECTION('',(0.466000624692478,0.,0.884784390564289));
#11821=DIRECTION('',(0.,-1.,0.));
#11822=DIRECTION('',(0.466000624692478,0.,0.884784390564289));
#11823=DIRECTION('center_axis',(-0.697477847743102,0.,-0.716606343753424));
#11824=DIRECTION('ref_axis',(-0.716606343753424,0.,0.697477847743102));
#11825=DIRECTION('',(-0.716606343753424,0.,0.697477847743102));
#11826=DIRECTION('',(-0.716606343753424,0.,0.697477847743102));
#11827=DIRECTION('center_axis',(-0.800992668068742,0.,0.598674156532682));
#11828=DIRECTION('ref_axis',(0.598674156532682,0.,0.800992668068742));
#11829=DIRECTION('',(0.598674156532682,0.,0.800992668068742));
#11830=DIRECTION('',(0.,-1.,0.));
#11831=DIRECTION('',(0.598674156532682,0.,0.800992668068742));
#11832=DIRECTION('center_axis',(-0.800992668068755,0.,-0.598674156532665));
#11833=DIRECTION('ref_axis',(-0.598674156532665,0.,0.800992668068755));
#11834=DIRECTION('',(-0.598674156532665,0.,0.800992668068755));
#11835=DIRECTION('',(-0.598674156532665,0.,0.800992668068755));
#11836=DIRECTION('center_axis',(-0.697477847743086,0.,0.71660634375344));
#11837=DIRECTION('ref_axis',(0.71660634375344,0.,0.697477847743086));
#11838=DIRECTION('',(0.71660634375344,0.,0.697477847743086));
#11839=DIRECTION('',(0.,-1.,0.));
#11840=DIRECTION('',(0.71660634375344,0.,0.697477847743086));
#11841=DIRECTION('center_axis',(-0.8847843905643,0.,-0.466000624692458));
#11842=DIRECTION('ref_axis',(-0.466000624692458,0.,0.8847843905643));
#11843=DIRECTION('',(-0.466000624692458,0.,0.8847843905643));
#11844=DIRECTION('',(-0.466000624692458,0.,0.8847843905643));
#11845=DIRECTION('center_axis',(-0.576788808009731,0.,0.816893304510885));
#11846=DIRECTION('ref_axis',(0.816893304510885,0.,0.576788808009731));
#11847=DIRECTION('',(0.816893304510885,0.,0.576788808009731));
#11848=DIRECTION('',(0.,-1.,0.));
#11849=DIRECTION('',(0.816893304510885,0.,0.576788808009731));
#11850=DIRECTION('center_axis',(-0.946789784933112,0.,-0.321852610904918));
#11851=DIRECTION('ref_axis',(-0.321852610904918,0.,0.946789784933112));
#11852=DIRECTION('',(-0.321852610904918,0.,0.946789784933111));
#11853=DIRECTION('',(-0.321852610904918,0.,0.946789784933111));
#11854=DIRECTION('center_axis',(-0.441897313570872,0.,0.897065640997829));
#11855=DIRECTION('ref_axis',(0.897065640997829,0.,0.441897313570872));
#11856=DIRECTION('',(0.897065640997829,0.,0.441897313570872));
#11857=DIRECTION('',(0.,-1.,0.));
#11858=DIRECTION('',(0.897065640997829,0.,0.441897313570872));
#11859=DIRECTION('center_axis',(-0.985482072581725,0.,-0.169779517669325));
#11860=DIRECTION('ref_axis',(-0.169779517669325,0.,0.985482072581725));
#11861=DIRECTION('',(-0.169779517669325,0.,0.985482072581724));
#11862=DIRECTION('',(-0.169779517669325,0.,0.985482072581724));
#11863=DIRECTION('center_axis',(-0.296124840698796,0.,0.955149244213234));
#11864=DIRECTION('ref_axis',(0.955149244213235,0.,0.296124840698796));
#11865=DIRECTION('',(0.955149244213234,0.,0.296124840698796));
#11866=DIRECTION('',(0.,-1.,0.));
#11867=DIRECTION('',(0.955149244213234,0.,0.296124840698796));
#11868=DIRECTION('center_axis',(-0.99990852097589,0.,-0.0135258892427971));
#11869=DIRECTION('ref_axis',(-0.0135258892427971,0.,0.99990852097589));
#11870=DIRECTION('',(-0.0135258892427971,0.,0.99990852097589));
#11871=DIRECTION('',(-0.0135258892427971,0.,0.99990852097589));
#11872=DIRECTION('center_axis',(-0.143060791466715,0.,0.989713903077509));
#11873=DIRECTION('ref_axis',(0.989713903077509,0.,0.143060791466715));
#11874=DIRECTION('',(0.989713903077509,0.,0.143060791466715));
#11875=DIRECTION('',(0.,-1.,0.));
#11876=DIRECTION('',(0.989713903077509,0.,0.143060791466715));
#11877=DIRECTION('center_axis',(-0.989713903077506,0.,0.14306079146674));
#11878=DIRECTION('ref_axis',(0.14306079146674,0.,0.989713903077506));
#11879=DIRECTION('',(0.14306079146674,0.,0.989713903077506));
#11880=DIRECTION('',(0.14306079146674,0.,0.989713903077506));
#11881=DIRECTION('center_axis',(0.0135258892428234,0.,0.99990852097589));
#11882=DIRECTION('ref_axis',(0.99990852097589,0.,-0.0135258892428234));
#11883=DIRECTION('',(0.999908520975889,0.,-0.0135258892428234));
#11884=DIRECTION('',(0.,-1.,0.));
#11885=DIRECTION('',(0.999908520975889,0.,-0.0135258892428234));
#11886=DIRECTION('center_axis',(-0.955149244213227,0.,0.296124840698821));
#11887=DIRECTION('ref_axis',(0.296124840698821,0.,0.955149244213227));
#11888=DIRECTION('',(0.296124840698821,0.,0.955149244213227));
#11889=DIRECTION('',(0.296124840698821,0.,0.955149244213227));
#11890=DIRECTION('center_axis',(0.169779517669349,0.,0.98548207258172));
#11891=DIRECTION('ref_axis',(0.98548207258172,0.,-0.169779517669349));
#11892=DIRECTION('',(0.98548207258172,0.,-0.169779517669349));
#11893=DIRECTION('',(0.,-1.,0.));
#11894=DIRECTION('',(0.98548207258172,0.,-0.169779517669349));
#11895=DIRECTION('center_axis',(-0.897065640997818,0.,0.441897313570894));
#11896=DIRECTION('ref_axis',(0.441897313570895,0.,0.897065640997818));
#11897=DIRECTION('',(0.441897313570894,0.,0.897065640997818));
#11898=DIRECTION('',(0.441897313570894,0.,0.897065640997818));
#11899=DIRECTION('center_axis',(0.321852610904942,0.,0.946789784933103));
#11900=DIRECTION('ref_axis',(0.946789784933103,0.,-0.321852610904942));
#11901=DIRECTION('',(0.946789784933103,0.,-0.321852610904942));
#11902=DIRECTION('',(0.,-1.,0.));
#11903=DIRECTION('',(0.946789784933103,0.,-0.321852610904942));
#11904=DIRECTION('center_axis',(-0.816893304510871,0.,0.576788808009752));
#11905=DIRECTION('ref_axis',(0.576788808009752,0.,0.816893304510871));
#11906=DIRECTION('',(0.576788808009752,0.,0.81689330451087));
#11907=DIRECTION('',(0.576788808009752,0.,0.81689330451087));
#11908=DIRECTION('center_axis',(0.466000624692481,0.,0.884784390564288));
#11909=DIRECTION('ref_axis',(0.884784390564287,0.,-0.466000624692481));
#11910=DIRECTION('',(0.884784390564287,0.,-0.466000624692481));
#11911=DIRECTION('',(0.,-1.,0.));
#11912=DIRECTION('',(0.884784390564287,0.,-0.466000624692481));
#11913=DIRECTION('center_axis',(-0.716606343753422,0.,0.697477847743104));
#11914=DIRECTION('ref_axis',(0.697477847743104,0.,0.716606343753422));
#11915=DIRECTION('',(0.697477847743104,0.,0.716606343753422));
#11916=DIRECTION('',(0.697477847743104,0.,0.716606343753422));
#11917=DIRECTION('center_axis',(0.,-1.,0.));
#11918=DIRECTION('ref_axis',(-1.07806057163162E-14,0.,1.));
#11919=DIRECTION('center_axis',(0.,1.,0.));
#11920=DIRECTION('ref_axis',(0.,0.,1.));
#11921=DIRECTION('center_axis',(0.,-1.,0.));
#11922=DIRECTION('ref_axis',(0.,0.,1.));
#11923=DIRECTION('center_axis',(0.,1.,0.));
#11924=DIRECTION('ref_axis',(0.,0.,1.));
#11925=DIRECTION('center_axis',(0.,1.,0.));
#11926=DIRECTION('ref_axis',(0.,0.,1.));
#11927=DIRECTION('center_axis',(0.,1.,0.));
#11928=DIRECTION('ref_axis',(0.,0.,1.));
#11929=DIRECTION('center_axis',(0.,-1.,0.));
#11930=DIRECTION('ref_axis',(0.,0.,1.));
#11931=DIRECTION('center_axis',(0.,-1.,0.));
#11932=DIRECTION('ref_axis',(0.,0.,-1.));
#11933=DIRECTION('center_axis',(0.,0.,-1.));
#11934=DIRECTION('ref_axis',(-1.,0.,0.));
#11935=DIRECTION('center_axis',(0.,0.,1.));
#11936=DIRECTION('ref_axis',(1.,0.,0.));
#11937=DIRECTION('',(0.,0.,1.));
#11938=DIRECTION('center_axis',(0.205494612278863,0.9481117507646,-0.242602704820958));
#11939=DIRECTION('ref_axis',(6.35112393104211E-18,0.247893179847911,0.968787371606841));
#11940=DIRECTION('center_axis',(-0.205494612278863,0.9481117507646,0.242602704820958));
#11941=DIRECTION('ref_axis',(-1.40903471563721E-18,-0.247893179847911,0.968787371606841));
#11942=DIRECTION('center_axis',(0.0116178137240244,-0.999746441108087,0.0192893726178047));
#11943=DIRECTION('ref_axis',(-0.389144902110929,-0.0222903798418516,-0.920906827061012));
#11944=DIRECTION('center_axis',(0.0116178138256172,0.999746441105387,0.0192893726965582));
#11945=DIRECTION('ref_axis',(0.398644886675284,-0.022322188382412,0.916833667702856));
#11946=DIRECTION('center_axis',(-0.205494612278863,0.9481117507646,-0.242602704820958));
#11947=DIRECTION('ref_axis',(-5.52985918827002E-18,0.247893179847911,0.968787371606841));
#11948=DIRECTION('center_axis',(-0.0116178136698366,0.999746441109573,0.0192893725734215));
#11949=DIRECTION('ref_axis',(-0.389144899953581,-0.0222903797723946,0.920906827974318));
#11950=DIRECTION('center_axis',(-0.0116178138280735,-0.999746441105327,
0.0192893726981682));
#11951=DIRECTION('ref_axis',(0.398644892757021,-0.0223221884045121,-0.916833665057941));
#11952=DIRECTION('center_axis',(0.205494612278853,0.948111750764605,0.242602704820948));
#11953=DIRECTION('ref_axis',(7.91791469497955E-18,-0.247893179847899,0.968787371606844));
#11954=DIRECTION('center_axis',(0.,-1.,0.));
#11955=DIRECTION('ref_axis',(0.,0.,-1.));
#11956=DIRECTION('center_axis',(0.,-1.,0.));
#11957=DIRECTION('ref_axis',(0.,0.,-1.));
#11958=DIRECTION('',(0.,-1.,0.));
#11959=DIRECTION('center_axis',(0.,-1.,0.));
#11960=DIRECTION('ref_axis',(0.,0.,-1.));
#11961=DIRECTION('center_axis',(0.589108138320174,0.,0.80805420694712));
#11962=DIRECTION('ref_axis',(0.80805420694712,0.,-0.589108138320173));
#11963=DIRECTION('center_axis',(0.6425724926294,0.,0.766224896303977));
#11964=DIRECTION('ref_axis',(0.766224896303977,0.,-0.6425724926294));
#11965=DIRECTION('center_axis',(0.,1.,0.));
#11966=DIRECTION('ref_axis',(0.,0.,1.));
#11967=DIRECTION('center_axis',(0.642572492629448,0.,-0.766224896303936));
#11968=DIRECTION('ref_axis',(-0.766224896303936,0.,-0.642572492629448));
#11969=DIRECTION('center_axis',(0.589108138320239,0.,-0.808054206947072));
#11970=DIRECTION('ref_axis',(-0.808054206947072,0.,-0.589108138320239));
#11971=DIRECTION('center_axis',(0.589108138321627,8.53137857429337E-12,
0.80805420694606));
#11972=DIRECTION('ref_axis',(0.80805420694606,-3.6224271017081E-27,-0.589108138321627));
#11973=DIRECTION('center_axis',(0.642572492629448,0.,0.766224896303936));
#11974=DIRECTION('ref_axis',(0.766224896303936,0.,-0.642572492629448));
#11975=DIRECTION('center_axis',(0.,1.,0.));
#11976=DIRECTION('ref_axis',(0.,0.,1.));
#11977=DIRECTION('center_axis',(0.642572492629365,0.,-0.766224896304006));
#11978=DIRECTION('ref_axis',(-0.766224896304006,0.,-0.642572492629365));
#11979=DIRECTION('center_axis',(0.589108138320241,7.59621770439584E-16,
-0.808054206947071));
#11980=DIRECTION('ref_axis',(-0.808054206947071,-1.44772128095523E-31,-0.589108138320241));
#11981=DIRECTION('center_axis',(0.,0.,1.));
#11982=DIRECTION('ref_axis',(1.,0.,0.));
#11983=DIRECTION('center_axis',(0.,0.,1.));
#11984=DIRECTION('ref_axis',(1.,0.,0.));
#11985=DIRECTION('center_axis',(0.,0.,1.));
#11986=DIRECTION('ref_axis',(1.,0.,0.));
#11987=DIRECTION('center_axis',(0.,0.,-1.));
#11988=DIRECTION('ref_axis',(1.,0.,0.));
#11989=DIRECTION('',(0.,0.,-1.));
#11990=DIRECTION('center_axis',(0.,0.,1.));
#11991=DIRECTION('ref_axis',(1.,0.,0.));
#11992=DIRECTION('center_axis',(1.22464679914735E-16,-1.,0.));
#11993=DIRECTION('ref_axis',(-1.,-1.22464679914735E-16,0.));
#11994=DIRECTION('center_axis',(0.,0.,1.));
#11995=DIRECTION('ref_axis',(1.,0.,0.));
#11996=DIRECTION('center_axis',(0.,0.,1.));
#11997=DIRECTION('ref_axis',(1.,0.,0.));
#11998=DIRECTION('',(0.0195766671631255,2.39745027792948E-18,-0.999808358688196));
#11999=DIRECTION('center_axis',(0.,0.,1.));
#12000=DIRECTION('ref_axis',(1.,0.,0.));
#12001=DIRECTION('center_axis',(0.,0.,1.));
#12002=DIRECTION('ref_axis',(1.,0.,0.));
#12003=DIRECTION('center_axis',(-1.22464679914735E-16,1.,0.));
#12004=DIRECTION('ref_axis',(-1.,-1.22464679914735E-16,0.));
#12005=DIRECTION('center_axis',(0.,1.,0.));
#12006=DIRECTION('ref_axis',(0.,0.,1.));
#12007=DIRECTION('',(0.,1.,0.));
#12008=DIRECTION('center_axis',(0.,0.,1.));
#12009=DIRECTION('ref_axis',(1.,0.,0.));
#12010=DIRECTION('',(-1.,1.22163625068789E-16,0.));
#12011=DIRECTION('',(0.,-1.,0.));
#12012=DIRECTION('',(1.,-1.22163625068789E-16,0.));
#12013=DIRECTION('',(0.,1.,0.));
#12014=DIRECTION('center_axis',(-0.981627183447664,0.,-0.190808995376545));
#12015=DIRECTION('ref_axis',(0.190808995376545,0.,-0.981627183447664));
#12016=DIRECTION('',(0.190808995376545,-2.33099185709326E-17,-0.981627183447664));
#12017=DIRECTION('',(0.,-1.,0.));
#12018=DIRECTION('',(0.190808995376545,-2.33099185709326E-17,-0.981627183447664));
#12019=DIRECTION('center_axis',(1.22163625068789E-16,1.,0.));
#12020=DIRECTION('ref_axis',(-1.,1.22163625068789E-16,0.));
#12021=DIRECTION('',(1.,-1.22163625068789E-16,0.));
#12022=DIRECTION('',(-0.190808995376545,2.33099185709326E-17,-0.981627183447664));
#12023=DIRECTION('center_axis',(0.981627183447664,0.,-0.190808995376545));
#12024=DIRECTION('ref_axis',(-0.190808995376545,0.,-0.981627183447664));
#12025=DIRECTION('',(0.,1.,0.));
#12026=DIRECTION('',(-0.190808995376545,2.33099185709326E-17,-0.981627183447664));
#12027=DIRECTION('center_axis',(-1.22163625068789E-16,-1.,0.));
#12028=DIRECTION('ref_axis',(1.,-1.22163625068789E-16,0.));
#12029=DIRECTION('',(-1.,1.22163625068789E-16,0.));
#12030=DIRECTION('center_axis',(0.,0.,-1.));
#12031=DIRECTION('ref_axis',(-1.,0.,0.));
#13916=CARTESIAN_POINT('',(0.,0.,0.));
#13917=CARTESIAN_POINT('Origin',(0.,10.75,0.));
#13918=CARTESIAN_POINT('',(-4.19956186204517,10.7500000000001,17.503247703408));
#13919=CARTESIAN_POINT('',(-4.19956186204517,-5.74999999999987,17.503247703408));
#13920=CARTESIAN_POINT('',(-4.19956186204517,333.257395605323,17.503247703408));
#13921=CARTESIAN_POINT('',(-4.20447115411988,-5.75,17.5020690866587));
#13922=CARTESIAN_POINT('Origin',(0.,-5.75,0.));
#13923=CARTESIAN_POINT('',(-4.20447115411988,10.7500000000001,17.5020690866587));
#13924=CARTESIAN_POINT('',(-4.20447115411988,333.257395605323,17.5020690866587));
#13925=CARTESIAN_POINT('Origin',(0.,10.75,0.));
#13926=CARTESIAN_POINT('Origin',(0.,10.75,0.));
#13927=CARTESIAN_POINT('',(-6.8859694776993,10.7500000000001,16.6307974659123));
#13928=CARTESIAN_POINT('',(-6.88596947769931,-5.74999999999998,16.6307974659123));
#13929=CARTESIAN_POINT('',(-6.8859694776993,333.257395605323,16.6307974659123));
#13930=CARTESIAN_POINT('',(-6.8906339519614,-5.75,16.6288653774116));
#13931=CARTESIAN_POINT('Origin',(0.,-5.75,0.));
#13932=CARTESIAN_POINT('',(-6.8906339519614,10.7500000000001,16.6288653774116));
#13933=CARTESIAN_POINT('',(-6.8906339519614,333.257395605323,16.6288653774116));
#13934=CARTESIAN_POINT('Origin',(0.,10.75,0.));
#13935=CARTESIAN_POINT('Origin',(0.,10.75,0.));
#13936=CARTESIAN_POINT('',(-9.40282167159,10.7500000000001,15.3488418003535));
#13937=CARTESIAN_POINT('',(-9.40282167159,-5.74999999999998,15.3488418003535));
#13938=CARTESIAN_POINT('',(-9.40282167159,333.257395605323,15.3488418003535));
#13939=CARTESIAN_POINT('',(-9.40712647320266,-5.75,15.3462038145324));
#13940=CARTESIAN_POINT('Origin',(0.,-5.75,0.));
#13941=CARTESIAN_POINT('',(-9.40712647320266,10.7500000000001,15.3462038145324));
#13942=CARTESIAN_POINT('',(-9.40712647320266,333.257395605323,15.3462038145324));
#13943=CARTESIAN_POINT('Origin',(0.,10.75,0.));
#13944=CARTESIAN_POINT('Origin',(0.,10.75,0.));
#13945=CARTESIAN_POINT('',(-11.6881451897502,10.7500000000001,13.6889467097845));
#13946=CARTESIAN_POINT('',(-11.6881451897502,-5.74999999999998,13.6889467097845));
#13947=CARTESIAN_POINT('',(-11.6881451897502,333.257395605323,13.6889467097845));
#13948=CARTESIAN_POINT('',(-11.6919843202109,-5.75,13.685667782609));
#13949=CARTESIAN_POINT('Origin',(0.,-5.75,0.));
#13950=CARTESIAN_POINT('',(-11.6919843202109,10.7500000000001,13.685667782609));
#13951=CARTESIAN_POINT('',(-11.6919843202109,333.257395605323,13.685667782609));
#13952=CARTESIAN_POINT('Origin',(0.,10.75,0.));
#13953=CARTESIAN_POINT('Origin',(0.,10.75,0.));
#13954=CARTESIAN_POINT('',(-13.6856677826088,10.7500000000001,11.6919843202112));
#13955=CARTESIAN_POINT('',(-13.6856677826088,-5.74999999999998,11.6919843202112));
#13956=CARTESIAN_POINT('',(-13.6856677826088,333.257395605323,11.6919843202112));
#13957=CARTESIAN_POINT('',(-13.6889467097842,-5.75,11.6881451897505));
#13958=CARTESIAN_POINT('Origin',(0.,-5.75,0.));
#13959=CARTESIAN_POINT('',(-13.6889467097842,10.7500000000001,11.6881451897505));
#13960=CARTESIAN_POINT('',(-13.6889467097842,333.257395605323,11.6881451897505));
#13961=CARTESIAN_POINT('Origin',(0.,10.75,0.));
#13962=CARTESIAN_POINT('Origin',(0.,10.75,0.));
#13963=CARTESIAN_POINT('',(-15.3462038145322,10.7500000000001,9.40712647320306));
#13964=CARTESIAN_POINT('',(-15.3462038145322,-5.74999999999998,9.40712647320306));
#13965=CARTESIAN_POINT('',(-15.3462038145322,333.257395605323,9.40712647320306));
#13966=CARTESIAN_POINT('',(-15.3488418003532,-5.75,9.40282167159038));
#13967=CARTESIAN_POINT('Origin',(0.,-5.75,0.));
#13968=CARTESIAN_POINT('',(-15.3488418003532,10.7500000000001,9.40282167159038));
#13969=CARTESIAN_POINT('',(-15.3488418003532,333.257395605323,9.40282167159038));
#13970=CARTESIAN_POINT('Origin',(0.,10.75,0.));
#13971=CARTESIAN_POINT('Origin',(0.,10.75,0.));
#13972=CARTESIAN_POINT('',(-16.6288653774114,10.7500000000001,6.89063395196181));
#13973=CARTESIAN_POINT('',(-16.6288653774114,-5.74999999999998,6.89063395196181));
#13974=CARTESIAN_POINT('',(-16.6288653774114,333.257395605323,6.89063395196181));
#13975=CARTESIAN_POINT('',(-16.6307974659121,-5.75,6.88596947769972));
#13976=CARTESIAN_POINT('Origin',(0.,-5.75,0.));
#13977=CARTESIAN_POINT('',(-16.6307974659121,10.7500000000001,6.88596947769972));
#13978=CARTESIAN_POINT('',(-16.6307974659121,333.257395605323,6.88596947769972));
#13979=CARTESIAN_POINT('Origin',(0.,10.75,0.));
#13980=CARTESIAN_POINT('Origin',(0.,10.75,0.));
#13981=CARTESIAN_POINT('',(-17.5020690866586,10.7500000000001,4.20447115412031));
#13982=CARTESIAN_POINT('',(-17.5020690866586,-5.74999999999998,4.20447115412031));
#13983=CARTESIAN_POINT('',(-17.5020690866586,333.257395605323,4.20447115412031));
#13984=CARTESIAN_POINT('',(-17.5032477034078,-5.75,4.19956186204562));
#13985=CARTESIAN_POINT('Origin',(0.,-5.75,0.));
#13986=CARTESIAN_POINT('',(-17.5032477034078,10.7500000000001,4.19956186204562));
#13987=CARTESIAN_POINT('',(-17.5032477034078,333.257395605323,4.19956186204562));
#13988=CARTESIAN_POINT('Origin',(0.,10.75,0.));
#13989=CARTESIAN_POINT('Origin',(0.,10.75,0.));
#13990=CARTESIAN_POINT('',(-17.9443137689552,10.7500000000001,1.41478032262462));
#13991=CARTESIAN_POINT('',(-17.9443137689552,-5.74999999999998,1.41478032262462));
#13992=CARTESIAN_POINT('',(-17.9443137689552,333.257395605323,1.41478032262462));
#13993=CARTESIAN_POINT('',(-17.944709892497,-5.75,1.40974709580119));
#13994=CARTESIAN_POINT('Origin',(0.,-5.75,0.));
#13995=CARTESIAN_POINT('',(-17.944709892497,10.7500000000001,1.40974709580119));
#13996=CARTESIAN_POINT('',(-17.944709892497,333.257395605323,1.40974709580119));
#13997=CARTESIAN_POINT('Origin',(0.,10.75,0.));
#13998=CARTESIAN_POINT('Origin',(0.,10.75,0.));
#13999=CARTESIAN_POINT('',(-17.944709892497,10.7500000000001,-1.40974709580081));
#14000=CARTESIAN_POINT('',(-17.944709892497,-5.74999999999998,-1.40974709580081));
#14001=CARTESIAN_POINT('',(-17.944709892497,333.257395605323,-1.40974709580081));
#14002=CARTESIAN_POINT('',(-17.9443137689552,-5.75,-1.41478032262422));
#14003=CARTESIAN_POINT('Origin',(0.,-5.75,0.));
#14004=CARTESIAN_POINT('',(-17.9443137689552,10.7500000000001,-1.41478032262422));
#14005=CARTESIAN_POINT('',(-17.9443137689552,333.257395605323,-1.41478032262422));
#14006=CARTESIAN_POINT('Origin',(0.,10.75,0.));
#14007=CARTESIAN_POINT('Origin',(0.,10.75,0.));
#14008=CARTESIAN_POINT('',(-17.5032477034079,10.7500000000001,-4.19956186204523));
#14009=CARTESIAN_POINT('',(-17.5032477034079,-5.74999999999998,-4.19956186204523));
#14010=CARTESIAN_POINT('',(-17.5032477034079,333.257395605323,-4.19956186204523));
#14011=CARTESIAN_POINT('',(-17.5020690866587,-5.75,-4.20447115411994));
#14012=CARTESIAN_POINT('Origin',(0.,-5.75,0.));
#14013=CARTESIAN_POINT('',(-17.5020690866587,10.7500000000001,-4.20447115411994));
#14014=CARTESIAN_POINT('',(-17.5020690866587,333.257395605323,-4.20447115411994));
#14015=CARTESIAN_POINT('Origin',(0.,10.75,0.));
#14016=CARTESIAN_POINT('Origin',(0.,10.75,0.));
#14017=CARTESIAN_POINT('',(-16.6307974659122,10.7500000000001,-6.88596947769936));
#14018=CARTESIAN_POINT('',(-16.6307974659122,-5.74999999999998,-6.88596947769936));
#14019=CARTESIAN_POINT('',(-16.6307974659122,333.257395605323,-6.88596947769936));
#14020=CARTESIAN_POINT('',(-16.6288653774115,-5.75,-6.89063395196146));
#14021=CARTESIAN_POINT('Origin',(0.,-5.75,0.));
#14022=CARTESIAN_POINT('',(-16.6288653774115,10.7500000000001,-6.89063395196146));
#14023=CARTESIAN_POINT('',(-16.6288653774115,333.257395605323,-6.89063395196146));
#14024=CARTESIAN_POINT('Origin',(0.,10.75,0.));
#14025=CARTESIAN_POINT('Origin',(0.,10.75,0.));
#14026=CARTESIAN_POINT('',(-15.3488418003534,10.7500000000001,-9.40282167159006));
#14027=CARTESIAN_POINT('',(-15.3488418003534,-5.74999999999998,-9.40282167159006));
#14028=CARTESIAN_POINT('',(-15.3488418003534,333.257395605323,-9.40282167159006));
#14029=CARTESIAN_POINT('',(-15.3462038145324,-5.75,-9.40712647320272));
#14030=CARTESIAN_POINT('Origin',(0.,-5.75,0.));
#14031=CARTESIAN_POINT('',(-15.3462038145324,10.7500000000001,-9.40712647320272));
#14032=CARTESIAN_POINT('',(-15.3462038145324,333.257395605323,-9.40712647320272));
#14033=CARTESIAN_POINT('Origin',(0.,10.75,0.));
#14034=CARTESIAN_POINT('Origin',(0.,10.75,0.));
#14035=CARTESIAN_POINT('',(-13.6889467097845,10.7500000000001,-11.6881451897502));
#14036=CARTESIAN_POINT('',(-13.6889467097845,-5.74999999999998,-11.6881451897502));
#14037=CARTESIAN_POINT('',(-13.6889467097845,333.257395605323,-11.6881451897502));
#14038=CARTESIAN_POINT('',(-13.685667782609,-5.74999999999998,-11.6919843202109));
#14039=CARTESIAN_POINT('Origin',(0.,-5.75,0.));
#14040=CARTESIAN_POINT('',(-13.685667782609,10.7500000000001,-11.6919843202109));
#14041=CARTESIAN_POINT('',(-13.685667782609,333.257395605323,-11.6919843202109));
#14042=CARTESIAN_POINT('Origin',(0.,10.75,0.));
#14043=CARTESIAN_POINT('Origin',(0.,10.75,0.));
#14044=CARTESIAN_POINT('',(-11.6919843202112,10.7500000000001,-13.6856677826088));
#14045=CARTESIAN_POINT('',(-11.6919843202112,-5.75,-13.6856677826088));
#14046=CARTESIAN_POINT('',(-11.6919843202112,333.257395605323,-13.6856677826088));
#14047=CARTESIAN_POINT('',(-11.6881451897505,-5.74999999999998,-13.6889467097843));
#14048=CARTESIAN_POINT('Origin',(0.,-5.75,0.));
#14049=CARTESIAN_POINT('',(-11.6881451897505,10.7500000000001,-13.6889467097843));
#14050=CARTESIAN_POINT('',(-11.6881451897505,333.257395605323,-13.6889467097843));
#14051=CARTESIAN_POINT('Origin',(0.,10.75,0.));
#14052=CARTESIAN_POINT('Origin',(0.,10.75,0.));
#14053=CARTESIAN_POINT('',(-9.40712647320301,10.7500000000001,-15.3462038145322));
#14054=CARTESIAN_POINT('',(-9.40712647320301,-5.75,-15.3462038145322));
#14055=CARTESIAN_POINT('',(-9.40712647320301,333.257395605323,-15.3462038145322));
#14056=CARTESIAN_POINT('',(-9.40282167159034,-5.74999999999998,-15.3488418003532));
#14057=CARTESIAN_POINT('Origin',(0.,-5.75,0.));
#14058=CARTESIAN_POINT('',(-9.40282167159034,10.7500000000001,-15.3488418003532));
#14059=CARTESIAN_POINT('',(-9.40282167159034,333.257395605323,-15.3488418003532));
#14060=CARTESIAN_POINT('Origin',(0.,10.75,0.));
#14061=CARTESIAN_POINT('Origin',(0.,10.75,0.));
#14062=CARTESIAN_POINT('',(-6.89063395196176,10.7500000000001,-16.6288653774114));
#14063=CARTESIAN_POINT('',(-6.89063395196176,-5.75,-16.6288653774114));
#14064=CARTESIAN_POINT('',(-6.89063395196176,333.257395605323,-16.6288653774114));
#14065=CARTESIAN_POINT('',(-6.88596947769966,-5.74999999999998,-16.6307974659121));
#14066=CARTESIAN_POINT('Origin',(0.,-5.75,0.));
#14067=CARTESIAN_POINT('',(-6.88596947769966,10.7500000000001,-16.6307974659121));
#14068=CARTESIAN_POINT('',(-6.88596947769966,333.257395605323,-16.6307974659121));
#14069=CARTESIAN_POINT('Origin',(0.,10.75,0.));
#14070=CARTESIAN_POINT('Origin',(0.,10.75,0.));
#14071=CARTESIAN_POINT('',(-4.20447115412025,10.7500000000001,-17.5020690866586));
#14072=CARTESIAN_POINT('',(-4.20447115412025,-5.75,-17.5020690866586));
#14073=CARTESIAN_POINT('',(-4.20447115412025,333.257395605323,-17.5020690866586));
#14074=CARTESIAN_POINT('',(-4.19956186204555,-5.74999999999998,-17.5032477034079));
#14075=CARTESIAN_POINT('Origin',(0.,-5.75,0.));
#14076=CARTESIAN_POINT('',(-4.19956186204555,10.7500000000001,-17.5032477034079));
#14077=CARTESIAN_POINT('',(-4.19956186204555,333.257395605323,-17.5032477034079));
#14078=CARTESIAN_POINT('Origin',(0.,10.75,0.));
#14079=CARTESIAN_POINT('Origin',(0.,10.75,0.));
#14080=CARTESIAN_POINT('',(-1.41478032262455,10.7500000000001,-17.9443137689552));
#14081=CARTESIAN_POINT('',(-1.41478032262455,-5.75,-17.9443137689552));
#14082=CARTESIAN_POINT('',(-1.41478032262455,333.257395605323,-17.9443137689552));
#14083=CARTESIAN_POINT('',(-1.409747095801,-5.74999999999998,-17.944709892497));
#14084=CARTESIAN_POINT('Origin',(0.,-5.75,0.));
#14085=CARTESIAN_POINT('',(-1.409747095801,10.7500000000001,-17.944709892497));
#14086=CARTESIAN_POINT('',(-1.409747095801,333.257395605323,-17.944709892497));
#14087=CARTESIAN_POINT('Origin',(0.,10.75,0.));
#14088=CARTESIAN_POINT('Origin',(0.,10.75,0.));
#14089=CARTESIAN_POINT('',(1.40974709580099,10.7500000000001,-17.944709892497));
#14090=CARTESIAN_POINT('',(1.40974709580099,-5.75,-17.944709892497));
#14091=CARTESIAN_POINT('',(1.40974709580099,333.257395605323,-17.944709892497));
#14092=CARTESIAN_POINT('',(1.41478032262429,-5.74999999999998,-17.9443137689552));
#14093=CARTESIAN_POINT('Origin',(0.,-5.75,0.));
#14094=CARTESIAN_POINT('',(1.41478032262429,10.7500000000001,-17.9443137689552));
#14095=CARTESIAN_POINT('',(1.41478032262429,333.257395605323,-17.9443137689552));
#14096=CARTESIAN_POINT('Origin',(0.,10.75,0.));
#14097=CARTESIAN_POINT('Origin',(0.,10.75,0.));
#14098=CARTESIAN_POINT('',(4.1995618620453,10.7500000000001,-17.5032477034079));
#14099=CARTESIAN_POINT('',(4.19956186204529,-5.75,-17.5032477034079));
#14100=CARTESIAN_POINT('',(4.1995618620453,333.257395605323,-17.5032477034079));
#14101=CARTESIAN_POINT('',(4.20447115411999,-5.74999999999998,-17.5020690866587));
#14102=CARTESIAN_POINT('Origin',(0.,-5.75,0.));
#14103=CARTESIAN_POINT('',(4.20447115411999,10.7500000000001,-17.5020690866587));
#14104=CARTESIAN_POINT('',(4.20447115411999,333.257395605323,-17.5020690866587));
#14105=CARTESIAN_POINT('Origin',(0.,10.75,0.));
#14106=CARTESIAN_POINT('Origin',(0.,10.75,0.));
#14107=CARTESIAN_POINT('',(6.88596947769941,10.7500000000001,-16.6307974659122));
#14108=CARTESIAN_POINT('',(6.88596947769941,-5.75,-16.6307974659122));
#14109=CARTESIAN_POINT('',(6.88596947769941,333.257395605323,-16.6307974659122));
#14110=CARTESIAN_POINT('',(6.89063395196152,-5.74999999999998,-16.6288653774115));
#14111=CARTESIAN_POINT('Origin',(0.,-5.75,0.));
#14112=CARTESIAN_POINT('',(6.89063395196152,10.7500000000001,-16.6288653774115));
#14113=CARTESIAN_POINT('',(6.89063395196152,333.257395605323,-16.6288653774115));
#14114=CARTESIAN_POINT('Origin',(0.,10.75,0.));
#14115=CARTESIAN_POINT('Origin',(0.,10.75,0.));
#14116=CARTESIAN_POINT('',(9.40282167159011,10.7500000000001,-15.3488418003534));
#14117=CARTESIAN_POINT('',(9.40282167159011,-5.75,-15.3488418003534));
#14118=CARTESIAN_POINT('',(9.40282167159011,333.257395605323,-15.3488418003534));
#14119=CARTESIAN_POINT('',(9.40712647320278,-5.74999999999998,-15.3462038145324));
#14120=CARTESIAN_POINT('Origin',(0.,-5.75,0.));
#14121=CARTESIAN_POINT('',(9.40712647320278,10.7500000000001,-15.3462038145324));
#14122=CARTESIAN_POINT('',(9.40712647320278,333.257395605323,-15.3462038145324));
#14123=CARTESIAN_POINT('Origin',(0.,10.75,0.));
#14124=CARTESIAN_POINT('Origin',(0.,10.75,0.));
#14125=CARTESIAN_POINT('',(11.6881451897503,10.7500000000001,-13.6889467097844));
#14126=CARTESIAN_POINT('',(11.6881451897503,-5.75,-13.6889467097844));
#14127=CARTESIAN_POINT('',(11.6881451897503,333.257395605323,-13.6889467097844));
#14128=CARTESIAN_POINT('',(11.691984320211,-5.74999999999998,-13.685667782609));
#14129=CARTESIAN_POINT('Origin',(0.,-5.75,0.));
#14130=CARTESIAN_POINT('',(11.691984320211,10.7500000000001,-13.685667782609));
#14131=CARTESIAN_POINT('',(11.691984320211,333.257395605323,-13.685667782609));
#14132=CARTESIAN_POINT('Origin',(0.,10.75,0.));
#14133=CARTESIAN_POINT('Origin',(0.,10.75,0.));
#14134=CARTESIAN_POINT('',(13.6856677826088,10.7500000000001,-11.6919843202111));
#14135=CARTESIAN_POINT('',(13.6856677826088,-5.75,-11.6919843202111));
#14136=CARTESIAN_POINT('',(13.6856677826088,333.257395605323,-11.6919843202111));
#14137=CARTESIAN_POINT('',(13.6889467097843,-5.74999999999998,-11.6881451897504));
#14138=CARTESIAN_POINT('Origin',(0.,-5.75,0.));
#14139=CARTESIAN_POINT('',(13.6889467097843,10.7500000000001,-11.6881451897504));
#14140=CARTESIAN_POINT('',(13.6889467097843,333.257395605323,-11.6881451897504));
#14141=CARTESIAN_POINT('Origin',(0.,10.75,0.));
#14142=CARTESIAN_POINT('Origin',(0.,10.75,0.));
#14143=CARTESIAN_POINT('',(15.3462038145323,10.7500000000001,-9.40712647320295));
#14144=CARTESIAN_POINT('',(15.3462038145323,-5.75,-9.40712647320295));
#14145=CARTESIAN_POINT('',(15.3462038145323,333.257395605323,-9.40712647320295));
#14146=CARTESIAN_POINT('',(15.3488418003533,-5.74999999999998,-9.40282167159028));
#14147=CARTESIAN_POINT('Origin',(0.,-5.75,0.));
#14148=CARTESIAN_POINT('',(15.3488418003533,10.7500000000001,-9.40282167159028));
#14149=CARTESIAN_POINT('',(15.3488418003533,333.257395605323,-9.40282167159028));
#14150=CARTESIAN_POINT('Origin',(0.,10.75,0.));
#14151=CARTESIAN_POINT('Origin',(0.,10.75,0.));
#14152=CARTESIAN_POINT('',(16.6288653774114,10.7500000000001,-6.8906339519617));
#14153=CARTESIAN_POINT('',(16.6288653774114,-5.75,-6.8906339519617));
#14154=CARTESIAN_POINT('',(16.6288653774114,333.257395605323,-6.8906339519617));
#14155=CARTESIAN_POINT('',(16.6307974659121,-5.74999999999998,-6.8859694776996));
#14156=CARTESIAN_POINT('Origin',(0.,-5.75,0.));
#14157=CARTESIAN_POINT('',(16.6307974659121,10.7500000000001,-6.8859694776996));
#14158=CARTESIAN_POINT('',(16.6307974659121,333.257395605323,-6.8859694776996));
#14159=CARTESIAN_POINT('Origin',(0.,10.75,0.));
#14160=CARTESIAN_POINT('Origin',(0.,10.75,0.));
#14161=CARTESIAN_POINT('',(17.5020690866586,10.7500000000001,-4.20447115412019));
#14162=CARTESIAN_POINT('',(17.5020690866586,-5.75,-4.20447115412019));
#14163=CARTESIAN_POINT('',(17.5020690866586,333.257395605323,-4.20447115412019));
#14164=CARTESIAN_POINT('',(17.5032477034079,-5.74999999999998,-4.19956186204549));
#14165=CARTESIAN_POINT('Origin',(0.,-5.75,0.));
#14166=CARTESIAN_POINT('',(17.5032477034079,10.7500000000001,-4.19956186204549));
#14167=CARTESIAN_POINT('',(17.5032477034079,333.257395605323,-4.19956186204549));
#14168=CARTESIAN_POINT('Origin',(0.,10.75,0.));
#14169=CARTESIAN_POINT('Origin',(0.,10.75,0.));
#14170=CARTESIAN_POINT('',(17.9443137689552,10.7500000000001,-1.41478032262448));
#14171=CARTESIAN_POINT('',(17.9443137689552,-5.75,-1.41478032262448));
#14172=CARTESIAN_POINT('',(17.9443137689552,333.257395605323,-1.41478032262448));
#14173=CARTESIAN_POINT('',(17.944709892497,-5.74999999999998,-1.40974709580106));
#14174=CARTESIAN_POINT('Origin',(0.,-5.75,0.));
#14175=CARTESIAN_POINT('',(17.944709892497,10.7500000000001,-1.40974709580106));
#14176=CARTESIAN_POINT('',(17.944709892497,333.257395605323,-1.40974709580106));
#14177=CARTESIAN_POINT('Origin',(0.,10.75,0.));
#14178=CARTESIAN_POINT('Origin',(0.,10.75,0.));
#14179=CARTESIAN_POINT('',(17.944709892497,10.7500000000001,1.40974709580093));
#14180=CARTESIAN_POINT('',(17.944709892497,-5.75,1.40974709580093));
#14181=CARTESIAN_POINT('',(17.944709892497,333.257395605323,1.40974709580093));
#14182=CARTESIAN_POINT('',(17.9443137689552,-5.74999999999998,1.41478032262435));
#14183=CARTESIAN_POINT('Origin',(0.,-5.75,0.));
#14184=CARTESIAN_POINT('',(17.9443137689552,10.7500000000001,1.41478032262435));
#14185=CARTESIAN_POINT('',(17.9443137689552,333.257395605323,1.41478032262435));
#14186=CARTESIAN_POINT('Origin',(0.,10.75,0.));
#14187=CARTESIAN_POINT('Origin',(0.,10.75,0.));
#14188=CARTESIAN_POINT('',(17.5032477034079,10.7500000000001,4.19956186204535));
#14189=CARTESIAN_POINT('',(17.5032477034079,-5.75,4.19956186204535));
#14190=CARTESIAN_POINT('',(17.5032477034079,333.257395605323,4.19956186204535));
#14191=CARTESIAN_POINT('',(17.5020690866587,-5.74999999999998,4.20447115412006));
#14192=CARTESIAN_POINT('Origin',(0.,-5.75,0.));
#14193=CARTESIAN_POINT('',(17.5020690866587,10.7500000000001,4.20447115412006));
#14194=CARTESIAN_POINT('',(17.5020690866587,333.257395605323,4.20447115412006));
#14195=CARTESIAN_POINT('Origin',(0.,10.75,0.));
#14196=CARTESIAN_POINT('Origin',(0.,10.75,0.));
#14197=CARTESIAN_POINT('',(16.6307974659122,10.7500000000001,6.88596947769947));
#14198=CARTESIAN_POINT('',(16.6307974659122,-5.75,6.88596947769947));
#14199=CARTESIAN_POINT('',(16.6307974659122,333.257395605323,6.88596947769947));
#14200=CARTESIAN_POINT('',(16.6288653774115,-5.74999999999998,6.89063395196158));
#14201=CARTESIAN_POINT('Origin',(0.,-5.75,0.));
#14202=CARTESIAN_POINT('',(16.6288653774115,10.7500000000001,6.89063395196158));
#14203=CARTESIAN_POINT('',(16.6288653774115,333.257395605323,6.89063395196158));
#14204=CARTESIAN_POINT('Origin',(0.,10.75,0.));
#14205=CARTESIAN_POINT('Origin',(0.,10.75,0.));
#14206=CARTESIAN_POINT('',(15.3488418003534,10.7500000000001,9.40282167159017));
#14207=CARTESIAN_POINT('',(15.3488418003534,-5.75,9.40282167159017));
#14208=CARTESIAN_POINT('',(15.3488418003534,333.257395605323,9.40282167159017));
#14209=CARTESIAN_POINT('',(15.3462038145323,-5.74999999999998,9.40712647320283));
#14210=CARTESIAN_POINT('Origin',(0.,-5.75,0.));
#14211=CARTESIAN_POINT('',(15.3462038145323,10.7500000000001,9.40712647320283));
#14212=CARTESIAN_POINT('',(15.3462038145323,333.257395605323,9.40712647320283));
#14213=CARTESIAN_POINT('Origin',(0.,10.75,0.));
#14214=CARTESIAN_POINT('Origin',(0.,10.75,0.));
#14215=CARTESIAN_POINT('',(13.6889467097844,10.7500000000001,11.6881451897503));
#14216=CARTESIAN_POINT('',(13.6889467097844,-5.75,11.6881451897503));
#14217=CARTESIAN_POINT('',(13.6889467097844,333.257395605323,11.6881451897503));
#14218=CARTESIAN_POINT('',(13.6856677826089,-5.74999999999998,11.691984320211));
#14219=CARTESIAN_POINT('Origin',(0.,-5.75,0.));
#14220=CARTESIAN_POINT('',(13.6856677826089,10.7500000000001,11.691984320211));
#14221=CARTESIAN_POINT('',(13.6856677826089,333.257395605323,11.691984320211));
#14222=CARTESIAN_POINT('Origin',(0.,10.75,0.));
#14223=CARTESIAN_POINT('Origin',(0.,10.75,0.));
#14224=CARTESIAN_POINT('',(11.6919843202111,10.7500000000001,13.6856677826089));
#14225=CARTESIAN_POINT('',(11.6919843202111,-5.75,13.6856677826089));
#14226=CARTESIAN_POINT('',(11.6919843202111,333.257395605323,13.6856677826089));
#14227=CARTESIAN_POINT('',(11.6881451897504,-5.74999999999998,13.6889467097843));
#14228=CARTESIAN_POINT('Origin',(0.,-5.75,0.));
#14229=CARTESIAN_POINT('',(11.6881451897504,10.7500000000001,13.6889467097843));
#14230=CARTESIAN_POINT('',(11.6881451897504,333.257395605323,13.6889467097843));
#14231=CARTESIAN_POINT('Origin',(0.,10.75,0.));
#14232=CARTESIAN_POINT('Origin',(0.,10.75,0.));
#14233=CARTESIAN_POINT('',(9.4071264732029,10.7500000000001,15.3462038145323));
#14234=CARTESIAN_POINT('',(9.40712647320289,-5.75,15.3462038145323));
#14235=CARTESIAN_POINT('',(9.4071264732029,333.257395605323,15.3462038145323));
#14236=CARTESIAN_POINT('',(9.40282167159022,-5.74999999999998,15.3488418003533));
#14237=CARTESIAN_POINT('Origin',(0.,-5.75,0.));
#14238=CARTESIAN_POINT('',(9.40282167159023,10.7500000000001,15.3488418003533));
#14239=CARTESIAN_POINT('',(9.40282167159023,333.257395605323,15.3488418003533));
#14240=CARTESIAN_POINT('Origin',(0.,10.75,0.));
#14241=CARTESIAN_POINT('Origin',(0.,10.75,0.));
#14242=CARTESIAN_POINT('',(6.89063395196164,10.7500000000001,16.6288653774115));
#14243=CARTESIAN_POINT('',(6.89063395196164,-5.75,16.6288653774115));
#14244=CARTESIAN_POINT('',(6.89063395196164,333.257395605323,16.6288653774115));
#14245=CARTESIAN_POINT('',(6.88596947769954,-5.74999999999998,16.6307974659122));
#14246=CARTESIAN_POINT('Origin',(0.,-5.75,0.));
#14247=CARTESIAN_POINT('',(6.88596947769954,10.7500000000001,16.6307974659122));
#14248=CARTESIAN_POINT('',(6.88596947769954,333.257395605323,16.6307974659122));
#14249=CARTESIAN_POINT('Origin',(0.,10.75,0.));
#14250=CARTESIAN_POINT('Origin',(0.,10.75,0.));
#14251=CARTESIAN_POINT('',(4.20447115412013,10.7500000000001,17.5020690866586));
#14252=CARTESIAN_POINT('',(4.20447115412013,-5.75,17.5020690866586));
#14253=CARTESIAN_POINT('',(4.20447115412013,333.257395605323,17.5020690866586));
#14254=CARTESIAN_POINT('',(4.19956186204543,-5.74999999999998,17.5032477034079));
#14255=CARTESIAN_POINT('Origin',(0.,-5.75,0.));
#14256=CARTESIAN_POINT('',(4.19956186204542,10.7500000000001,17.5032477034079));
#14257=CARTESIAN_POINT('',(4.19956186204542,333.257395605323,17.5032477034079));
#14258=CARTESIAN_POINT('Origin',(0.,10.75,0.));
#14259=CARTESIAN_POINT('Origin',(0.,10.75,0.));
#14260=CARTESIAN_POINT('',(1.41478032262442,10.7500000000001,17.9443137689552));
#14261=CARTESIAN_POINT('',(1.41478032262442,-5.75,17.9443137689552));
#14262=CARTESIAN_POINT('',(1.41478032262442,333.257395605323,17.9443137689552));
#14263=CARTESIAN_POINT('',(1.409747095801,-5.74999999999998,17.944709892497));
#14264=CARTESIAN_POINT('Origin',(0.,-5.75,0.));
#14265=CARTESIAN_POINT('',(1.409747095801,10.7500000000001,17.944709892497));
#14266=CARTESIAN_POINT('',(1.409747095801,333.257395605323,17.944709892497));
#14267=CARTESIAN_POINT('Origin',(0.,10.75,0.));
#14268=CARTESIAN_POINT('Origin',(0.,10.75,0.));
#14269=CARTESIAN_POINT('',(-1.40974709580099,10.7500000000001,17.944709892497));
#14270=CARTESIAN_POINT('',(-1.40974709580099,-5.75,17.944709892497));
#14271=CARTESIAN_POINT('',(-1.40974709580099,333.257395605323,17.944709892497));
#14272=CARTESIAN_POINT('',(-1.41478032262415,-5.74999999999998,17.9443137689552));
#14273=CARTESIAN_POINT('Origin',(0.,-5.75,0.));
#14274=CARTESIAN_POINT('',(-1.41478032262415,10.7500000000001,17.9443137689552));
#14275=CARTESIAN_POINT('',(-1.41478032262415,333.257395605323,17.9443137689552));
#14276=CARTESIAN_POINT('Origin',(0.,10.75,0.));
#14277=CARTESIAN_POINT('Origin',(2.35100371814953E-15,333.257395605323,
18.9983764079945));
#14278=CARTESIAN_POINT('',(2.35100371814953E-15,-5.74999999999998,18.9983764079945));
#14279=CARTESIAN_POINT('',(2.35100371814953E-15,-5.74999999999998,18.9983764079945));
#14280=CARTESIAN_POINT('',(2.35100371814953E-15,10.7500000000001,18.9983764079945));
#14281=CARTESIAN_POINT('',(2.35100371814953E-15,333.257395605323,18.9983764079945));
#14282=CARTESIAN_POINT('',(9.1103600220179,10.75,12.1891541525139));
#14283=CARTESIAN_POINT('Origin',(2.35100371814953E-15,333.257395605323,
18.9983764079945));
#14284=CARTESIAN_POINT('',(2.35100371814953E-15,-5.74999999999998,18.9983764079945));
#14285=CARTESIAN_POINT('',(-9.11036002201789,10.75,12.1891541525139));
#14286=CARTESIAN_POINT('Origin',(2.97200085001758,333.257395605323,18.7644748684139));
#14287=CARTESIAN_POINT('',(2.97200085001758,-5.74999999999998,18.7644748684139));
#14288=CARTESIAN_POINT('',(2.97200085001758,-5.74999999999998,18.7644748684139));
#14289=CARTESIAN_POINT('',(2.97200085001758,10.7500000000001,18.7644748684139));
#14290=CARTESIAN_POINT('',(2.97200085001758,333.257395605323,18.7644748684139));
#14291=CARTESIAN_POINT('',(10.9050001815126,10.75,10.6139111417865));
#14292=CARTESIAN_POINT('Origin',(2.97200085001758,333.257395605323,18.7644748684139));
#14293=CARTESIAN_POINT('',(2.97200085001758,-5.74999999999998,18.7644748684139));
#14294=CARTESIAN_POINT('',(-7.09139256322972,10.75,13.4642597345231));
#14295=CARTESIAN_POINT('Origin',(5.8708211756024,333.257395605323,18.0685296818513));
#14296=CARTESIAN_POINT('',(5.8708211756024,-5.74999999999998,18.0685296818513));
#14297=CARTESIAN_POINT('',(5.8708211756024,-5.74999999999998,18.0685296818513));
#14298=CARTESIAN_POINT('',(5.8708211756024,10.7500000000001,18.0685296818513));
#14299=CARTESIAN_POINT('',(5.8708211756024,333.257395605323,18.0685296818513));
#14300=CARTESIAN_POINT('',(12.4311230449177,10.75,8.77731841319679));
#14301=CARTESIAN_POINT('Origin',(5.8708211756024,333.257395605323,18.0685296818513));
#14302=CARTESIAN_POINT('',(5.8708211756024,-5.74999999999998,18.0685296818513));
#14303=CARTESIAN_POINT('',(-4.89781148455222,10.75,14.4078305565521));
#14304=CARTESIAN_POINT('Origin',(8.62508239970547,333.257395605323,16.9276773285095));
#14305=CARTESIAN_POINT('',(8.62508239970547,-5.74999999999998,16.9276773285095));
#14306=CARTESIAN_POINT('',(8.62508239970547,-5.74999999999998,16.9276773285095));
#14307=CARTESIAN_POINT('',(8.62508239970547,10.7500000000001,16.9276773285095));
#14308=CARTESIAN_POINT('',(8.62508239970547,333.257395605323,16.9276773285095));
#14309=CARTESIAN_POINT('',(13.651150402425,10.75,6.72459897502448));
#14310=CARTESIAN_POINT('Origin',(8.62508239970547,333.257395605323,16.9276773285095));
#14311=CARTESIAN_POINT('',(8.62508239970547,-5.74999999999998,16.9276773285095));
#14312=CARTESIAN_POINT('',(-2.58363003222066,10.75,14.9966327734307));
#14313=CARTESIAN_POINT('Origin',(11.1669654701205,333.257395605323,15.3700093795996));
#14314=CARTESIAN_POINT('',(11.1669654701205,-5.74999999999998,15.3700093795996));
#14315=CARTESIAN_POINT('',(11.1669654701205,-5.74999999999998,15.3700093795996));
#14316=CARTESIAN_POINT('',(11.1669654701205,10.7500000000001,15.3700093795996));
#14317=CARTESIAN_POINT('',(11.1669654701205,333.257395605323,15.3700093795996));
#14318=CARTESIAN_POINT('',(14.5350411314538,10.75,4.50629759242261));
#14319=CARTESIAN_POINT('Origin',(11.1669654701205,333.257395605323,15.3700093795996));
#14320=CARTESIAN_POINT('',(11.1669654701205,-5.74999999999998,15.3700093795996));
#14321=CARTESIAN_POINT('',(-0.205831033919359,10.75,15.2161681204567));
#14322=CARTESIAN_POINT('Origin',(13.4338807896275,333.257395605323,13.4338807896274));
#14323=CARTESIAN_POINT('',(13.4338807896275,-5.74999999999998,13.4338807896274));
#14324=CARTESIAN_POINT('',(13.4338807896275,-5.74999999999998,13.4338807896274));
#14325=CARTESIAN_POINT('',(13.4338807896275,10.7500000000001,13.4338807896274));
#14326=CARTESIAN_POINT('',(13.4338807896275,333.257395605323,13.4338807896274));
#14327=CARTESIAN_POINT('',(15.0610309087904,10.75,2.17703620755101));
#14328=CARTESIAN_POINT('Origin',(13.4338807896275,333.257395605323,13.4338807896274));
#14329=CARTESIAN_POINT('',(13.4338807896275,-5.74999999999998,13.4338807896274));
#14330=CARTESIAN_POINT('',(2.17703620755108,10.75,15.0610309087904));
#14331=CARTESIAN_POINT('Origin',(15.3700093795997,333.257395605323,11.1669654701204));
#14332=CARTESIAN_POINT('',(15.3700093795997,-5.74999999999998,11.1669654701204));
#14333=CARTESIAN_POINT('',(15.3700093795997,-5.74999999999998,11.1669654701204));
#14334=CARTESIAN_POINT('',(15.3700093795997,10.7500000000001,11.1669654701204));
#14335=CARTESIAN_POINT('',(15.3700093795997,333.257395605323,11.1669654701204));
#14336=CARTESIAN_POINT('',(15.2161681204567,10.75,-0.205831033919424));
#14337=CARTESIAN_POINT('Origin',(15.3700093795997,333.257395605323,11.1669654701204));
#14338=CARTESIAN_POINT('',(15.3700093795997,-5.74999999999998,11.1669654701204));
#14339=CARTESIAN_POINT('',(4.50629759242267,10.75,14.5350411314538));
#14340=CARTESIAN_POINT('Origin',(16.9276773285095,333.257395605323,8.62508239970541));
#14341=CARTESIAN_POINT('',(16.9276773285095,-5.74999999999998,8.62508239970541));
#14342=CARTESIAN_POINT('',(16.9276773285095,-5.74999999999998,8.62508239970541));
#14343=CARTESIAN_POINT('',(16.9276773285095,10.7500000000001,8.62508239970541));
#14344=CARTESIAN_POINT('',(16.9276773285095,333.257395605323,8.62508239970541));
#14345=CARTESIAN_POINT('',(14.9966327734307,10.75,-2.58363003222073));
#14346=CARTESIAN_POINT('Origin',(16.9276773285095,333.257395605323,8.62508239970541));
#14347=CARTESIAN_POINT('',(16.9276773285095,-5.74999999999998,8.62508239970541));
#14348=CARTESIAN_POINT('',(6.72459897502454,10.75,13.651150402425));
#14349=CARTESIAN_POINT('Origin',(18.0685296818513,333.257395605323,5.87082117560233));
#14350=CARTESIAN_POINT('',(18.0685296818513,-5.74999999999998,5.87082117560233));
#14351=CARTESIAN_POINT('',(18.0685296818513,-5.74999999999998,5.87082117560233));
#14352=CARTESIAN_POINT('',(18.0685296818513,10.7500000000001,5.87082117560233));
#14353=CARTESIAN_POINT('',(18.0685296818513,333.257395605323,5.87082117560233));
#14354=CARTESIAN_POINT('',(14.4078305565521,10.75,-4.89781148455228));
#14355=CARTESIAN_POINT('Origin',(18.0685296818513,333.257395605323,5.87082117560233));
#14356=CARTESIAN_POINT('',(18.0685296818513,-5.74999999999998,5.87082117560233));
#14357=CARTESIAN_POINT('',(8.77731841319684,10.75,12.4311230449177));
#14358=CARTESIAN_POINT('Origin',(18.7644748684139,333.257395605323,2.9720008500175));
#14359=CARTESIAN_POINT('',(18.7644748684139,-5.74999999999998,2.9720008500175));
#14360=CARTESIAN_POINT('',(18.7644748684139,-5.74999999999998,2.9720008500175));
#14361=CARTESIAN_POINT('',(18.7644748684139,10.7500000000001,2.9720008500175));
#14362=CARTESIAN_POINT('',(18.7644748684139,333.257395605323,2.9720008500175));
#14363=CARTESIAN_POINT('',(13.464259734523,10.75,-7.09139256322977));
#14364=CARTESIAN_POINT('Origin',(18.7644748684139,333.257395605323,2.9720008500175));
#14365=CARTESIAN_POINT('',(18.7644748684139,-5.74999999999998,2.9720008500175));
#14366=CARTESIAN_POINT('',(10.6139111417865,10.75,10.9050001815125));
#14367=CARTESIAN_POINT('Origin',(18.9983764079945,333.257395605323,-6.86834804149801E-14));
#14368=CARTESIAN_POINT('',(18.9983764079945,-5.74999999999998,-6.86834804149801E-14));
#14369=CARTESIAN_POINT('',(18.9983764079945,-5.74999999999998,-6.86834804149801E-14));
#14370=CARTESIAN_POINT('',(18.9983764079945,10.7500000000001,-6.86834804149801E-14));
#14371=CARTESIAN_POINT('',(18.9983764079945,333.257395605323,-6.86834804149801E-14));
#14372=CARTESIAN_POINT('',(12.1891541525138,10.75,-9.11036002201794));
#14373=CARTESIAN_POINT('Origin',(18.9983764079945,333.257395605323,-6.86834804149801E-14));
#14374=CARTESIAN_POINT('',(18.9983764079945,-5.74999999999998,-6.86834804149801E-14));
#14375=CARTESIAN_POINT('',(12.1891541525139,10.75,9.11036002201785));
#14376=CARTESIAN_POINT('Origin',(18.7644748684139,333.257395605323,-2.97200085001764));
#14377=CARTESIAN_POINT('',(18.7644748684139,-5.74999999999998,-2.97200085001764));
#14378=CARTESIAN_POINT('',(18.7644748684139,-5.74999999999998,-2.97200085001764));
#14379=CARTESIAN_POINT('',(18.7644748684139,10.7500000000001,-2.97200085001764));
#14380=CARTESIAN_POINT('',(18.7644748684139,333.257395605323,-2.97200085001764));
#14381=CARTESIAN_POINT('',(10.6139111417864,10.75,-10.9050001815126));
#14382=CARTESIAN_POINT('Origin',(18.7644748684139,333.257395605323,-2.97200085001764));
#14383=CARTESIAN_POINT('',(18.7644748684139,-5.74999999999998,-2.97200085001764));
#14384=CARTESIAN_POINT('',(13.4642597345231,10.75,7.09139256322967));
#14385=CARTESIAN_POINT('Origin',(18.0685296818513,333.257395605323,-5.87082117560246));
#14386=CARTESIAN_POINT('',(18.0685296818513,-5.74999999999998,-5.87082117560246));
#14387=CARTESIAN_POINT('',(18.0685296818513,-5.74999999999998,-5.87082117560246));
#14388=CARTESIAN_POINT('',(18.0685296818513,10.7500000000001,-5.87082117560246));
#14389=CARTESIAN_POINT('',(18.0685296818513,333.257395605323,-5.87082117560246));
#14390=CARTESIAN_POINT('',(8.77731841319674,10.75,-12.4311230449178));
#14391=CARTESIAN_POINT('Origin',(18.0685296818513,333.257395605323,-5.87082117560246));
#14392=CARTESIAN_POINT('',(18.0685296818513,-5.74999999999998,-5.87082117560246));
#14393=CARTESIAN_POINT('',(14.4078305565521,10.75,4.89781148455217));
#14394=CARTESIAN_POINT('Origin',(16.9276773285095,333.257395605323,-8.62508239970554));
#14395=CARTESIAN_POINT('',(16.9276773285095,-5.74999999999998,-8.62508239970554));
#14396=CARTESIAN_POINT('',(16.9276773285095,-5.74999999999998,-8.62508239970554));
#14397=CARTESIAN_POINT('',(16.9276773285095,10.7500000000001,-8.62508239970554));
#14398=CARTESIAN_POINT('',(16.9276773285095,333.257395605323,-8.62508239970554));
#14399=CARTESIAN_POINT('',(6.72459897502443,10.75,-13.651150402425));
#14400=CARTESIAN_POINT('Origin',(16.9276773285095,333.257395605323,-8.62508239970554));
#14401=CARTESIAN_POINT('',(16.9276773285095,-5.74999999999998,-8.62508239970554));
#14402=CARTESIAN_POINT('',(14.9966327734307,10.75,2.58363003222061));
#14403=CARTESIAN_POINT('Origin',(15.3700093795996,333.257395605323,-11.1669654701205));
#14404=CARTESIAN_POINT('',(15.3700093795996,-5.74999999999998,-11.1669654701205));
#14405=CARTESIAN_POINT('',(15.3700093795996,-5.74999999999998,-11.1669654701205));
#14406=CARTESIAN_POINT('',(15.3700093795996,10.7500000000001,-11.1669654701205));
#14407=CARTESIAN_POINT('',(15.3700093795996,333.257395605323,-11.1669654701205));
#14408=CARTESIAN_POINT('',(4.50629759242255,10.75,-14.5350411314538));
#14409=CARTESIAN_POINT('Origin',(15.3700093795996,333.257395605323,-11.1669654701205));
#14410=CARTESIAN_POINT('',(15.3700093795996,-5.74999999999998,-11.1669654701205));
#14411=CARTESIAN_POINT('',(15.2161681204567,10.75,0.205831033919306));
#14412=CARTESIAN_POINT('Origin',(13.4338807896274,333.257395605323,-13.4338807896275));
#14413=CARTESIAN_POINT('',(13.4338807896274,-5.74999999999998,-13.4338807896275));
#14414=CARTESIAN_POINT('',(13.4338807896274,-5.74999999999998,-13.4338807896275));
#14415=CARTESIAN_POINT('',(13.4338807896274,10.7500000000001,-13.4338807896275));
#14416=CARTESIAN_POINT('',(13.4338807896274,333.257395605323,-13.4338807896275));
#14417=CARTESIAN_POINT('',(2.17703620755096,10.75,-15.0610309087904));
#14418=CARTESIAN_POINT('Origin',(13.4338807896274,333.257395605323,-13.4338807896275));
#14419=CARTESIAN_POINT('',(13.4338807896274,-5.74999999999998,-13.4338807896275));
#14420=CARTESIAN_POINT('',(15.0610309087904,10.75,-2.17703620755113));
#14421=CARTESIAN_POINT('Origin',(11.1669654701203,333.257395605323,-15.3700093795997));
#14422=CARTESIAN_POINT('',(11.1669654701203,-5.74999999999998,-15.3700093795997));
#14423=CARTESIAN_POINT('',(11.1669654701203,-5.74999999999998,-15.3700093795997));
#14424=CARTESIAN_POINT('',(11.1669654701203,10.7500000000001,-15.3700093795997));
#14425=CARTESIAN_POINT('',(11.1669654701203,333.257395605323,-15.3700093795997));
#14426=CARTESIAN_POINT('',(-0.205831033919478,10.75,-15.2161681204567));
#14427=CARTESIAN_POINT('Origin',(11.1669654701203,333.257395605323,-15.3700093795997));
#14428=CARTESIAN_POINT('',(11.1669654701203,-5.74999999999998,-15.3700093795997));
#14429=CARTESIAN_POINT('',(14.5350411314538,10.75,-4.50629759242272));
#14430=CARTESIAN_POINT('Origin',(8.62508239970535,333.257395605323,-16.9276773285096));
#14431=CARTESIAN_POINT('',(8.62508239970535,-5.74999999999998,-16.9276773285096));
#14432=CARTESIAN_POINT('',(8.62508239970535,-5.74999999999998,-16.9276773285096));
#14433=CARTESIAN_POINT('',(8.62508239970535,10.7500000000001,-16.9276773285096));
#14434=CARTESIAN_POINT('',(8.62508239970535,333.257395605323,-16.9276773285096));
#14435=CARTESIAN_POINT('',(-2.58363003222078,10.75,-14.9966327734307));
#14436=CARTESIAN_POINT('Origin',(8.62508239970535,333.257395605323,-16.9276773285096));
#14437=CARTESIAN_POINT('',(8.62508239970535,-5.74999999999998,-16.9276773285096));
#14438=CARTESIAN_POINT('',(13.6511504024249,10.75,-6.72459897502459));
#14439=CARTESIAN_POINT('Origin',(5.87082117560226,333.257395605323,-18.0685296818514));
#14440=CARTESIAN_POINT('',(5.87082117560226,-5.74999999999998,-18.0685296818514));
#14441=CARTESIAN_POINT('',(5.87082117560226,-5.74999999999998,-18.0685296818514));
#14442=CARTESIAN_POINT('',(5.87082117560226,10.7500000000001,-18.0685296818514));
#14443=CARTESIAN_POINT('',(5.87082117560226,333.257395605323,-18.0685296818514));
#14444=CARTESIAN_POINT('',(-4.89781148455233,10.75,-14.4078305565521));
#14445=CARTESIAN_POINT('Origin',(5.87082117560226,333.257395605323,-18.0685296818514));
#14446=CARTESIAN_POINT('',(5.87082117560226,-5.74999999999998,-18.0685296818514));
#14447=CARTESIAN_POINT('',(12.4311230449177,10.75,-8.77731841319689));
#14448=CARTESIAN_POINT('Origin',(2.97200085001744,333.257395605323,-18.764474868414));
#14449=CARTESIAN_POINT('',(2.97200085001744,-5.74999999999998,-18.764474868414));
#14450=CARTESIAN_POINT('',(2.97200085001744,-5.74999999999998,-18.764474868414));
#14451=CARTESIAN_POINT('',(2.97200085001744,10.7500000000001,-18.764474868414));
#14452=CARTESIAN_POINT('',(2.97200085001744,333.257395605323,-18.764474868414));
#14453=CARTESIAN_POINT('',(-7.09139256322982,10.75,-13.464259734523));
#14454=CARTESIAN_POINT('Origin',(2.97200085001744,333.257395605323,-18.764474868414));
#14455=CARTESIAN_POINT('',(2.97200085001744,-5.74999999999998,-18.764474868414));
#14456=CARTESIAN_POINT('',(10.9050001815125,10.75,-10.6139111417866));
#14457=CARTESIAN_POINT('Origin',(-2.35100371814953E-15,333.257395605323,
-18.9983764079945));
#14458=CARTESIAN_POINT('',(-2.35100371814953E-15,-5.74999999999998,-18.9983764079945));
#14459=CARTESIAN_POINT('',(-2.35100371814953E-15,-5.74999999999998,-18.9983764079945));
#14460=CARTESIAN_POINT('',(-2.35100371814953E-15,10.7500000000001,-18.9983764079945));
#14461=CARTESIAN_POINT('',(-2.35100371814953E-15,333.257395605323,-18.9983764079945));
#14462=CARTESIAN_POINT('',(-9.1103600220179,10.75,-12.1891541525139));
#14463=CARTESIAN_POINT('Origin',(-2.35100371814953E-15,333.257395605323,
-18.9983764079945));
#14464=CARTESIAN_POINT('',(-2.35100371814953E-15,-5.74999999999998,-18.9983764079945));
#14465=CARTESIAN_POINT('',(9.11036002201789,10.75,-12.1891541525139));
#14466=CARTESIAN_POINT('Origin',(-2.97200085001771,333.257395605323,-18.7644748684139));
#14467=CARTESIAN_POINT('',(-2.97200085001771,-5.74999999999998,-18.7644748684139));
#14468=CARTESIAN_POINT('',(-2.97200085001771,-5.74999999999998,-18.7644748684139));
#14469=CARTESIAN_POINT('',(-2.97200085001771,10.7500000000001,-18.7644748684139));
#14470=CARTESIAN_POINT('',(-2.97200085001771,333.257395605323,-18.7644748684139));
#14471=CARTESIAN_POINT('',(-10.9050001815126,10.75,-10.6139111417864));
#14472=CARTESIAN_POINT('Origin',(-2.97200085001771,333.257395605323,-18.7644748684139));
#14473=CARTESIAN_POINT('',(-2.97200085001771,-5.74999999999998,-18.7644748684139));
#14474=CARTESIAN_POINT('',(7.09139256322962,10.75,-13.4642597345231));
#14475=CARTESIAN_POINT('Origin',(-5.87082117560253,333.257395605323,-18.0685296818513));
#14476=CARTESIAN_POINT('',(-5.87082117560253,-5.74999999999998,-18.0685296818513));
#14477=CARTESIAN_POINT('',(-5.87082117560253,-5.74999999999998,-18.0685296818513));
#14478=CARTESIAN_POINT('',(-5.87082117560253,10.7500000000001,-18.0685296818513));
#14479=CARTESIAN_POINT('',(-5.87082117560253,333.257395605323,-18.0685296818513));
#14480=CARTESIAN_POINT('',(-12.4311230449178,10.75,-8.7773184131967));
#14481=CARTESIAN_POINT('Origin',(-5.87082117560253,333.257395605323,-18.0685296818513));
#14482=CARTESIAN_POINT('',(-5.87082117560253,-5.74999999999998,-18.0685296818513));
#14483=CARTESIAN_POINT('',(4.89781148455211,10.75,-14.4078305565521));
#14484=CARTESIAN_POINT('Origin',(-8.6250823997056,333.257395605323,-16.9276773285094));
#14485=CARTESIAN_POINT('',(-8.6250823997056,-5.74999999999998,-16.9276773285094));
#14486=CARTESIAN_POINT('',(-8.6250823997056,-5.74999999999998,-16.9276773285094));
#14487=CARTESIAN_POINT('',(-8.6250823997056,10.7500000000001,-16.9276773285094));
#14488=CARTESIAN_POINT('',(-8.6250823997056,333.257395605323,-16.9276773285094));
#14489=CARTESIAN_POINT('',(-13.651150402425,10.75,-6.72459897502439));
#14490=CARTESIAN_POINT('Origin',(-8.6250823997056,333.257395605323,-16.9276773285094));
#14491=CARTESIAN_POINT('',(-8.6250823997056,-5.74999999999998,-16.9276773285094));
#14492=CARTESIAN_POINT('',(2.58363003222055,10.75,-14.9966327734307));
#14493=CARTESIAN_POINT('Origin',(-11.1669654701206,333.257395605323,-15.3700093795995));
#14494=CARTESIAN_POINT('',(-11.1669654701206,-5.74999999999998,-15.3700093795995));
#14495=CARTESIAN_POINT('',(-11.1669654701206,-5.74999999999998,-15.3700093795995));
#14496=CARTESIAN_POINT('',(-11.1669654701206,10.7500000000001,-15.3700093795995));
#14497=CARTESIAN_POINT('',(-11.1669654701206,333.257395605323,-15.3700093795995));
#14498=CARTESIAN_POINT('',(-14.5350411314539,10.75,-4.5062975924225));
#14499=CARTESIAN_POINT('Origin',(-11.1669654701206,333.257395605323,-15.3700093795995));
#14500=CARTESIAN_POINT('',(-11.1669654701206,-5.74999999999998,-15.3700093795995));
#14501=CARTESIAN_POINT('',(0.205831033919245,10.75,-15.2161681204567));
#14502=CARTESIAN_POINT('Origin',(-13.4338807896276,333.257395605323,-13.4338807896273));
#14503=CARTESIAN_POINT('',(-13.4338807896276,-5.74999999999998,-13.4338807896273));
#14504=CARTESIAN_POINT('',(-13.4338807896276,-5.74999999999998,-13.4338807896273));
#14505=CARTESIAN_POINT('',(-13.4338807896276,10.7500000000001,-13.4338807896273));
#14506=CARTESIAN_POINT('',(-13.4338807896276,333.257395605323,-13.4338807896273));
#14507=CARTESIAN_POINT('',(-15.0610309087904,10.75,-2.17703620755091));
#14508=CARTESIAN_POINT('Origin',(-13.4338807896276,333.257395605323,-13.4338807896273));
#14509=CARTESIAN_POINT('',(-13.4338807896276,-5.74999999999998,-13.4338807896273));
#14510=CARTESIAN_POINT('',(-2.17703620755118,10.75,-15.0610309087904));
#14511=CARTESIAN_POINT('Origin',(-15.3700093795998,333.257395605323,-11.1669654701203));
#14512=CARTESIAN_POINT('',(-15.3700093795998,-5.74999999999998,-11.1669654701203));
#14513=CARTESIAN_POINT('',(-15.3700093795998,-5.74999999999998,-11.1669654701203));
#14514=CARTESIAN_POINT('',(-15.3700093795998,10.7500000000001,-11.1669654701203));
#14515=CARTESIAN_POINT('',(-15.3700093795998,333.257395605323,-11.1669654701203));
#14516=CARTESIAN_POINT('',(-15.2161681204567,10.75,0.205831033919538));
#14517=CARTESIAN_POINT('Origin',(-15.3700093795998,333.257395605323,-11.1669654701203));
#14518=CARTESIAN_POINT('',(-15.3700093795998,-5.74999999999998,-11.1669654701203));
#14519=CARTESIAN_POINT('',(-4.50629759242278,10.75,-14.5350411314538));
#14520=CARTESIAN_POINT('Origin',(-16.9276773285096,333.257395605323,-8.62508239970529));
#14521=CARTESIAN_POINT('',(-16.9276773285096,-5.74999999999998,-8.62508239970529));
#14522=CARTESIAN_POINT('',(-16.9276773285096,-5.74999999999998,-8.62508239970529));
#14523=CARTESIAN_POINT('',(-16.9276773285096,10.7500000000001,-8.62508239970529));
#14524=CARTESIAN_POINT('',(-16.9276773285096,333.257395605323,-8.62508239970529));
#14525=CARTESIAN_POINT('',(-14.9966327734307,10.75,2.58363003222083));
#14526=CARTESIAN_POINT('Origin',(-16.9276773285096,333.257395605323,-8.62508239970529));
#14527=CARTESIAN_POINT('',(-16.9276773285096,-5.74999999999998,-8.62508239970529));
#14528=CARTESIAN_POINT('',(-6.72459897502464,10.75,-13.6511504024249));
#14529=CARTESIAN_POINT('Origin',(-18.0685296818514,333.257395605323,-5.8708211756022));
#14530=CARTESIAN_POINT('',(-18.0685296818514,-5.74999999999998,-5.8708211756022));
#14531=CARTESIAN_POINT('',(-18.0685296818514,-5.74999999999998,-5.8708211756022));
#14532=CARTESIAN_POINT('',(-18.0685296818514,10.7500000000001,-5.8708211756022));
#14533=CARTESIAN_POINT('',(-18.0685296818514,333.257395605323,-5.8708211756022));
#14534=CARTESIAN_POINT('',(-14.407830556552,10.75,4.89781148455238));
#14535=CARTESIAN_POINT('Origin',(-18.0685296818514,333.257395605323,-5.8708211756022));
#14536=CARTESIAN_POINT('',(-18.0685296818514,-5.74999999999998,-5.8708211756022));
#14537=CARTESIAN_POINT('',(-8.77731841319692,10.75,-12.4311230449176));
#14538=CARTESIAN_POINT('Origin',(-18.764474868414,333.257395605323,-2.97200085001737));
#14539=CARTESIAN_POINT('',(-18.764474868414,-5.74999999999998,-2.97200085001737));
#14540=CARTESIAN_POINT('',(-18.764474868414,-5.74999999999998,-2.97200085001737));
#14541=CARTESIAN_POINT('',(-18.764474868414,10.7500000000001,-2.97200085001737));
#14542=CARTESIAN_POINT('',(-18.764474868414,333.257395605323,-2.97200085001737));
#14543=CARTESIAN_POINT('',(-13.464259734523,10.75,7.09139256322987));
#14544=CARTESIAN_POINT('Origin',(-18.764474868414,333.257395605323,-2.97200085001737));
#14545=CARTESIAN_POINT('',(-18.764474868414,-5.74999999999998,-2.97200085001737));
#14546=CARTESIAN_POINT('',(-10.6139111417866,10.75,-10.9050001815124));
#14547=CARTESIAN_POINT('Origin',(-18.9983764079945,333.257395605323,2.01348433808641E-13));
#14548=CARTESIAN_POINT('',(-18.9983764079945,-5.74999999999998,2.01348433808641E-13));
#14549=CARTESIAN_POINT('',(-18.9983764079945,-5.74999999999998,2.01348433808641E-13));
#14550=CARTESIAN_POINT('',(-18.9983764079945,10.7500000000001,2.01348433808641E-13));
#14551=CARTESIAN_POINT('',(-18.9983764079945,333.257395605323,2.01348433808641E-13));
#14552=CARTESIAN_POINT('',(-12.1891541525138,10.75,9.11036002201803));
#14553=CARTESIAN_POINT('Origin',(-18.9983764079945,333.257395605323,2.01348433808641E-13));
#14554=CARTESIAN_POINT('',(-18.9983764079945,-5.74999999999998,2.01348433808641E-13));
#14555=CARTESIAN_POINT('',(-12.189154152514,10.75,-9.11036002201777));
#14556=CARTESIAN_POINT('Origin',(-18.7644748684139,333.257395605323,2.97200085001778));
#14557=CARTESIAN_POINT('',(-18.7644748684139,-5.74999999999998,2.97200085001778));
#14558=CARTESIAN_POINT('',(-18.7644748684139,-5.74999999999998,2.97200085001778));
#14559=CARTESIAN_POINT('',(-18.7644748684139,10.7500000000001,2.97200085001778));
#14560=CARTESIAN_POINT('',(-18.7644748684139,333.257395605323,2.97200085001778));
#14561=CARTESIAN_POINT('',(-10.6139111417864,10.75,10.9050001815127));
#14562=CARTESIAN_POINT('Origin',(-18.7644748684139,333.257395605323,2.97200085001778));
#14563=CARTESIAN_POINT('',(-18.7644748684139,-5.74999999999998,2.97200085001778));
#14564=CARTESIAN_POINT('',(-13.4642597345231,10.75,-7.09139256322957));
#14565=CARTESIAN_POINT('Origin',(-18.0685296818512,333.257395605323,5.87082117560259));
#14566=CARTESIAN_POINT('',(-18.0685296818512,-5.74999999999998,5.87082117560259));
#14567=CARTESIAN_POINT('',(-18.0685296818512,-5.74999999999998,5.87082117560259));
#14568=CARTESIAN_POINT('',(-18.0685296818512,10.7500000000001,5.87082117560259));
#14569=CARTESIAN_POINT('',(-18.0685296818512,333.257395605323,5.87082117560259));
#14570=CARTESIAN_POINT('',(-8.77731841319665,10.75,12.4311230449178));
#14571=CARTESIAN_POINT('Origin',(-18.0685296818512,333.257395605323,5.87082117560259));
#14572=CARTESIAN_POINT('',(-18.0685296818512,-5.74999999999998,5.87082117560259));
#14573=CARTESIAN_POINT('',(-14.4078305565522,10.75,-4.89781148455206));
#14574=CARTESIAN_POINT('Origin',(-16.9276773285094,333.257395605323,8.62508239970565));
#14575=CARTESIAN_POINT('',(-16.9276773285094,-5.74999999999998,8.62508239970565));
#14576=CARTESIAN_POINT('',(-16.9276773285094,-5.74999999999998,8.62508239970565));
#14577=CARTESIAN_POINT('',(-16.9276773285094,10.7500000000001,8.62508239970565));
#14578=CARTESIAN_POINT('',(-16.9276773285094,333.257395605323,8.62508239970565));
#14579=CARTESIAN_POINT('',(-6.72459897502434,10.75,13.6511504024251));
#14580=CARTESIAN_POINT('Origin',(-16.9276773285094,333.257395605323,8.62508239970565));
#14581=CARTESIAN_POINT('',(-16.9276773285094,-5.74999999999998,8.62508239970565));
#14582=CARTESIAN_POINT('',(-14.9966327734307,10.75,-2.58363003222051));
#14583=CARTESIAN_POINT('Origin',(-15.3700093795995,333.257395605323,11.1669654701206));
#14584=CARTESIAN_POINT('',(-15.3700093795995,-5.74999999999998,11.1669654701206));
#14585=CARTESIAN_POINT('',(-15.3700093795995,-5.74999999999998,11.1669654701206));
#14586=CARTESIAN_POINT('',(-15.3700093795995,10.7500000000001,11.1669654701206));
#14587=CARTESIAN_POINT('',(-15.3700093795995,333.257395605323,11.1669654701206));
#14588=CARTESIAN_POINT('',(-4.50629759242245,10.75,14.5350411314539));
#14589=CARTESIAN_POINT('Origin',(-15.3700093795995,333.257395605323,11.1669654701206));
#14590=CARTESIAN_POINT('',(-15.3700093795995,-5.74999999999998,11.1669654701206));
#14591=CARTESIAN_POINT('',(-15.2161681204567,10.75,-0.205831033919193));
#14592=CARTESIAN_POINT('Origin',(-13.4338807896273,333.257395605323,13.4338807896276));
#14593=CARTESIAN_POINT('',(-13.4338807896273,-5.74999999999998,13.4338807896276));
#14594=CARTESIAN_POINT('',(-13.4338807896273,-5.74999999999998,13.4338807896276));
#14595=CARTESIAN_POINT('',(-13.4338807896273,10.7500000000001,13.4338807896276));
#14596=CARTESIAN_POINT('',(-13.4338807896273,333.257395605323,13.4338807896276));
#14597=CARTESIAN_POINT('',(-2.17703620755086,10.75,15.0610309087904));
#14598=CARTESIAN_POINT('Origin',(-13.4338807896273,333.257395605323,13.4338807896276));
#14599=CARTESIAN_POINT('',(-13.4338807896273,-5.74999999999998,13.4338807896276));
#14600=CARTESIAN_POINT('',(-15.0610309087904,10.75,2.17703620755124));
#14601=CARTESIAN_POINT('Origin',(-11.1669654701202,333.257395605323,15.3700093795998));
#14602=CARTESIAN_POINT('',(-11.1669654701202,-5.74999999999998,15.3700093795998));
#14603=CARTESIAN_POINT('',(-11.1669654701202,-5.74999999999998,15.3700093795998));
#14604=CARTESIAN_POINT('',(-11.1669654701202,10.7500000000001,15.3700093795998));
#14605=CARTESIAN_POINT('',(-11.1669654701202,333.257395605323,15.3700093795998));
#14606=CARTESIAN_POINT('',(0.205831033919592,10.75,15.2161681204567));
#14607=CARTESIAN_POINT('Origin',(-11.1669654701202,333.257395605323,15.3700093795998));
#14608=CARTESIAN_POINT('',(-11.1669654701202,-5.74999999999998,15.3700093795998));
#14609=CARTESIAN_POINT('',(-14.5350411314538,10.75,4.50629759242283));
#14610=CARTESIAN_POINT('Origin',(-8.62508239970523,333.257395605323,16.9276773285096));
#14611=CARTESIAN_POINT('',(-8.62508239970523,-5.74999999999998,16.9276773285096));
#14612=CARTESIAN_POINT('',(-8.62508239970523,-5.74999999999998,16.9276773285096));
#14613=CARTESIAN_POINT('',(-8.62508239970523,10.7500000000001,16.9276773285096));
#14614=CARTESIAN_POINT('',(-8.62508239970523,333.257395605323,16.9276773285096));
#14615=CARTESIAN_POINT('',(2.58363003222089,10.75,14.9966327734307));
#14616=CARTESIAN_POINT('Origin',(-8.62508239970523,333.257395605323,16.9276773285096));
#14617=CARTESIAN_POINT('',(-8.62508239970523,-5.74999999999998,16.9276773285096));
#14618=CARTESIAN_POINT('',(-13.6511504024249,10.75,6.72459897502469));
#14619=CARTESIAN_POINT('Origin',(-5.87082117560214,333.257395605323,18.0685296818514));
#14620=CARTESIAN_POINT('',(-5.87082117560214,-5.74999999999998,18.0685296818514));
#14621=CARTESIAN_POINT('',(-5.87082117560214,-5.74999999999998,18.0685296818514));
#14622=CARTESIAN_POINT('',(-5.87082117560214,10.7500000000001,18.0685296818514));
#14623=CARTESIAN_POINT('',(-5.87082117560214,333.257395605323,18.0685296818514));
#14624=CARTESIAN_POINT('',(4.89781148455243,10.75,14.407830556552));
#14625=CARTESIAN_POINT('Origin',(-5.87082117560214,333.257395605323,18.0685296818514));
#14626=CARTESIAN_POINT('',(-5.87082117560214,-5.74999999999998,18.0685296818514));
#14627=CARTESIAN_POINT('',(-12.4311230449176,10.75,8.77731841319697));
#14628=CARTESIAN_POINT('Origin',(-2.9720008500173,333.257395605323,18.764474868414));
#14629=CARTESIAN_POINT('',(-2.9720008500173,-5.74999999999998,18.764474868414));
#14630=CARTESIAN_POINT('',(-2.9720008500173,-5.74999999999998,18.764474868414));
#14631=CARTESIAN_POINT('',(-2.9720008500173,10.7500000000001,18.764474868414));
#14632=CARTESIAN_POINT('',(-2.9720008500173,333.257395605323,18.764474868414));
#14633=CARTESIAN_POINT('',(7.09139256322992,10.75,13.4642597345229));
#14634=CARTESIAN_POINT('Origin',(-2.9720008500173,333.257395605323,18.764474868414));
#14635=CARTESIAN_POINT('',(-2.9720008500173,-5.74999999999998,18.764474868414));
#14636=CARTESIAN_POINT('',(-10.9050001815124,10.75,10.6139111417866));
#14637=CARTESIAN_POINT('Origin',(0.,10.75,0.));
#14638=CARTESIAN_POINT('',(-19.1556296640195,9.75000000013554,-16.0643184011738));
#14639=CARTESIAN_POINT('',(-19.1556295034202,-9.75000000012816,-16.0643182664888));
#14640=CARTESIAN_POINT('Ctrl Pts',(-19.1556296640195,9.75000000013554,-16.0643184011738));
#14641=CARTESIAN_POINT('Ctrl Pts',(-19.2208712137408,8.88364083244263,-15.986541870064));
#14642=CARTESIAN_POINT('Ctrl Pts',(-19.277148698093,8.01647570568422,-15.9184997691583));
#14643=CARTESIAN_POINT('Ctrl Pts',(-19.3246365744442,7.14847237162856,-15.8606239542862));
#14644=CARTESIAN_POINT('Ctrl Pts',(-19.3555503720308,6.58341700518073,-15.8229477858916));
#14645=CARTESIAN_POINT('Ctrl Pts',(-19.382739481617,6.01800679455978,-15.7895788865733));
#14646=CARTESIAN_POINT('Ctrl Pts',(-19.4062538058647,5.45223695733227,-15.760625407086));
#14647=CARTESIAN_POINT('Ctrl Pts',(-19.4438538502091,4.54755559186186,-15.714328005503));
#14648=CARTESIAN_POINT('Ctrl Pts',(-19.4720583966136,3.64194990530234,-15.6793387997003));
#14649=CARTESIAN_POINT('Ctrl Pts',(-19.4908797533348,2.73541348832897,-15.6559072598279));
#14650=CARTESIAN_POINT('Ctrl Pts',(-19.5097011100559,1.82887707135561,-15.6324757199555));
#14651=CARTESIAN_POINT('Ctrl Pts',(-19.5191393000384,0.92140994008045,-15.6206018131959));
#14652=CARTESIAN_POINT('Ctrl Pts',(-19.5192292333076,0.0130267934213882,
-15.6204894333562));
#14653=CARTESIAN_POINT('Ctrl Pts',(-19.5192296032355,0.00929028666506758,
-15.6204889710975));
#14654=CARTESIAN_POINT('Ctrl Pts',(-19.5192298134397,0.0055537642579053,
-15.6204887085208));
#14655=CARTESIAN_POINT('Ctrl Pts',(-19.5192298639648,0.0018172286253885,
-15.6204886455658));
#14656=CARTESIAN_POINT('Ctrl Pts',(-19.5192348828353,-0.369348115401582,
-15.6204823919898));
#14657=CARTESIAN_POINT('Ctrl Pts',(-19.5176643582502,-0.742191948960099,
-15.6224458020841));
#14658=CARTESIAN_POINT('Ctrl Pts',(-19.5145222635014,-1.11439334044658,
-15.6263694993203));
#14659=CARTESIAN_POINT('Ctrl Pts',(-19.5138140224602,-1.19828906037605,
-15.6272539167673));
#14660=CARTESIAN_POINT('Ctrl Pts',(-19.5130259293773,-1.2821519315032,-15.6282379367204));
#14661=CARTESIAN_POINT('Ctrl Pts',(-19.5121580206301,-1.36595500125534,
-15.6293214624937));
#14662=CARTESIAN_POINT('Ctrl Pts',(-19.5074230252224,-1.82315416151734,
-15.6352327862095));
#14663=CARTESIAN_POINT('Ctrl Pts',(-19.5003166417668,-2.27969557163659,
-15.6441004685152));
#14664=CARTESIAN_POINT('Ctrl Pts',(-19.4908482971583,-2.73568903694017,
-15.6558881146102));
#14665=CARTESIAN_POINT('Ctrl Pts',(-19.4720570197323,-3.64067296657114,
-15.6792823759227));
#14666=CARTESIAN_POINT('Ctrl Pts',(-19.4439717335206,-4.54350017251021,
-15.7141810578403));
#14667=CARTESIAN_POINT('Ctrl Pts',(-19.4065533265704,-5.44501179353637,
-15.7602565963606));
#14668=CARTESIAN_POINT('Ctrl Pts',(-19.3696896813279,-6.33315768985542,
-15.8056490233721));
#14669=CARTESIAN_POINT('Ctrl Pts',(-19.3237923792374,-7.22002942330059,
-15.8618979160963));
#14670=CARTESIAN_POINT('Ctrl Pts',(-19.268630719331,-8.1064004316186,-15.9286257991776));
#14671=CARTESIAN_POINT('Ctrl Pts',(-19.2345270546457,-8.65439880051663,
-15.969880274725));
#14672=CARTESIAN_POINT('Ctrl Pts',(-19.1968812804388,-9.20220540462824,
-16.0151404436434));
#14673=CARTESIAN_POINT('Ctrl Pts',(-19.1556295034202,-9.75000000012816,
-16.0643182664888));
#14674=CARTESIAN_POINT('',(19.1556241815518,-9.75000000004565,-16.0643138034269));
#14675=CARTESIAN_POINT('Origin',(0.,-9.75,0.));
#14676=CARTESIAN_POINT('',(19.1556296640198,9.75000000013388,-16.0643184011734));
#14677=CARTESIAN_POINT('Ctrl Pts',(19.1556295034199,-9.75000000013029,-16.0643182664893));
#14678=CARTESIAN_POINT('Ctrl Pts',(19.2223530215835,-8.86395859090214,-15.9847746057545));
#14679=CARTESIAN_POINT('Ctrl Pts',(19.2796449976598,-7.97788652210568,-15.9154801855084));
#14680=CARTESIAN_POINT('Ctrl Pts',(19.3277664720456,-7.09102032943713,-15.8568081429397));
#14681=CARTESIAN_POINT('Ctrl Pts',(19.3575175462091,-6.54271581034458,-15.8205341859993));
#14682=CARTESIAN_POINT('Ctrl Pts',(19.3837623989102,-5.99410748762773,-15.7883204384884));
#14683=CARTESIAN_POINT('Ctrl Pts',(19.4065533265683,-5.44501179353533,-15.7602565963632));
#14684=CARTESIAN_POINT('Ctrl Pts',(19.4439717335214,-4.54350017251043,-15.7141810578394));
#14685=CARTESIAN_POINT('Ctrl Pts',(19.4720570197304,-3.64067296657162,-15.6792823759249));
#14686=CARTESIAN_POINT('Ctrl Pts',(19.4908482971575,-2.73568903693967,-15.6558881146111));
#14687=CARTESIAN_POINT('Ctrl Pts',(19.5003166417666,-2.27969557163557,-15.6441004685155));
#14688=CARTESIAN_POINT('Ctrl Pts',(19.507423025222,-1.82315416151661,-15.6352327862101));
#14689=CARTESIAN_POINT('Ctrl Pts',(19.5121580206299,-1.36595500125495,-15.629321462494));
#14690=CARTESIAN_POINT('Ctrl Pts',(19.5160084774074,-0.994164650117414,
-15.6245144258432));
#14691=CARTESIAN_POINT('Ctrl Pts',(19.5182880791429,-0.621201496409886,
-15.6216657746395));
#14692=CARTESIAN_POINT('Ctrl Pts',(19.5189931473135,-0.249398212559946,
-15.6207845393862));
#14693=CARTESIAN_POINT('Ctrl Pts',(19.5191520725705,-0.165592227709809,
-15.6205859053464));
#14694=CARTESIAN_POINT('Ctrl Pts',(19.5192309952388,-0.0818449619717695,
-15.6204872359842));
#14695=CARTESIAN_POINT('Ctrl Pts',(19.5192298639648,0.00181722862345685,
-15.6204886455658));
#14696=CARTESIAN_POINT('Ctrl Pts',(19.5192298134397,0.00555376425672661,
-15.6204887085208));
#14697=CARTESIAN_POINT('Ctrl Pts',(19.5192296032355,0.00929028666463934,
-15.6204889710975));
#14698=CARTESIAN_POINT('Ctrl Pts',(19.5192292333076,0.0130267934217134,
-15.6204894333562));
#14699=CARTESIAN_POINT('Ctrl Pts',(19.5191393000384,0.921409940080897,-15.6206018131959));
#14700=CARTESIAN_POINT('Ctrl Pts',(19.5097011100581,1.82887707135682,-15.6324757199528));
#14701=CARTESIAN_POINT('Ctrl Pts',(19.4908797533385,2.73541348833066,-15.6559072598234));
#14702=CARTESIAN_POINT('Ctrl Pts',(19.4720583966188,3.6419499053045,-15.6793387996939));
#14703=CARTESIAN_POINT('Ctrl Pts',(19.4438538502151,4.54755559186421,-15.7143280054956));
#14704=CARTESIAN_POINT('Ctrl Pts',(19.4062538058678,5.45223695733326,-15.7606254070823));
#14705=CARTESIAN_POINT('Ctrl Pts',(19.370132545756,6.32133781845157,-15.8051019632736));
#14706=CARTESIAN_POINT('Ctrl Pts',(19.325339443103,7.18958919548238,-15.8599999935407));
#14707=CARTESIAN_POINT('Ctrl Pts',(19.2716949593314,8.05701156886618,-15.9249190639256));
#14708=CARTESIAN_POINT('Ctrl Pts',(19.2367733154138,8.62168873825368,-15.9671802714169));
#14709=CARTESIAN_POINT('Ctrl Pts',(19.1981008001052,9.1860149588975,-16.0136872060053));
#14710=CARTESIAN_POINT('Ctrl Pts',(19.1556296640198,9.75000000013389,-16.0643184011734));
#14711=CARTESIAN_POINT('Origin',(0.,9.75,0.));
#14712=CARTESIAN_POINT('Origin',(0.,10.75,0.));
#14713=CARTESIAN_POINT('',(18.3893975112944,10.75,-15.4217398231068));
#14714=CARTESIAN_POINT('',(16.4780203712833,10.75,-17.8656547184434));
#14715=CARTESIAN_POINT('Ctrl Pts',(18.3893975112944,10.75,-15.4217398231068));
#14716=CARTESIAN_POINT('Ctrl Pts',(17.7244634951049,10.75,-16.214629346884));
#14717=CARTESIAN_POINT('Ctrl Pts',(17.0876222525083,10.75,-17.0294901288799));
#14718=CARTESIAN_POINT('Ctrl Pts',(16.478020371287,10.75,-17.8656547184383));
#14719=CARTESIAN_POINT('',(4.08240831242321E-16,10.75,-25.));
#14720=CARTESIAN_POINT('Ctrl Pts',(16.4780203712861,10.75,-17.8656547184465));
#14721=CARTESIAN_POINT('Ctrl Pts',(16.4205369211924,10.75,-17.9445022924812));
#14722=CARTESIAN_POINT('Ctrl Pts',(16.3614956607445,10.75,-18.0219137128354));
#14723=CARTESIAN_POINT('Ctrl Pts',(16.3008084559825,10.75,-18.0978225947332));
#14724=CARTESIAN_POINT('Ctrl Pts',(16.2401227350897,10.75,-18.173729620575));
#14725=CARTESIAN_POINT('Ctrl Pts',(16.1778528394289,10.75,-18.2481856138866));
#14726=CARTESIAN_POINT('Ctrl Pts',(16.1143503256155,10.75,-18.321511971579));
#14727=CARTESIAN_POINT('Ctrl Pts',(15.9879798174003,10.7499999999999,-18.4674320073492));
#14728=CARTESIAN_POINT('Ctrl Pts',(15.8568594587015,10.7499999999999,-18.6089990995592));
#14729=CARTESIAN_POINT('Ctrl Pts',(15.7224917977638,10.7499999999988,-18.7475834112698));
#14730=CARTESIAN_POINT('Ctrl Pts',(15.7218180802141,10.7499999999988,-18.7482782710468));
#14731=CARTESIAN_POINT('Ctrl Pts',(15.7211442809102,10.7499999999988,-18.7489730559038));
#14732=CARTESIAN_POINT('Ctrl Pts',(15.7204704000415,10.7499999999988,-18.7496677660139));
#14733=CARTESIAN_POINT('Ctrl Pts',(15.451667324727,10.7499999999965,-19.0267793783135));
#14734=CARTESIAN_POINT('Ctrl Pts',(15.1690227653331,10.7500000000022,-19.2927577243446));
#14735=CARTESIAN_POINT('Ctrl Pts',(14.8798428323191,10.7499999999975,-19.5474336688286));
#14736=CARTESIAN_POINT('Ctrl Pts',(14.8783928927866,10.7499999999974,-19.5487106063949));
#14737=CARTESIAN_POINT('Ctrl Pts',(14.8769427885263,10.7499999999974,-19.5499872599372));
#14738=CARTESIAN_POINT('Ctrl Pts',(14.8754925204573,10.7499999999974,-19.5512636294347));
#14739=CARTESIAN_POINT('Ctrl Pts',(14.2970016154696,10.7499999999879,-20.0603889156465));
#14740=CARTESIAN_POINT('Ctrl Pts',(13.6908620621195,10.7500000000124,-20.5261584715322));
#14741=CARTESIAN_POINT('Ctrl Pts',(13.0629303706253,10.7499999999841,-20.957705974607));
#14742=CARTESIAN_POINT('Ctrl Pts',(13.0597819615603,10.7499999999839,-20.9598697259976));
#14743=CARTESIAN_POINT('Ctrl Pts',(13.0566330040481,10.7499999999838,-20.9620326166144));
#14744=CARTESIAN_POINT('Ctrl Pts',(13.0534834988268,10.7499999999836,-20.9641946476136));
#14745=CARTESIAN_POINT('Ctrl Pts',(12.4269079271698,10.7499999999561,-21.3943180206715));
#14746=CARTESIAN_POINT('Ctrl Pts',(11.7782352837989,10.7500000000018,-21.7897586824007));
#14747=CARTESIAN_POINT('Ctrl Pts',(11.1089027616845,10.7499999999977,-22.1527729443761));
#14748=CARTESIAN_POINT('Ctrl Pts',(11.103856085206,10.7499999999977,-22.1555100226993));
#14749=CARTESIAN_POINT('Ctrl Pts',(11.0988082712334,10.7499999999976,-22.1582452363645));
#14750=CARTESIAN_POINT('Ctrl Pts',(11.0937593195539,10.7499999999976,-22.1609785868902));
#14751=CARTESIAN_POINT('Ctrl Pts',(10.7597836855235,10.7499999999956,-22.341782946449));
#14752=CARTESIAN_POINT('Ctrl Pts',(10.4203659800424,10.7499999999967,-22.5145993685236));
#14753=CARTESIAN_POINT('Ctrl Pts',(10.075955307883,10.7499999999979,-22.6792702920911));
#14754=CARTESIAN_POINT('Ctrl Pts',(9.73154463572366,10.7499999999991,-22.8439412156585));
#14755=CARTESIAN_POINT('Ctrl Pts',(9.38214027285201,10.7499999999998,-23.0004669395086));
#14756=CARTESIAN_POINT('Ctrl Pts',(9.02816344904727,10.7499999999999,-23.148638564313));
#14757=CARTESIAN_POINT('Ctrl Pts',(9.02106352923122,10.7499999999999,-23.1516105290982));
#14758=CARTESIAN_POINT('Ctrl Pts',(9.01396146848508,10.7499999999999,-23.1545792568972));
#14759=CARTESIAN_POINT('Ctrl Pts',(9.00685727508312,10.7499999999999,-23.1575447426818));
#14760=CARTESIAN_POINT('Ctrl Pts',(8.69609748902353,10.75,-23.287264427359));
#14761=CARTESIAN_POINT('Ctrl Pts',(8.38265057292746,10.75,-23.4103036057306));
#14762=CARTESIAN_POINT('Ctrl Pts',(8.06678449157996,10.75,-23.5265460693149));
#14763=CARTESIAN_POINT('Ctrl Pts',(7.74909985495579,10.75,-23.6434577828062));
#14764=CARTESIAN_POINT('Ctrl Pts',(7.4289681233337,10.75,-23.7534943162534));
#14765=CARTESIAN_POINT('Ctrl Pts',(7.10667522874612,10.75,-23.8565884582872));
#14766=CARTESIAN_POINT('Ctrl Pts',(7.02075621786697,10.75,-23.8840719891367));
#14767=CARTESIAN_POINT('Ctrl Pts',(6.93468368892621,10.75,-23.911062412747));
#14768=CARTESIAN_POINT('Ctrl Pts',(6.84846321645907,10.75,-23.9375590587731));
#14769=CARTESIAN_POINT('Ctrl Pts',(6.47917928205354,10.75,-24.0510447010236));
#14770=CARTESIAN_POINT('Ctrl Pts',(6.10762958554647,10.75,-24.155334970232));
#14771=CARTESIAN_POINT('Ctrl Pts',(5.73386157021048,10.75,-24.2505804378535));
#14772=CARTESIAN_POINT('Ctrl Pts',(5.3600935548745,10.75,-24.3458259054749));
#14773=CARTESIAN_POINT('Ctrl Pts',(4.98410756392965,10.75,-24.4320267971511));
#14774=CARTESIAN_POINT('Ctrl Pts',(4.6059333896843,10.75,-24.5093375099453));
#14775=CARTESIAN_POINT('Ctrl Pts',(4.60558352323334,10.75,-24.5094090336678));
#14776=CARTESIAN_POINT('Ctrl Pts',(4.60523365489507,10.75,-24.5094805497838));
#14777=CARTESIAN_POINT('Ctrl Pts',(4.60488378466999,10.75,-24.5095520582932));
#14778=CARTESIAN_POINT('Ctrl Pts',(4.29775236332103,10.75,-24.5723253626734));
#14779=CARTESIAN_POINT('Ctrl Pts',(3.98912819460999,10.75,-24.6291799941854));
#14780=CARTESIAN_POINT('Ctrl Pts',(3.67936135400966,10.75,-24.6800307868044));
#14781=CARTESIAN_POINT('Ctrl Pts',(3.37064081951635,10.7499999999999,-24.7307098196095));
#14782=CARTESIAN_POINT('Ctrl Pts',(3.06078535062693,10.7499999999999,-24.775425478857));
#14783=CARTESIAN_POINT('Ctrl Pts',(2.75015409326968,10.7499999999996,-24.814143692227));
#14784=CARTESIAN_POINT('Ctrl Pts',(2.60693647555524,10.7499999999995,-24.8319948586814));
#14785=CARTESIAN_POINT('Ctrl Pts',(2.46355412155261,10.7499999999993,-24.8485718507124));
#14786=CARTESIAN_POINT('Ctrl Pts',(2.32004310769269,10.7499999999991,-24.8638749604557));
#14787=CARTESIAN_POINT('Ctrl Pts',(2.31835963494414,10.7499999999991,-24.8640544753761));
#14788=CARTESIAN_POINT('Ctrl Pts',(2.31667617442673,10.7499999999991,-24.8642338083549));
#14789=CARTESIAN_POINT('Ctrl Pts',(2.31499272620476,10.7499999999991,-24.8644129594266));
#14790=CARTESIAN_POINT('Ctrl Pts',(1.70961577407402,10.7499999999982,-24.9288366395314));
#14791=CARTESIAN_POINT('Ctrl Pts',(1.10236193375945,10.75,-24.9700975683441));
#14792=CARTESIAN_POINT('Ctrl Pts',(0.493954693746763,10.75,-24.9892687909964));
#14793=CARTESIAN_POINT('Ctrl Pts',(0.386484823791873,10.75,-24.9926552214493));
#14794=CARTESIAN_POINT('Ctrl Pts',(0.278978971249718,10.75,-24.9953525365432));
#14795=CARTESIAN_POINT('Ctrl Pts',(0.171441131934135,10.75,-24.9973668172451));
#14796=CARTESIAN_POINT('Ctrl Pts',(0.114302919084394,10.75,-24.9984370674957));
#14797=CARTESIAN_POINT('Ctrl Pts',(0.0571556757661779,10.75,-24.9993144879768));
#14798=CARTESIAN_POINT('Ctrl Pts',(6.03940677783316E-16,10.75,-25.));
#14799=CARTESIAN_POINT('',(-16.4780203712963,10.75,-17.8656547184255));
#14800=CARTESIAN_POINT('Ctrl Pts',(8.88178419700125E-16,10.75,-25.));
#14801=CARTESIAN_POINT('Ctrl Pts',(-0.631893351362637,10.75,-24.992420407891));
#14802=CARTESIAN_POINT('Ctrl Pts',(-1.26314073990296,10.75,-24.9608795160537));
#14803=CARTESIAN_POINT('Ctrl Pts',(-1.89206141815216,10.75,-24.9051003815217));
#14804=CARTESIAN_POINT('Ctrl Pts',(-2.03226925017558,10.75,-24.8926653133242));
#14805=CARTESIAN_POINT('Ctrl Pts',(-2.17236144346044,10.75,-24.8790258193833));
#14806=CARTESIAN_POINT('Ctrl Pts',(-2.31231938275716,10.75,-24.864179185895));
#14807=CARTESIAN_POINT('Ctrl Pts',(-2.93636235324608,10.75,-24.7979811744756));
#14808=CARTESIAN_POINT('Ctrl Pts',(-3.55773440824655,10.75,-24.7077804387484));
#14809=CARTESIAN_POINT('Ctrl Pts',(-4.17479133535945,10.75,-24.5933678196603));
#14810=CARTESIAN_POINT('Ctrl Pts',(-4.31689719651806,10.75,-24.5670190290569));
#14811=CARTESIAN_POINT('Ctrl Pts',(-4.45877423678966,10.75,-24.5393863433226));
#14812=CARTESIAN_POINT('Ctrl Pts',(-4.60040245249664,10.75,-24.5104675943794));
#14813=CARTESIAN_POINT('Ctrl Pts',(-4.60074315414983,10.75,-24.5103980272701));
#14814=CARTESIAN_POINT('Ctrl Pts',(-4.60108385438549,10.75,-24.5103284527139));
#14815=CARTESIAN_POINT('Ctrl Pts',(-4.60142455320338,10.75,-24.5102588707109));
#14816=CARTESIAN_POINT('Ctrl Pts',(-5.27342211797078,10.75,-24.3730146711527));
#14817=CARTESIAN_POINT('Ctrl Pts',(-5.93871948223922,10.75,-24.2073770139159));
#14818=CARTESIAN_POINT('Ctrl Pts',(-6.59553787934151,10.75,-24.0134739845937));
#14819=CARTESIAN_POINT('Ctrl Pts',(-7.24524697488622,10.75,-23.8216697319112));
#14820=CARTESIAN_POINT('Ctrl Pts',(-7.88666018322436,10.75,-23.6022085437364));
#14821=CARTESIAN_POINT('Ctrl Pts',(-8.51803988731519,10.75,-23.3551660550721));
#14822=CARTESIAN_POINT('Ctrl Pts',(-8.68535124885221,10.75,-23.2897014624219));
#14823=CARTESIAN_POINT('Ctrl Pts',(-8.85195793187626,10.75,-23.2222998119581));
#14824=CARTESIAN_POINT('Ctrl Pts',(-9.01782734025242,10.75,-23.1529619510151));
#14825=CARTESIAN_POINT('Ctrl Pts',(-9.01859758920051,10.75,-23.1526399662984));
#14826=CARTESIAN_POINT('Ctrl Pts',(-9.01936782291524,10.75,-23.1523179395502));
#14827=CARTESIAN_POINT('Ctrl Pts',(-9.02013804139308,10.75,-23.1519958707704));
#14828=CARTESIAN_POINT('Ctrl Pts',(-9.73165202060789,10.75,-22.8544745236052));
#14829=CARTESIAN_POINT('Ctrl Pts',(-10.4267722486049,10.75,-22.5225508541856));
#14830=CARTESIAN_POINT('Ctrl Pts',(-11.1049075898659,10.75,-22.1549367784204));
#14831=CARTESIAN_POINT('Ctrl Pts',(-11.1050463232738,10.75,-22.1548615716727));
#14832=CARTESIAN_POINT('Ctrl Pts',(-11.1051850560842,10.75,-22.1547863633518));
#14833=CARTESIAN_POINT('Ctrl Pts',(-11.105323788297,10.75,-22.1547111534577));
#14834=CARTESIAN_POINT('Ctrl Pts',(-11.4745607689731,10.75,-21.9545393718602));
#14835=CARTESIAN_POINT('Ctrl Pts',(-11.8388346073417,10.7499999999999,-21.7436243514817));
#14836=CARTESIAN_POINT('Ctrl Pts',(-12.196154206087,10.7499999999996,-21.5227465720604));
#14837=CARTESIAN_POINT('Ctrl Pts',(-12.4953092091938,10.7499999999994,-21.3378233464075));
#14838=CARTESIAN_POINT('Ctrl Pts',(-12.7895904599738,10.7499999999992,-21.1459156366744));
#14839=CARTESIAN_POINT('Ctrl Pts',(-13.0778256121902,10.7499999999995,-20.9474537314311));
#14840=CARTESIAN_POINT('Ctrl Pts',(-13.0784156919486,10.7499999999995,-20.9470474369448));
#14841=CARTESIAN_POINT('Ctrl Pts',(-13.0790057477787,10.7499999999995,-20.9466411152569));
#14842=CARTESIAN_POINT('Ctrl Pts',(-13.0795957796768,10.7499999999995,-20.9462347663615));
#14843=CARTESIAN_POINT('Ctrl Pts',(-13.7123512511636,10.7500000000004,-20.5104625857627));
#14844=CARTESIAN_POINT('Ctrl Pts',(-14.3179636229281,10.7499999999992,-20.0431451182884));
#14845=CARTESIAN_POINT('Ctrl Pts',(-14.8908179209084,10.7499999999998,-19.5377573520794));
#14846=CARTESIAN_POINT('Ctrl Pts',(-14.891085008639,10.7499999999998,-19.5375217199615));
#14847=CARTESIAN_POINT('Ctrl Pts',(-14.8913520892958,10.7499999999998,-19.5372860796229));
#14848=CARTESIAN_POINT('Ctrl Pts',(-14.8916191628765,10.7499999999998,-19.5370504310607));
#14849=CARTESIAN_POINT('Ctrl Pts',(-15.1780311374702,10.7500000000001,-19.284338912937));
#14850=CARTESIAN_POINT('Ctrl Pts',(-15.4563063216582,10.7499999999999,-19.022171134779));
#14851=CARTESIAN_POINT('Ctrl Pts',(-15.7232342401124,10.75,-18.7468157768201));
#14852=CARTESIAN_POINT('Ctrl Pts',(-15.7233586926443,10.75,-18.746687395077));
#14853=CARTESIAN_POINT('Ctrl Pts',(-15.7234831427055,10.75,-18.7465590104624));
#14854=CARTESIAN_POINT('Ctrl Pts',(-15.7236075902949,10.75,-18.7464306229752));
#14855=CARTESIAN_POINT('Ctrl Pts',(-15.8570635065209,10.75,-18.6087496134541));
#14856=CARTESIAN_POINT('Ctrl Pts',(-15.9876823298412,10.75,-18.4677594530587));
#14857=CARTESIAN_POINT('Ctrl Pts',(-16.1140602454271,10.75,-18.3218466327017));
#14858=CARTESIAN_POINT('Ctrl Pts',(-16.1773091023549,10.75,-18.2488210644612));
#14859=CARTESIAN_POINT('Ctrl Pts',(-16.2394660158614,10.75,-18.1745279741513));
#14860=CARTESIAN_POINT('Ctrl Pts',(-16.300199402483,10.75,-18.0985842575497));
#14861=CARTESIAN_POINT('Ctrl Pts',(-16.3609359034934,10.75,-18.0226366465785));
#14862=CARTESIAN_POINT('Ctrl Pts',(-16.4201884779383,10.75,-17.94498023769));
#14863=CARTESIAN_POINT('Ctrl Pts',(-16.4780203712963,10.75,-17.8656547184255));
#14864=CARTESIAN_POINT('',(-18.3893975112961,10.75,-15.4217398231048));
#14865=CARTESIAN_POINT('Ctrl Pts',(-16.4780203712963,10.75,-17.8656547184255));
#14866=CARTESIAN_POINT('Ctrl Pts',(-17.0876222525177,10.75,-17.0294901288675));
#14867=CARTESIAN_POINT('Ctrl Pts',(-17.7244634951036,10.75,-16.2146293468709));
#14868=CARTESIAN_POINT('Ctrl Pts',(-18.3893975112961,10.75,-15.4217398231048));
#14869=CARTESIAN_POINT('Origin',(0.,10.75,0.));
#14870=CARTESIAN_POINT('Origin',(0.,-10.75,0.));
#14871=CARTESIAN_POINT('',(18.3893975112955,-10.75,-15.4217398231056));
#14872=CARTESIAN_POINT('',(-18.3893975112944,-10.75,-15.4217398231068));
#14873=CARTESIAN_POINT('Origin',(0.,-10.75,0.));
#14874=CARTESIAN_POINT('',(-16.4780203712963,-10.75,-17.8656547184255));
#14875=CARTESIAN_POINT('Ctrl Pts',(-18.3893975112945,-10.75,-15.4217398231068));
#14876=CARTESIAN_POINT('Ctrl Pts',(-17.7244634951085,-10.75,-16.2146293468773));
#14877=CARTESIAN_POINT('Ctrl Pts',(-17.0876222525172,-10.75,-17.0294901288682));
#14878=CARTESIAN_POINT('Ctrl Pts',(-16.4780203712963,-10.75,-17.8656547184255));
#14879=CARTESIAN_POINT('',(0.,-10.75,-25.));
#14880=CARTESIAN_POINT('Ctrl Pts',(-16.4780203712963,-10.75,-17.8656547184255));
#14881=CARTESIAN_POINT('Ctrl Pts',(-16.4201493510906,-10.75,-17.9450339063976));
#14882=CARTESIAN_POINT('Ctrl Pts',(-16.360820089721,-10.75,-18.0227902935397));
#14883=CARTESIAN_POINT('Ctrl Pts',(-16.2999644844546,-10.75,-18.0988780799066));
#14884=CARTESIAN_POINT('Ctrl Pts',(-16.2391116407599,-10.75,-18.1749624134795));
#14885=CARTESIAN_POINT('Ctrl Pts',(-16.1767937814564,-10.75,-18.2494353360594));
#14886=CARTESIAN_POINT('Ctrl Pts',(-16.1133493511491,-10.7499999999999,
-18.3226679211682));
#14887=CARTESIAN_POINT('Ctrl Pts',(-15.9876961209516,-10.7499999999997,
-18.467706828919));
#14888=CARTESIAN_POINT('Ctrl Pts',(-15.857743766938,-10.7499999999996,-18.6080126030319));
#14889=CARTESIAN_POINT('Ctrl Pts',(-15.724890365442,-10.7499999999952,-18.7451110957646));
#14890=CARTESIAN_POINT('Ctrl Pts',(-15.7235857860446,-10.7499999999952,
-18.7464573606476));
#14891=CARTESIAN_POINT('Ctrl Pts',(-15.7222809262691,-10.7499999999952,
-18.7478033165219));
#14892=CARTESIAN_POINT('Ctrl Pts',(-15.7209757874349,-10.7499999999951,
-18.749148964841));
#14893=CARTESIAN_POINT('Ctrl Pts',(-15.4551501413287,-10.7499999999865,
-19.02322542666));
#14894=CARTESIAN_POINT('Ctrl Pts',(-15.177768808186,-10.750000000015,-19.2845652736965));
#14895=CARTESIAN_POINT('Ctrl Pts',(-14.8920303997885,-10.7499999999828,
-19.5366947908981));
#14896=CARTESIAN_POINT('Ctrl Pts',(-14.8892245807239,-10.7499999999825,
-19.5391705861897));
#14897=CARTESIAN_POINT('Ctrl Pts',(-14.8864179605812,-10.7499999999821,
-19.5416454867311));
#14898=CARTESIAN_POINT('Ctrl Pts',(-14.8836105423087,-10.7499999999818,
-19.5441194959428));
#14899=CARTESIAN_POINT('Ctrl Pts',(-14.5626185949198,-10.7499999999458,
-19.826990432017));
#14900=CARTESIAN_POINT('Ctrl Pts',(-14.2310028354858,-10.7499999999655,
-20.0982233034529));
#14901=CARTESIAN_POINT('Ctrl Pts',(-13.8898057176469,-10.7499999999759,
-20.358849639778));
#14902=CARTESIAN_POINT('Ctrl Pts',(-13.6232076047817,-10.749999999984,-20.5624928881951));
#14903=CARTESIAN_POINT('Ctrl Pts',(-13.3507587393612,-10.7499999999906,
-20.7596595859911));
#14904=CARTESIAN_POINT('Ctrl Pts',(-13.0729414760137,-10.7499999999578,
-20.9508259365018));
#14905=CARTESIAN_POINT('Ctrl Pts',(-13.0667248663834,-10.7499999999571,
-20.9551035921135));
#14906=CARTESIAN_POINT('Ctrl Pts',(-13.0605051235057,-10.7499999999564,
-20.9593785431024));
#14907=CARTESIAN_POINT('Ctrl Pts',(-13.0542822577895,-10.7499999999557,
-20.9636507892648));
#14908=CARTESIAN_POINT('Ctrl Pts',(-12.8276147931846,-10.7499999999303,
-21.1192670679927));
#14909=CARTESIAN_POINT('Ctrl Pts',(-12.5979370989195,-10.7499999999392,
-21.2704240340891));
#14910=CARTESIAN_POINT('Ctrl Pts',(-12.365564761205,-10.7499999999554,-21.4170600650478));
#14911=CARTESIAN_POINT('Ctrl Pts',(-12.1277109810229,-10.749999999972,-21.5671551005305));
#14912=CARTESIAN_POINT('Ctrl Pts',(-11.8870339411185,-10.7499999999879,
-21.7125134564541));
#14913=CARTESIAN_POINT('Ctrl Pts',(-11.6438956109018,-10.7499999999931,
-21.8531191015724));
#14914=CARTESIAN_POINT('Ctrl Pts',(-11.4634201196036,-10.749999999997,-21.9574871494215));
#14915=CARTESIAN_POINT('Ctrl Pts',(-11.2815890286072,-10.7499999999978,
-22.0592376569264));
#14916=CARTESIAN_POINT('Ctrl Pts',(-11.0985582855635,-10.7499999999957,
-22.158380780832));
#14917=CARTESIAN_POINT('Ctrl Pts',(-11.0924596370167,-10.7499999999956,
-22.1616842644898));
#14918=CARTESIAN_POINT('Ctrl Pts',(-11.0863595888253,-10.7499999999955,
-22.1649848892748));
#14919=CARTESIAN_POINT('Ctrl Pts',(-11.0802581423629,-10.7499999999955,
-22.168282658021));
#14920=CARTESIAN_POINT('Ctrl Pts',(-10.4089256243362,-10.7499999999882,
-22.5311309448827));
#14921=CARTESIAN_POINT('Ctrl Pts',(-9.7205987275344,-10.7500000000003,-22.8592637055778));
#14922=CARTESIAN_POINT('Ctrl Pts',(-9.0158247965325,-10.7499999999996,-23.1537997929039));
#14923=CARTESIAN_POINT('Ctrl Pts',(-9.01167151414176,-10.7499999999996,
-23.1555355148015));
#14924=CARTESIAN_POINT('Ctrl Pts',(-9.00751768000453,-10.7499999999996,
-23.1572700615062));
#14925=CARTESIAN_POINT('Ctrl Pts',(-9.0033632951643,-10.7499999999996,-23.1590034328983));
#14926=CARTESIAN_POINT('Ctrl Pts',(-8.71652133934044,-10.7499999999993,
-23.2786850847921));
#14927=CARTESIAN_POINT('Ctrl Pts',(-8.42699173100363,-10.7499999999994,
-23.3927719037949));
#14928=CARTESIAN_POINT('Ctrl Pts',(-8.13515127880793,-10.7499999999996,
-23.5011251356437));
#14929=CARTESIAN_POINT('Ctrl Pts',(-7.84327400478459,-10.7499999999998,
-23.6094920385378));
#14930=CARTESIAN_POINT('Ctrl Pts',(-7.549085393291,-10.7499999999999,-23.7121238639655));
#14931=CARTESIAN_POINT('Ctrl Pts',(-7.25298387983204,-10.7499999999999,
-23.8089293460351));
#14932=CARTESIAN_POINT('Ctrl Pts',(-7.11519835173526,-10.7499999999999,
-23.8539760407103));
#14933=CARTESIAN_POINT('Ctrl Pts',(-6.97699891083036,-10.7499999999999,
-23.8977618104917));
#14934=CARTESIAN_POINT('Ctrl Pts',(-6.8384272034732,-10.7499999999999,-23.9402810023015));
#14935=CARTESIAN_POINT('Ctrl Pts',(-6.83474659856658,-10.7499999999999,
-23.9414103551037));
#14936=CARTESIAN_POINT('Ctrl Pts',(-6.83106554363849,-10.7499999999999,
-23.9425388719248));
#14937=CARTESIAN_POINT('Ctrl Pts',(-6.8273840387324,-10.7499999999999,-23.9436665526118));
#14938=CARTESIAN_POINT('Ctrl Pts',(-6.09245639192048,-10.7499999999998,
-24.1687820243408));
#14939=CARTESIAN_POINT('Ctrl Pts',(-5.34937233574249,-10.7500000000001,
-24.3576172870069));
#14940=CARTESIAN_POINT('Ctrl Pts',(-4.59800314866546,-10.7499999999998,
-24.5109577875767));
#14941=CARTESIAN_POINT('Ctrl Pts',(-4.59383852606573,-10.7499999999998,
-24.5118077097257));
#14942=CARTESIAN_POINT('Ctrl Pts',(-4.58967362230916,-10.7499999999998,
-24.5126565466446));
#14943=CARTESIAN_POINT('Ctrl Pts',(-4.585508438488,-10.7499999999998,-24.5135042982985));
#14944=CARTESIAN_POINT('Ctrl Pts',(-4.23868940594231,-10.7499999999997,
-24.5840933577707));
#14945=CARTESIAN_POINT('Ctrl Pts',(-3.8899125665333,-10.7500000007398,-24.6471311889045));
#14946=CARTESIAN_POINT('Ctrl Pts',(-3.53980407982917,-10.7499999989718,
-24.7025066732745));
#14947=CARTESIAN_POINT('Ctrl Pts',(-3.20653186901385,-10.7499999972888,
-24.75521922039));
#14948=CARTESIAN_POINT('Ctrl Pts',(-2.87205245696364,-10.7499999917215,
-24.8009885036796));
#14949=CARTESIAN_POINT('Ctrl Pts',(-2.53691289996853,-10.7499999750427,
-24.8397660990454));
#14950=CARTESIAN_POINT('Ctrl Pts',(-2.4616811610157,-10.7499999712987,-24.8484708486665));
#14951=CARTESIAN_POINT('Ctrl Pts',(-2.38641620209076,-10.7499999670649,
-24.8568234837151));
#14952=CARTESIAN_POINT('Ctrl Pts',(-2.3111242988961,-10.7499999624566,-24.8648238156686));
#14953=CARTESIAN_POINT('Ctrl Pts',(-1.9274828828541,-10.7499999389757,-24.905588606426));
#14954=CARTESIAN_POINT('Ctrl Pts',(-1.54279117061237,-10.7499999002255,
-24.9372493539721));
#14955=CARTESIAN_POINT('Ctrl Pts',(-1.15724985369559,-10.7499999035675,
-24.95979124596));
#14956=CARTESIAN_POINT('Ctrl Pts',(-1.01440345966211,-10.7499999048058,
-24.9681432119981));
#14957=CARTESIAN_POINT('Ctrl Pts',(-0.871510359726857,-10.7499999153928,
-24.9752345292119));
#14958=CARTESIAN_POINT('Ctrl Pts',(-0.728466427406036,-10.7499999352919,
-24.9810597553893));
#14959=CARTESIAN_POINT('Ctrl Pts',(-0.678473124110684,-10.7499999422465,
-24.9830956494977));
#14960=CARTESIAN_POINT('Ctrl Pts',(-0.62846143143074,-10.7499999499415,
-24.9849773637484));
#14961=CARTESIAN_POINT('Ctrl Pts',(-0.578426969045136,-10.74999995742,-24.9867061497547));
#14962=CARTESIAN_POINT('Ctrl Pts',(-0.481828888224218,-10.7499999718582,
-24.9900437974959));
#14963=CARTESIAN_POINT('Ctrl Pts',(-0.385082356737824,-10.7499999859661,
-24.99280714982));
#14964=CARTESIAN_POINT('Ctrl Pts',(-0.288554981890424,-10.7499999930961,
-24.9950091292011));
#14965=CARTESIAN_POINT('Ctrl Pts',(-0.192027607043022,-10.750000000226,
-24.9972111085822));
#14966=CARTESIAN_POINT('Ctrl Pts',(-0.0957196018798722,-10.75,-24.9988519611205));
#14967=CARTESIAN_POINT('Ctrl Pts',(-5.35841952801743E-40,-10.75,-25.));
#14968=CARTESIAN_POINT('',(16.4780203712966,-10.75,-17.8656547184251));
#14969=CARTESIAN_POINT('Ctrl Pts',(0.,-10.75,-25.));
#14970=CARTESIAN_POINT('Ctrl Pts',(0.63189335421386,-10.75,-24.9924204078283));
#14971=CARTESIAN_POINT('Ctrl Pts',(1.26314074559829,-10.75,-24.9608795157349));
#14972=CARTESIAN_POINT('Ctrl Pts',(1.89206142666417,-10.75,-24.905100380736));
#14973=CARTESIAN_POINT('Ctrl Pts',(2.03226925584466,-10.75,-24.8926653127422));
#14974=CARTESIAN_POINT('Ctrl Pts',(2.17236144629095,-10.75,-24.8790258190543));
#14975=CARTESIAN_POINT('Ctrl Pts',(2.31231938275462,-10.75,-24.8641791858681));
#14976=CARTESIAN_POINT('Ctrl Pts',(2.93636235981245,-10.75,-24.7979811737587));
#14977=CARTESIAN_POINT('Ctrl Pts',(3.55773442132701,-10.75,-24.7077804368426));
#14978=CARTESIAN_POINT('Ctrl Pts',(4.17479135484504,-10.75,-24.5933678160459));
#14979=CARTESIAN_POINT('Ctrl Pts',(4.3168972094877,-10.75,-24.5670190265306));
#14980=CARTESIAN_POINT('Ctrl Pts',(4.4587742432633,-10.75,-24.5393863420014));
#14981=CARTESIAN_POINT('Ctrl Pts',(4.60040245249694,-10.75,-24.5104675943802));
#14982=CARTESIAN_POINT('Ctrl Pts',(4.60074315415015,-10.75,-24.5103980272708));
#14983=CARTESIAN_POINT('Ctrl Pts',(4.60108385438582,-10.75,-24.5103284527146));
#14984=CARTESIAN_POINT('Ctrl Pts',(4.60142455320371,-10.75,-24.5102588707117));
#14985=CARTESIAN_POINT('Ctrl Pts',(5.27342211902175,-10.75,-24.3730146709398));
#14986=CARTESIAN_POINT('Ctrl Pts',(5.93871948432097,-10.75,-24.2073770134027));
#14987=CARTESIAN_POINT('Ctrl Pts',(6.59553788242437,-10.75,-24.0134739836911));
#14988=CARTESIAN_POINT('Ctrl Pts',(7.24524697964132,-10.75,-23.8216697304222));
#14989=CARTESIAN_POINT('Ctrl Pts',(7.88666018960527,-10.75,-23.6022085415156));
#14990=CARTESIAN_POINT('Ctrl Pts',(8.51803989526079,-10.75,-23.3551660519723));
#14991=CARTESIAN_POINT('Ctrl Pts',(8.68535125412791,-10.75,-23.2897014602961));
#14992=CARTESIAN_POINT('Ctrl Pts',(8.85195793450375,-10.75,-23.2222998108673));
#14993=CARTESIAN_POINT('Ctrl Pts',(9.01782734025492,-10.75,-23.1529619510203));
#14994=CARTESIAN_POINT('Ctrl Pts',(9.01859758920301,-10.75,-23.1526399663036));
#14995=CARTESIAN_POINT('Ctrl Pts',(9.01936782291774,-10.75,-23.1523179395554));
#14996=CARTESIAN_POINT('Ctrl Pts',(9.02013804139559,-10.75,-23.1519958707756));
#14997=CARTESIAN_POINT('Ctrl Pts',(9.73165202060862,-10.75,-22.8544745236056));
#14998=CARTESIAN_POINT('Ctrl Pts',(10.4267722486079,-10.75,-22.5225508541904));
#14999=CARTESIAN_POINT('Ctrl Pts',(11.1049075898677,-10.75,-22.1549367784228));
#15000=CARTESIAN_POINT('Ctrl Pts',(11.1050463232755,-10.75,-22.1548615716751));
#15001=CARTESIAN_POINT('Ctrl Pts',(11.1051850560859,-10.75,-22.1547863633542));
#15002=CARTESIAN_POINT('Ctrl Pts',(11.1053237882988,-10.75,-22.1547111534601));
#15003=CARTESIAN_POINT('Ctrl Pts',(11.4745607700401,-10.75,-21.9545393712836));
#15004=CARTESIAN_POINT('Ctrl Pts',(11.8388346094455,-10.7499999999999,-21.7436243502645));
#15005=CARTESIAN_POINT('Ctrl Pts',(12.1961542091821,-10.7499999999996,-21.5227465701481));
#15006=CARTESIAN_POINT('Ctrl Pts',(12.4953092112239,-10.7499999999994,-21.3378233450845));
#15007=CARTESIAN_POINT('Ctrl Pts',(12.7895904609685,-10.7499999999992,-21.1459156359909));
#15008=CARTESIAN_POINT('Ctrl Pts',(13.0778256121919,-10.7499999999995,-20.9474537314328));
#15009=CARTESIAN_POINT('Ctrl Pts',(13.0784156919504,-10.7499999999995,-20.9470474369465));
#15010=CARTESIAN_POINT('Ctrl Pts',(13.0790057477804,-10.7499999999995,-20.9466411152586));
#15011=CARTESIAN_POINT('Ctrl Pts',(13.0795957796785,-10.7499999999995,-20.9462347663633));
#15012=CARTESIAN_POINT('Ctrl Pts',(13.712351251167,-10.7500000000004,-20.5104625857665));
#15013=CARTESIAN_POINT('Ctrl Pts',(14.3179636229283,-10.7499999999992,-20.043145118288));
#15014=CARTESIAN_POINT('Ctrl Pts',(14.8908179209099,-10.7499999999998,-19.5377573520803));
#15015=CARTESIAN_POINT('Ctrl Pts',(14.8910850086404,-10.7499999999998,-19.5375217199623));
#15016=CARTESIAN_POINT('Ctrl Pts',(14.8913520892973,-10.7499999999998,-19.5372860796237));
#15017=CARTESIAN_POINT('Ctrl Pts',(14.8916191628779,-10.7499999999998,-19.5370504310615));
#15018=CARTESIAN_POINT('Ctrl Pts',(15.1780311374723,-10.7500000000001,-19.2843389129384));
#15019=CARTESIAN_POINT('Ctrl Pts',(15.4563063216585,-10.7499999999999,-19.0221711347786));
#15020=CARTESIAN_POINT('Ctrl Pts',(15.723234240113,-10.75,-18.7468157768199));
#15021=CARTESIAN_POINT('Ctrl Pts',(15.7233586926449,-10.75,-18.7466873950767));
#15022=CARTESIAN_POINT('Ctrl Pts',(15.7234831427061,-10.75,-18.7465590104622));
#15023=CARTESIAN_POINT('Ctrl Pts',(15.7236075902955,-10.75,-18.746430622975));
#15024=CARTESIAN_POINT('Ctrl Pts',(15.8570635065216,-10.75,-18.6087496134539));
#15025=CARTESIAN_POINT('Ctrl Pts',(15.9876823298417,-10.75,-18.4677594530583));
#15026=CARTESIAN_POINT('Ctrl Pts',(16.1140602454275,-10.75,-18.3218466327013));
#15027=CARTESIAN_POINT('Ctrl Pts',(16.1773091023553,-10.75,-18.2488210644609));
#15028=CARTESIAN_POINT('Ctrl Pts',(16.2394660158614,-10.75,-18.1745279741503));
#15029=CARTESIAN_POINT('Ctrl Pts',(16.3001994024834,-10.75,-18.0985842575493));
#15030=CARTESIAN_POINT('Ctrl Pts',(16.360935903494,-10.75,-18.0226366465788));
#15031=CARTESIAN_POINT('Ctrl Pts',(16.4201884779384,-10.75,-17.9449802376892));
#15032=CARTESIAN_POINT('Ctrl Pts',(16.4780203712966,-10.75,-17.8656547184251));
#15033=CARTESIAN_POINT('Ctrl Pts',(16.4780203712966,-10.75,-17.8656547184251));
#15034=CARTESIAN_POINT('Ctrl Pts',(17.0876222525178,-10.75,-17.0294901288675));
#15035=CARTESIAN_POINT('Ctrl Pts',(17.7244634951146,-10.75,-16.2146293468808));
#15036=CARTESIAN_POINT('Ctrl Pts',(18.3893975112954,-10.75,-15.4217398231056));
#15037=CARTESIAN_POINT('',(-2.44929359829471E-15,-10.75,20.));
#15038=CARTESIAN_POINT('Origin',(0.,-10.75,0.));
#15039=CARTESIAN_POINT('Origin',(0.,0.,25.002));
#15040=CARTESIAN_POINT('',(10.75,0.,-61.5));
#15041=CARTESIAN_POINT('Origin',(0.,0.,-61.5));
#15042=CARTESIAN_POINT('',(10.7499999978076,1.45695088265319E-14,-40.6132670239265));
#15043=CARTESIAN_POINT('',(10.75,-1.3164953090834E-15,25.002));
#15044=CARTESIAN_POINT('',(10.5060622858799,-2.277093596059,-42.0119030751999));
#15045=CARTESIAN_POINT('Ctrl Pts',(10.7499999978076,2.23887749120318E-14,
-40.6132670239265));
#15046=CARTESIAN_POINT('Ctrl Pts',(10.7499999122695,-0.0543484520734741,
-40.6132674463034));
#15047=CARTESIAN_POINT('Ctrl Pts',(10.7495859465627,-0.108343313907444,
-40.6157107158717));
#15048=CARTESIAN_POINT('Ctrl Pts',(10.7487784221861,-0.161956425874147,
-40.620473106121));
#15049=CARTESIAN_POINT('Ctrl Pts',(10.748135179199,-0.204662577278424,-40.6242666437757));
#15050=CARTESIAN_POINT('Ctrl Pts',(10.7472420423001,-0.247126965572841,
-40.6295327410255));
#15051=CARTESIAN_POINT('Ctrl Pts',(10.7461054443956,-0.289340245956811,
-40.6362316036066));
#15052=CARTESIAN_POINT('Ctrl Pts',(10.7456145340568,-0.307572670717383,
-40.6391249231231));
#15053=CARTESIAN_POINT('Ctrl Pts',(10.7450782430497,-0.325766720886662,
-40.6422852991148));
#15054=CARTESIAN_POINT('Ctrl Pts',(10.7444969181079,-0.343927986990267,
-40.6457102653304));
#15055=CARTESIAN_POINT('Ctrl Pts',(10.7431102516456,-0.387249057198522,
-40.6538800262404));
#15056=CARTESIAN_POINT('Ctrl Pts',(10.7414636104447,-0.430474944517902,
-40.6635775017438));
#15057=CARTESIAN_POINT('Ctrl Pts',(10.7395706012187,-0.473417805392778,
-40.6747168887078));
#15058=CARTESIAN_POINT('Ctrl Pts',(10.7380019900666,-0.509001705115955,
-40.6839473596321));
#15059=CARTESIAN_POINT('Ctrl Pts',(10.7362643862015,-0.544391317906246,
-40.6941668777214));
#15060=CARTESIAN_POINT('Ctrl Pts',(10.7343701126333,-0.579481048012099,
-40.7052999616701));
#15061=CARTESIAN_POINT('Ctrl Pts',(10.7325718074294,-0.612793049673637,
-40.715869017342));
#15062=CARTESIAN_POINT('Ctrl Pts',(10.7306324527749,-0.645834797347597,
-40.727261544876));
#15063=CARTESIAN_POINT('Ctrl Pts',(10.7285656648372,-0.678516863957403,
-40.7393930149516));
#15064=CARTESIAN_POINT('Ctrl Pts',(10.7249857341197,-0.735126219971907,
-40.7604062120877));
#15065=CARTESIAN_POINT('Ctrl Pts',(10.7210297007888,-0.790581697174948,
-40.7836007783321));
#15066=CARTESIAN_POINT('Ctrl Pts',(10.7167394974661,-0.844993427083508,
-40.8087109236785));
#15067=CARTESIAN_POINT('Ctrl Pts',(10.7123146364162,-0.901112992104639,
-40.8346092076849));
#15068=CARTESIAN_POINT('Ctrl Pts',(10.7075342933432,-0.956122257581554,
-40.8625453016496));
#15069=CARTESIAN_POINT('Ctrl Pts',(10.7024356672764,-1.01013949976628,-40.8922833787714));
#15070=CARTESIAN_POINT('Ctrl Pts',(10.6978560693835,-1.05865791340333,-40.918994189398));
#15071=CARTESIAN_POINT('Ctrl Pts',(10.6930195520167,-1.10637595385721,-40.9471596883995));
#15072=CARTESIAN_POINT('Ctrl Pts',(10.6879474115916,-1.15337770355406,-40.9766442613547));
#15073=CARTESIAN_POINT('Ctrl Pts',(10.6831241063421,-1.1980735847896,-41.0046823446087));
#15074=CARTESIAN_POINT('Ctrl Pts',(10.6780884706721,-1.24212147909129,-41.0339143291386));
#15075=CARTESIAN_POINT('Ctrl Pts',(10.6728535582484,-1.28559258333327,-41.0642464718845));
#15076=CARTESIAN_POINT('Ctrl Pts',(10.6660476352044,-1.34210947724856,-41.1036813683216));
#15077=CARTESIAN_POINT('Ctrl Pts',(10.658945115275,-1.39731842014561,-41.1447431707096));
#15078=CARTESIAN_POINT('Ctrl Pts',(10.6515892046568,-1.45131987859543,-41.1871531562581));
#15079=CARTESIAN_POINT('Ctrl Pts',(10.6440807744717,-1.50644101881918,-41.2304424826469));
#15080=CARTESIAN_POINT('Ctrl Pts',(10.6363083207675,-1.56030407412022,-41.275136692109));
#15081=CARTESIAN_POINT('Ctrl Pts',(10.6283098169498,-1.61301335515717,-41.3209937151806));
#15082=CARTESIAN_POINT('Ctrl Pts',(10.6200706514067,-1.66730857111461,-41.3682305000857));
#15083=CARTESIAN_POINT('Ctrl Pts',(10.6115916232549,-1.72037953278926,-41.416701263838));
#15084=CARTESIAN_POINT('Ctrl Pts',(10.6029060066273,-1.77233769176879,-41.466195898445));
#15085=CARTESIAN_POINT('Ctrl Pts',(10.6005973086165,-1.78614853599859,-41.4793519205634));
#15086=CARTESIAN_POINT('Ctrl Pts',(10.5982739708202,-1.79988074355578,-41.4925805664047));
#15087=CARTESIAN_POINT('Ctrl Pts',(10.5959365250946,-1.81353637906657,-41.5058784916094));
#15088=CARTESIAN_POINT('Ctrl Pts',(10.5866048558053,-1.8680530992313,-41.5589671425614));
#15089=CARTESIAN_POINT('Ctrl Pts',(10.5770362062685,-1.92142430401211,-41.6132278236985));
#15090=CARTESIAN_POINT('Ctrl Pts',(10.5672567498948,-1.97377158735742,-41.6684916149444));
#15091=CARTESIAN_POINT('Ctrl Pts',(10.5571324670662,-2.02796465102488,-41.7257040234229));
#15092=CARTESIAN_POINT('Ctrl Pts',(10.5467822523826,-2.08106030959691,-41.7839916348728));
#15093=CARTESIAN_POINT('Ctrl Pts',(10.5362259798091,-2.13319086452431,-41.8432233948788));
#15094=CARTESIAN_POINT('Ctrl Pts',(10.5263487812712,-2.18196791507197,-41.8986448373681));
#15095=CARTESIAN_POINT('Ctrl Pts',(10.5162910689449,-2.22990000148053,-41.9548936385444));
#15096=CARTESIAN_POINT('Ctrl Pts',(10.50606228588,-2.27709359605839,-42.0119030751991));
#15097=CARTESIAN_POINT('Ctrl Pts',(10.5060622858799,-2.27709359605899,-42.0119030751999));
#15098=CARTESIAN_POINT('Ctrl Pts',(10.490385853827,-2.3494215723234,-42.0992746181432));
#15099=CARTESIAN_POINT('Ctrl Pts',(10.4736968030171,-2.42282523877563,-42.1850875945437));
#15100=CARTESIAN_POINT('Ctrl Pts',(10.4558750724626,-2.49744213414836,-42.2692654755833));
#15101=CARTESIAN_POINT('Ctrl Pts',(10.4383088491055,-2.57098925945792,-42.3522365122926));
#15102=CARTESIAN_POINT('Ctrl Pts',(10.4196422455777,-2.64571509969582,-42.4336189546246));
#15103=CARTESIAN_POINT('Ctrl Pts',(10.3997435370924,-2.72174811639428,-42.5132910671944));
#15104=CARTESIAN_POINT('Ctrl Pts',(10.3794106775262,-2.79944002549812,-42.5947014701569));
#15105=CARTESIAN_POINT('Ctrl Pts',(10.3577915447461,-2.87849682700923,-42.6743263557515));
#15106=CARTESIAN_POINT('Ctrl Pts',(10.3347260481738,-2.95905154512446,-42.7519828652624));
#15107=CARTESIAN_POINT('Ctrl Pts',(10.3116605516015,-3.0396062632397,-42.8296393747733));
#15108=CARTESIAN_POINT('Ctrl Pts',(10.2871488217403,-3.12165894470907,-42.9053275688886));
#15109=CARTESIAN_POINT('Ctrl Pts',(10.2610091614508,-3.20533788993066,-42.978810037564));
#15110=CARTESIAN_POINT('Ctrl Pts',(10.2369004525664,-3.28251530186928,-43.0465832000986));
#15111=CARTESIAN_POINT('Ctrl Pts',(10.2114051900379,-3.36107882835082,-43.1124719480028));
#15112=CARTESIAN_POINT('Ctrl Pts',(10.1843579213735,-3.44112785944755,-43.1762137875122));
#15113=CARTESIAN_POINT('Ctrl Pts',(10.181433339465,-3.44978344500928,-43.1831061001133));
#15114=CARTESIAN_POINT('Ctrl Pts',(10.1784905933372,-3.45845639526026,-43.1899732648885));
#15115=CARTESIAN_POINT('Ctrl Pts',(10.1755294601893,-3.46714683325529,-43.1968149158648));
#15116=CARTESIAN_POINT('Ctrl Pts',(10.1534379069397,-3.53198190285161,-43.2478570977958));
#15117=CARTESIAN_POINT('Ctrl Pts',(10.1302922806719,-3.59787987795324,-43.2975482341483));
#15118=CARTESIAN_POINT('Ctrl Pts',(10.1060391066297,-3.66476105295717,-43.3456209213258));
#15119=CARTESIAN_POINT('Ctrl Pts',(10.0774789910471,-3.7435191604564,-43.4022304809556));
#15120=CARTESIAN_POINT('Ctrl Pts',(10.047380801416,-3.82362678339096,-43.4565636983405));
#15121=CARTESIAN_POINT('Ctrl Pts',(10.0157618677699,-3.90473120949845,-43.5081008020532));
#15122=CARTESIAN_POINT('Ctrl Pts',(9.98816221636101,-3.97552594006497,-43.5530866992061));
#15123=CARTESIAN_POINT('Ctrl Pts',(9.95940424480961,-4.04707940129396,-43.5959421869557));
#15124=CARTESIAN_POINT('Ctrl Pts',(9.92951515284022,-4.1191296203893,-43.6363292172926));
#15125=CARTESIAN_POINT('Ctrl Pts',(9.92514363536094,-4.12966753811807,-43.6422361417731));
#15126=CARTESIAN_POINT('Ctrl Pts',(9.92074740166525,-4.14021801800802,-43.6480926845481));
#15127=CARTESIAN_POINT('Ctrl Pts',(9.91632635362652,-4.15078073859809,-43.653898081324));
#15128=CARTESIAN_POINT('Ctrl Pts',(9.8823854072034,-4.23187208401886,-43.6984668485503));
#15129=CARTESIAN_POINT('Ctrl Pts',(9.8469257129122,-4.31382280718569,-43.7400429325073));
#15130=CARTESIAN_POINT('Ctrl Pts',(9.80979522521179,-4.39669658017479,-43.7783856209309));
#15131=CARTESIAN_POINT('Ctrl Pts',(9.79294577200484,-4.43430389013879,-43.7957851590042));
#15132=CARTESIAN_POINT('Ctrl Pts',(9.77575204596624,-4.47210120717099,-43.8125181941916));
#15133=CARTESIAN_POINT('Ctrl Pts',(9.75819873711376,-4.51009410634067,-43.8285588699776));
#15134=CARTESIAN_POINT('Ctrl Pts',(9.73442906213901,-4.56154189161018,-43.8502802247951));
#15135=CARTESIAN_POINT('Ctrl Pts',(9.70992373941314,-4.61351031125972,-43.8707967158323));
#15136=CARTESIAN_POINT('Ctrl Pts',(9.68475440784897,-4.6657702690997,-43.8899311961881));
#15137=CARTESIAN_POINT('Ctrl Pts',(9.65977375932576,-4.71763845778443,-43.90892223404));
#15138=CARTESIAN_POINT('Ctrl Pts',(9.63413899471342,-4.76979381627444,-43.9265518693464));
#15139=CARTESIAN_POINT('Ctrl Pts',(9.60793275939673,-4.82201931450148,-43.9426963378945));
#15140=CARTESIAN_POINT('Ctrl Pts',(9.59807555104078,-4.8416634034481,-43.9487689152163));
#15141=CARTESIAN_POINT('Ctrl Pts',(9.58813762048602,-4.8613174875905,-43.9546318746589));
#15142=CARTESIAN_POINT('Ctrl Pts',(9.57812384114847,-4.88097027922755,-43.9602804639433));
#15143=CARTESIAN_POINT('Ctrl Pts',(9.47988016989897,-5.07378083912112,-44.0156979172321));
#15144=CARTESIAN_POINT('Ctrl Pts',(9.37498500850867,-5.26520200497458,-44.0501809838329));
#15145=CARTESIAN_POINT('Ctrl Pts',(9.2631046846633,-5.45512072416129,-44.0630753329145));
#15146=CARTESIAN_POINT('Ctrl Pts',(9.23044829970098,-5.51055548330521,-44.0668390226589));
#15147=CARTESIAN_POINT('Ctrl Pts',(9.1971967976106,-5.56586196042964,-44.0687635893465));
#15148=CARTESIAN_POINT('Ctrl Pts',(9.16334192291174,-5.6210366840491,-44.0688332970512));
#15149=CARTESIAN_POINT('Ctrl Pts',(9.13431980327446,-5.66833526199634,-44.0688930540393));
#15150=CARTESIAN_POINT('Ctrl Pts',(9.10476428938674,-5.71568116575118,-44.0675714534323));
#15151=CARTESIAN_POINT('Ctrl Pts',(9.07480312871612,-5.76285537335169,-44.0648683451569));
#15152=CARTESIAN_POINT('Ctrl Pts',(9.05948004307397,-5.78698175587437,-44.0634858900492));
#15153=CARTESIAN_POINT('Ctrl Pts',(9.04405107690922,-5.81106335134459,-44.0617428892334));
#15154=CARTESIAN_POINT('Ctrl Pts',(9.02853471299363,-5.83507163077697,-44.0596443418483));
#15155=CARTESIAN_POINT('Ctrl Pts',(8.9982064294724,-5.88199821160759,-44.055542521317));
#15156=CARTESIAN_POINT('Ctrl Pts',(8.96754046580988,-5.92864274808812,-44.0500576047013));
#15157=CARTESIAN_POINT('Ctrl Pts',(8.93668327281857,-5.974796952149,-44.043250137711));
#15158=CARTESIAN_POINT('Ctrl Pts',(8.9345094068387,-5.97804848102476,-44.0427705567944));
#15159=CARTESIAN_POINT('Ctrl Pts',(8.93233459747658,-5.98129757948401,-44.0422844323534));
#15160=CARTESIAN_POINT('Ctrl Pts',(8.93015889852956,-5.98454417612983,-44.0417917948209));
#15161=CARTESIAN_POINT('Ctrl Pts',(8.87228268877637,-6.07090755315648,-44.0286870437248));
#15162=CARTESIAN_POINT('Ctrl Pts',(8.81378786331644,-6.15548448285228,-44.010978867558));
#15163=CARTESIAN_POINT('Ctrl Pts',(8.75476238688098,-6.23831993001784,-43.9890041642558));
#15164=CARTESIAN_POINT('Ctrl Pts',(8.73245078970895,-6.26963168284619,-43.9806977386637));
#15165=CARTESIAN_POINT('Ctrl Pts',(8.71004631052358,-6.30071602093377,-43.9717711696754));
#15166=CARTESIAN_POINT('Ctrl Pts',(8.68756771503185,-6.33155719715209,-43.9622493672949));
#15167=CARTESIAN_POINT('Ctrl Pts',(8.63693389296735,-6.40102802460982,-43.9408011746067));
#15168=CARTESIAN_POINT('Ctrl Pts',(8.58568689344058,-6.46958806014974,-43.9162245598352));
#15169=CARTESIAN_POINT('Ctrl Pts',(8.53411477772601,-6.53692068547023,-43.8887772589834));
#15170=CARTESIAN_POINT('Ctrl Pts',(8.50992046471492,-6.56850881386656,-43.8759007543274));
#15171=CARTESIAN_POINT('Ctrl Pts',(8.485654610908,-6.59982718076872,-43.8623930899435));
#15172=CARTESIAN_POINT('Ctrl Pts',(8.46134684828327,-6.63084530909066,-43.8482841546627));
#15173=CARTESIAN_POINT('Ctrl Pts',(8.40630859602086,-6.70107734145193,-43.8163383457814));
#15174=CARTESIAN_POINT('Ctrl Pts',(8.3511331781303,-6.76968547698108,-43.7813828521671));
#15175=CARTESIAN_POINT('Ctrl Pts',(8.29600947438739,-6.83657937909929,-43.7437667180354));
#15176=CARTESIAN_POINT('Ctrl Pts',(8.25940112988745,-6.88100446027871,-43.718785370565));
#15177=CARTESIAN_POINT('Ctrl Pts',(8.22281581705429,-6.92467378385051,-43.6926316589223));
#15178=CARTESIAN_POINT('Ctrl Pts',(8.18631127030164,-6.96756410281864,-43.6654197758277));
#15179=CARTESIAN_POINT('Ctrl Pts',(8.12642898534381,-7.03792164813442,-43.6207812339839));
#15180=CARTESIAN_POINT('Ctrl Pts',(8.06676026536889,-7.10619090896531,-43.5733019776517));
#15181=CARTESIAN_POINT('Ctrl Pts',(8.00730071472223,-7.17256758947659,-43.5232728467731));
#15182=CARTESIAN_POINT('Ctrl Pts',(7.94784116407556,-7.23894426998787,-43.4732437158945));
#15183=CARTESIAN_POINT('Ctrl Pts',(7.88859071459035,-7.30342827304296,-43.4206643974407));
#15184=CARTESIAN_POINT('Ctrl Pts',(7.82953376242443,-7.3661999065718,-43.3657719705771));
#15185=CARTESIAN_POINT('Ctrl Pts',(7.78246051217696,-7.4162340635199,-43.3220181896644));
#15186=CARTESIAN_POINT('Ctrl Pts',(7.73551173823827,-7.46518289020138,-43.2768135657487));
#15187=CARTESIAN_POINT('Ctrl Pts',(7.68867196096467,-7.51312673470191,-43.2302274255216));
#15188=CARTESIAN_POINT('Ctrl Pts',(7.62941400079359,-7.57378147290157,-43.1712903467654));
#15189=CARTESIAN_POINT('Ctrl Pts',(7.57024340356674,-7.63291386982353,-43.1100539400161));
#15190=CARTESIAN_POINT('Ctrl Pts',(7.51134952905245,-7.69045086723973,-43.0468902512232));
#15191=CARTESIAN_POINT('Ctrl Pts',(7.4510109776655,-7.74939925709996,-42.9821771462789));
#15192=CARTESIAN_POINT('Ctrl Pts',(7.39096291968201,-7.80667305865563,-42.9154410886981));
#15193=CARTESIAN_POINT('Ctrl Pts',(7.33141801277851,-7.86220712602253,-42.8471352398619));
#15194=CARTESIAN_POINT('Ctrl Pts',(7.28787285714568,-7.90281915704535,-42.7971832125118));
#15195=CARTESIAN_POINT('Ctrl Pts',(7.24459698063875,-7.9425010699813,-42.746392803258));
#15196=CARTESIAN_POINT('Ctrl Pts',(7.20167632415019,-7.98123150622032,-42.6949580898006));
#15197=CARTESIAN_POINT('Ctrl Pts',(7.13930068925887,-8.03751758727477,-42.6202091653936));
#15198=CARTESIAN_POINT('Ctrl Pts',(7.07752996222588,-8.0919282722449,-42.543925714373));
#15199=CARTESIAN_POINT('Ctrl Pts',(7.01632524916812,-8.14464761366221,-42.4662769769472));
#15200=CARTESIAN_POINT('Ctrl Pts',(6.95400229919708,-8.19833016053661,-42.3872095630809));
#15201=CARTESIAN_POINT('Ctrl Pts',(6.89226620642754,-8.25025895328182,-42.3067264627181));
#15202=CARTESIAN_POINT('Ctrl Pts',(6.83106473230173,-8.30061305883954,-42.2249555226949));
#15203=CARTESIAN_POINT('Ctrl Pts',(6.79926069456621,-8.32678013890045,-42.1824623295273));
#15204=CARTESIAN_POINT('Ctrl Pts',(6.76760085014226,-8.35252173355581,-42.13962053505));
#15205=CARTESIAN_POINT('Ctrl Pts',(6.73607674834671,-8.37786144795066,-42.0964428903655));
#15206=CARTESIAN_POINT('Ctrl Pts',(6.67199336517915,-8.42937297514509,-42.0086697456609));
#15207=CARTESIAN_POINT('Ctrl Pts',(6.60851060516834,-8.4791932576748,-41.9195563684189));
#15208=CARTESIAN_POINT('Ctrl Pts',(6.54557135950043,-8.52749545016914,-41.8292245834684));
#15209=CARTESIAN_POINT('Ctrl Pts',(6.49978585112311,-8.56263315186264,-41.7635122182708));
#15210=CARTESIAN_POINT('Ctrl Pts',(6.45428772304682,-8.59696718414578,-41.697154000995));
#15211=CARTESIAN_POINT('Ctrl Pts',(6.40905142763883,-8.63055964574283,-41.6301805545864));
#15212=CARTESIAN_POINT('Ctrl Pts',(6.35304742575302,-8.67214820346318,-41.5472652542699));
#15213=CARTESIAN_POINT('Ctrl Pts',(6.29738512281016,-8.71263450139334,-41.4632867952234));
#15214=CARTESIAN_POINT('Ctrl Pts',(6.24209165749993,-8.75206999235691,-41.3783888763224));
#15215=CARTESIAN_POINT('Ctrl Pts',(6.18469411014494,-8.79300612192211,-41.2902603372063));
#15216=CARTESIAN_POINT('Ctrl Pts',(6.12769384919897,-8.83281008866344,-41.2011409070487));
#15217=CARTESIAN_POINT('Ctrl Pts',(6.07110079616866,-8.87154004941081,-41.1111391356439));
#15218=CARTESIAN_POINT('Ctrl Pts',(6.05484968674209,-8.88266164113435,-41.0852944681915));
#15219=CARTESIAN_POINT('Ctrl Pts',(6.03863203907221,-8.89369466738167,-41.0593767317759));
#15220=CARTESIAN_POINT('Ctrl Pts',(6.02244782123643,-8.90464048912061,-41.0333877658766));
#15221=CARTESIAN_POINT('Ctrl Pts',(5.96789208360707,-8.94153800156061,-40.9457809862815));
#15222=CARTESIAN_POINT('Ctrl Pts',(5.91381192380562,-8.97738468492097,-40.8575269837696));
#15223=CARTESIAN_POINT('Ctrl Pts',(5.86012825013986,-9.01229190082115,-40.7685826949035));
#15224=CARTESIAN_POINT('Ctrl Pts',(5.78173848263364,-9.0632639813785,-40.638704807473));
#15225=CARTESIAN_POINT('Ctrl Pts',(5.70446841167932,-9.11205487886131,-40.5078066310375));
#15226=CARTESIAN_POINT('Ctrl Pts',(5.62824515844197,-9.15889493533431,-40.3760464765655));
#15227=CARTESIAN_POINT('Ctrl Pts',(5.55068166324207,-9.20655858574416,-40.2419695686026));
#15228=CARTESIAN_POINT('Ctrl Pts',(5.47420216133207,-9.25220373228151,-40.107007556575));
#15229=CARTESIAN_POINT('Ctrl Pts',(5.39872201476634,-9.29604069692326,-39.9712454669586));
#15230=CARTESIAN_POINT('Ctrl Pts',(5.32192875426745,-9.34064028500545,-39.833121549768));
#15231=CARTESIAN_POINT('Ctrl Pts',(5.24616988281148,-9.3833681445475,-39.6941694464635));
#15232=CARTESIAN_POINT('Ctrl Pts',(5.17134976653292,-9.42442267008781,-39.5544301786707));
#15233=CARTESIAN_POINT('Ctrl Pts',(5.13294490286178,-9.44549579232929,-39.4827025765763));
#15234=CARTESIAN_POINT('Ctrl Pts',(5.09478727515637,-9.4661276745041,-39.4107668026536));
#15235=CARTESIAN_POINT('Ctrl Pts',(5.05686335325628,-9.48634295751582,-39.3386236125273));
#15236=CARTESIAN_POINT('Ctrl Pts',(4.97902793754603,-9.52783299541494,-39.1905562473182));
#15237=CARTESIAN_POINT('Ctrl Pts',(4.90219178004977,-9.56756126829831,-39.0416213059113));
#15238=CARTESIAN_POINT('Ctrl Pts',(4.82630358622877,-9.60569069322725,-38.8919330766794));
#15239=CARTESIAN_POINT('Ctrl Pts',(4.73610193406239,-9.65101180250094,-38.7140117834354));
#15240=CARTESIAN_POINT('Ctrl Pts',(4.64723779780822,-9.6940793596263,-38.5350724280117));
#15241=CARTESIAN_POINT('Ctrl Pts',(4.55961797968078,-9.73512502144953,-38.3551653870197));
#15242=CARTESIAN_POINT('Ctrl Pts',(4.47869953974762,-9.77303141057178,-38.1890180769569));
#15243=CARTESIAN_POINT('Ctrl Pts',(4.39884221209784,-9.80921297956952,-38.0220450111243));
#15244=CARTESIAN_POINT('Ctrl Pts',(4.31996655994152,-9.84383312150245,-37.854251824959));
#15245=CARTESIAN_POINT('Ctrl Pts',(4.21884999459777,-9.88821525652471,-37.6391452589999));
#15246=CARTESIAN_POINT('Ctrl Pts',(4.11934342920933,-9.93003289724673,-37.422735917508));
#15247=CARTESIAN_POINT('Ctrl Pts',(4.02137300417622,-9.96955084295716,-37.205166603912));
#15248=CARTESIAN_POINT('Ctrl Pts',(3.92418102114997,-10.0087547915715,-36.9893260272593));
#15249=CARTESIAN_POINT('Ctrl Pts',(3.82850078243586,-10.0456952251983,-36.772343879366));
#15250=CARTESIAN_POINT('Ctrl Pts',(3.73425145285707,-10.0806028780048,-36.55431574799));
#15251=CARTESIAN_POINT('Ctrl Pts',(3.63886981326191,-10.1159299108228,-36.3336682299498));
#15252=CARTESIAN_POINT('Ctrl Pts',(3.54495362444972,-10.1491749110926,-36.1119496058682));
#15253=CARTESIAN_POINT('Ctrl Pts',(3.4524110597738,-10.1805508308637,-35.889212141429));
#15254=CARTESIAN_POINT('Ctrl Pts',(3.35986849509789,-10.2119267506348,-35.6664746769898));
#15255=CARTESIAN_POINT('Ctrl Pts',(3.26869949929918,-10.2414334400909,-35.4427184156961));
#15256=CARTESIAN_POINT('Ctrl Pts',(3.17880504329623,-10.2692598806778,-35.2179476947513));
#15257=CARTESIAN_POINT('Ctrl Pts',(3.11875845584299,-10.287847042473,-35.0678081271711));
#15258=CARTESIAN_POINT('Ctrl Pts',(3.05925105749683,-10.3056863347943,-34.9170987408754));
#15259=CARTESIAN_POINT('Ctrl Pts',(3.00037766351643,-10.322797517479,-34.766133239422));
#15260=CARTESIAN_POINT('Ctrl Pts',(2.93300394147518,-10.3423792671974,-34.5933708582329));
#15261=CARTESIAN_POINT('Ctrl Pts',(2.86626401996985,-10.3610642855586,-34.4197841786842));
#15262=CARTESIAN_POINT('Ctrl Pts',(2.80032934335272,-10.3788556834136,-34.245878496818));
#15263=CARTESIAN_POINT('Ctrl Pts',(2.78727949802178,-10.3823769714845,-34.2114589414799));
#15264=CARTESIAN_POINT('Ctrl Pts',(2.77426113538516,-10.3858632617225,-34.1770267382144));
#15265=CARTESIAN_POINT('Ctrl Pts',(2.76127549569092,-10.3893145893703,-34.142585582622));
#15266=CARTESIAN_POINT('Ctrl Pts',(2.6314416790793,-10.4238218644405,-33.7982339153683));
#15267=CARTESIAN_POINT('Ctrl Pts',(2.50457200205134,-10.4549409999092,-33.4522457830409));
#15268=CARTESIAN_POINT('Ctrl Pts',(2.38057046060466,-10.4830999541101,-33.1049548942437));
#15269=CARTESIAN_POINT('Ctrl Pts',(2.36970090201688,-10.4855682734462,-33.0745125415217));
#15270=CARTESIAN_POINT('Ctrl Pts',(2.35885337811822,-10.4880138159899,-33.0440601702302));
#15271=CARTESIAN_POINT('Ctrl Pts',(2.34802782249378,-10.4904368519569,-33.0135979999854));
#15272=CARTESIAN_POINT('Ctrl Pts',(2.21770246909838,-10.5196069961643,-32.6468738114017));
#15273=CARTESIAN_POINT('Ctrl Pts',(2.09055855130271,-10.5455214163713,-32.2787518271881));
#15274=CARTESIAN_POINT('Ctrl Pts',(1.96649166390134,-10.5686065331557,-31.9094939634275));
#15275=CARTESIAN_POINT('Ctrl Pts',(1.9280261851357,-10.5757638020135,-31.7950099071654));
#15276=CARTESIAN_POINT('Ctrl Pts',(1.88985642821586,-10.5826487298252,-31.680416686595));
#15277=CARTESIAN_POINT('Ctrl Pts',(1.85197914734771,-10.5892730327154,-31.5657221242989));
#15278=CARTESIAN_POINT('Ctrl Pts',(1.74502317759947,-10.6079784076336,-31.2418533603839));
#15279=CARTESIAN_POINT('Ctrl Pts',(1.6403504494956,-10.6246161413583,-30.9170110061736));
#15280=CARTESIAN_POINT('Ctrl Pts',(1.53788875472694,-10.6394265906664,-30.5913659316435));
#15281=CARTESIAN_POINT('Ctrl Pts',(1.41260154985877,-10.6575363808746,-30.1931765277));
#15282=CARTESIAN_POINT('Ctrl Pts',(1.29061928908997,-10.6729130832063,-29.7937918413145));
#15283=CARTESIAN_POINT('Ctrl Pts',(1.17182931764376,-10.6859396294529,-29.3933438455856));
#15284=CARTESIAN_POINT('Ctrl Pts',(1.06436790256251,-10.6977238825867,-29.0310850811159));
#15285=CARTESIAN_POINT('Ctrl Pts',(0.959518682671932,-10.7075839906054,
-28.6679570013368));
#15286=CARTESIAN_POINT('Ctrl Pts',(0.85719280919927,-10.7157695937709,-28.3040700635745));
#15287=CARTESIAN_POINT('Ctrl Pts',(0.822247336604926,-10.7185650721908,
-28.1797984538686));
#15288=CARTESIAN_POINT('Ctrl Pts',(0.787596463964595,-10.7211649655967,
-28.0554372461487));
#15289=CARTESIAN_POINT('Ctrl Pts',(0.753236825127353,-10.7235784272451,
-27.9309927285396));
#15290=CARTESIAN_POINT('Ctrl Pts',(0.636205486739294,-10.7317988467963,
-27.5071259783727));
#15291=CARTESIAN_POINT('Ctrl Pts',(0.52256763618542,-10.7378574576103,-27.08220648135));
#15292=CARTESIAN_POINT('Ctrl Pts',(0.412205680126688,-10.7420921052949,
-26.6564401459235));
#15293=CARTESIAN_POINT('Ctrl Pts',(0.334985882992854,-10.7450550704943,
-26.3585332292451));
#15294=CARTESIAN_POINT('Ctrl Pts',(0.259459073243975,-10.7471216958854,
-26.060554842328));
#15295=CARTESIAN_POINT('Ctrl Pts',(0.185425494016263,-10.7483995046789,
-25.7619706453529));
#15296=CARTESIAN_POINT('Ctrl Pts',(0.122586226530908,-10.7494841012823,
-25.5085341315934));
#15297=CARTESIAN_POINT('Ctrl Pts',(0.0608224917771859,-10.75,-25.2546607217708));
#15298=CARTESIAN_POINT('Ctrl Pts',(2.5146574731546E-15,-10.75,-25.));
#15299=CARTESIAN_POINT('',(-10.5060622858798,-2.27709359605911,-42.0119030752));
#15300=CARTESIAN_POINT('Ctrl Pts',(2.37847882546591E-15,-10.75,-25.));
#15301=CARTESIAN_POINT('Ctrl Pts',(-0.107236928456273,-10.75,-25.4489956397202));
#15302=CARTESIAN_POINT('Ctrl Pts',(-0.217860528274796,-10.7483974074849,
-25.8972288329737));
#15303=CARTESIAN_POINT('Ctrl Pts',(-0.332035266389469,-10.7448689509013,
-26.3445236238487));
#15304=CARTESIAN_POINT('Ctrl Pts',(-0.441369847169077,-10.7414900745602,
-26.7728564516946));
#15305=CARTESIAN_POINT('Ctrl Pts',(-0.553961059582523,-10.7363452340984,
-27.2003277499857));
#15306=CARTESIAN_POINT('Ctrl Pts',(-0.669944683009056,-10.7291037616657,
-27.6267852425981));
#15307=CARTESIAN_POINT('Ctrl Pts',(-0.697532936495075,-10.7273812807569,
-27.7282238514259));
#15308=CARTESIAN_POINT('Ctrl Pts',(-0.725313081771794,-10.7255399552348,
-27.8296051483714));
#15309=CARTESIAN_POINT('Ctrl Pts',(-0.753286850688558,-10.7235749134903,
-27.9309272016471));
#15310=CARTESIAN_POINT('Ctrl Pts',(-0.867733545662818,-10.7155355057934,
-28.3454574767741));
#15311=CARTESIAN_POINT('Ctrl Pts',(-0.985408417919781,-10.7054316754645,
-28.7590760985836));
#15312=CARTESIAN_POINT('Ctrl Pts',(-1.10644537552961,-10.6929073769954,
-29.1716055677841));
#15313=CARTESIAN_POINT('Ctrl Pts',(-1.22118601148511,-10.681034590372,-29.5626753251639));
#15314=CARTESIAN_POINT('Ctrl Pts',(-1.33894815018126,-10.6669865555435,
-29.9527656100601));
#15315=CARTESIAN_POINT('Ctrl Pts',(-1.45983743148625,-10.6504165883258,
-30.3417420844204));
#15316=CARTESIAN_POINT('Ctrl Pts',(-1.48571264619969,-10.6468699425444,
-30.4249988436955));
#15317=CARTESIAN_POINT('Ctrl Pts',(-1.51173109023162,-10.6432075943637,
-30.5082046613194));
#15318=CARTESIAN_POINT('Ctrl Pts',(-1.53789373804128,-10.6394258703545,
-30.5913583746477));
#15319=CARTESIAN_POINT('Ctrl Pts',(-1.64034562245505,-10.6246167901002,
-30.9169849965578));
#15320=CARTESIAN_POINT('Ctrl Pts',(-1.74501002042912,-10.6079804855205,
-31.2418078298158));
#15321=CARTESIAN_POINT('Ctrl Pts',(-1.85195771748882,-10.5892767805307,
-31.5656535771436));
#15322=CARTESIAN_POINT('Ctrl Pts',(-1.97412810450694,-10.5679108330621,
-31.9355947855375));
#15323=CARTESIAN_POINT('Ctrl Pts',(-2.09934183067117,-10.5438372894304,
-32.3044816612346));
#15324=CARTESIAN_POINT('Ctrl Pts',(-2.2277055130733,-10.5166457094765,-32.6720516062204));
#15325=CARTESIAN_POINT('Ctrl Pts',(-2.26750916245566,-10.5082140090579,
-32.7860295238053));
#15326=CARTESIAN_POINT('Ctrl Pts',(-2.30761563823564,-10.4994821320271,
-32.8998808229037));
#15327=CARTESIAN_POINT('Ctrl Pts',(-2.34802797257565,-10.490436818365,-33.0135977355672));
#15328=CARTESIAN_POINT('Ctrl Pts',(-2.47153733442923,-10.4627922653735,
-33.361142700351));
#15329=CARTESIAN_POINT('Ctrl Pts',(-2.59790667502491,-10.4322221869952,
-33.7074132250065));
#15330=CARTESIAN_POINT('Ctrl Pts',(-2.72723242795073,-10.3983029233844,
-34.0520766841272));
#15331=CARTESIAN_POINT('Ctrl Pts',(-2.73855743066555,-10.3953326274937,
-34.0822587207435));
#15332=CARTESIAN_POINT('Ctrl Pts',(-2.7499051011573,-10.3923366166284,-34.1124284254007));
#15333=CARTESIAN_POINT('Ctrl Pts',(-2.76127550222569,-10.3893145876335,
-34.1425855701607));
#15334=CARTESIAN_POINT('Ctrl Pts',(-2.82688668944206,-10.3718764243739,
-34.3166028329513));
#15335=CARTESIAN_POINT('Ctrl Pts',(-2.89333478271947,-10.3535455195258,
-34.4903953522009));
#15336=CARTESIAN_POINT('Ctrl Pts',(-2.96045216143973,-10.3343182819924,
-34.6634673794312));
#15337=CARTESIAN_POINT('Ctrl Pts',(-2.97372789205513,-10.3305151593014,
-34.6977008023446));
#15338=CARTESIAN_POINT('Ctrl Pts',(-2.98702974736202,-10.3266769758128,
-34.7319058852893));
#15339=CARTESIAN_POINT('Ctrl Pts',(-3.0003563392787,-10.3228037152111,-34.7660785653851));
#15340=CARTESIAN_POINT('Ctrl Pts',(-3.05923669243037,-10.3056906413286,
-34.9170623641507));
#15341=CARTESIAN_POINT('Ctrl Pts',(-3.11875120968947,-10.2878492854881,
-35.0677900111587));
#15342=CARTESIAN_POINT('Ctrl Pts',(-3.17880504322316,-10.2692598807004,
-35.2179476948946));
#15343=CARTESIAN_POINT('Ctrl Pts',(-3.2683423400296,-10.2415439972009,-35.441825377722));
#15344=CARTESIAN_POINT('Ctrl Pts',(-3.35914405717459,-10.2121611770437,
-35.6646965966392));
#15345=CARTESIAN_POINT('Ctrl Pts',(-3.45130806413639,-10.1809247273861,
-35.8865571686432));
#15346=CARTESIAN_POINT('Ctrl Pts',(-3.54283782722993,-10.1499032372048,
-36.1068909655857));
#15347=CARTESIAN_POINT('Ctrl Pts',(-3.63571123979394,-10.1170536586038,
-36.3262278829965));
#15348=CARTESIAN_POINT('Ctrl Pts',(-3.73001725013496,-10.0821701109077,
-36.544517773388));
#15349=CARTESIAN_POINT('Ctrl Pts',(-3.82530348275741,-10.0469239815418,
-36.7650765818855));
#15350=CARTESIAN_POINT('Ctrl Pts',(-3.92205232525191,-10.0096015921242,
-36.9845664962694));
#15351=CARTESIAN_POINT('Ctrl Pts',(-4.02034750444548,-9.96996443329666,
-37.2028890356457));
#15352=CARTESIAN_POINT('Ctrl Pts',(-4.11864268363905,-9.93032727446916,
-37.4212115750219));
#15353=CARTESIAN_POINT('Ctrl Pts',(-4.21848427270404,-9.88837553748256,
-37.6383666359865));
#15354=CARTESIAN_POINT('Ctrl Pts',(-4.31994691208665,-9.84384174532468,
-37.8542100277663));
#15355=CARTESIAN_POINT('Ctrl Pts',(-4.40535485324238,-9.80635465132431,
-38.0358999563563));
#15356=CARTESIAN_POINT('Ctrl Pts',(-4.49191389414606,-9.76703709859576,
-38.2166288568363));
#15357=CARTESIAN_POINT('Ctrl Pts',(-4.57972460026303,-9.72568071364687,
-38.3963878422841));
#15358=CARTESIAN_POINT('Ctrl Pts',(-4.660825535451,-9.68748444301353,-38.562411126607));
#15359=CARTESIAN_POINT('Ctrl Pts',(-4.74299414114367,-9.64754886736609,
-38.7276065505638));
#15360=CARTESIAN_POINT('Ctrl Pts',(-4.82630358598209,-9.6056906933512,-38.8919330774143));
#15361=CARTESIAN_POINT('Ctrl Pts',(-4.90218572876413,-9.56756430872154,
-39.0416093715911));
#15362=CARTESIAN_POINT('Ctrl Pts',(-4.97901568325355,-9.52783933124077,
-39.1905324952367));
#15363=CARTESIAN_POINT('Ctrl Pts',(-5.05684473081742,-9.48635288415197,
-39.3385881853712));
#15364=CARTESIAN_POINT('Ctrl Pts',(-5.13087767171036,-9.4468899357886,-39.4794224689669));
#15365=CARTESIAN_POINT('Ctrl Pts',(-5.20580158432899,-9.40584069228541,
-39.6194691944838));
#15366=CARTESIAN_POINT('Ctrl Pts',(-5.28171573037305,-9.36301668773194,
-39.7587113462651));
#15367=CARTESIAN_POINT('Ctrl Pts',(-5.35632406140468,-9.32092930778603,
-39.8955583648382));
#15368=CARTESIAN_POINT('Ctrl Pts',(-5.43188888889226,-9.27712777591539,
-40.03162827474));
#15369=CARTESIAN_POINT('Ctrl Pts',(-5.50849864103087,-9.23141218467567,
-40.1668597120882));
#15370=CARTESIAN_POINT('Ctrl Pts',(-5.54813074290765,-9.20776238920196,
-40.236818248075));
#15371=CARTESIAN_POINT('Ctrl Pts',(-5.5880423937018,-9.18359999174024,-40.306551642029));
#15372=CARTESIAN_POINT('Ctrl Pts',(-5.62824515816366,-9.15889493550534,
-40.3760464775997));
#15373=CARTESIAN_POINT('Ctrl Pts',(-5.70446273045627,-9.11205837004071,
-40.5077968118111));
#15374=CARTESIAN_POINT('Ctrl Pts',(-5.78172696287714,-9.06327125490934,
-40.6386852930282));
#15375=CARTESIAN_POINT('Ctrl Pts',(-5.86011071648358,-9.01230330186323,
-40.7685536452044));
#15376=CARTESIAN_POINT('Ctrl Pts',(-5.91380013799187,-8.9773924971543,-40.8575077508675));
#15377=CARTESIAN_POINT('Ctrl Pts',(-5.96788613468601,-8.94154202497618,
-40.9457714335175));
#15378=CARTESIAN_POINT('Ctrl Pts',(-6.02244782126864,-8.90464048909882,
-41.033387765718));
#15379=CARTESIAN_POINT('Ctrl Pts',(-6.07897394773201,-8.86641034970353,
-41.1241586378155));
#15380=CARTESIAN_POINT('Ctrl Pts',(-6.13590921690286,-8.82711651281615,
-41.2140642892948));
#15381=CARTESIAN_POINT('Ctrl Pts',(-6.19324883006869,-8.78670052801951,
-41.3030092871971));
#15382=CARTESIAN_POINT('Ctrl Pts',(-6.2484433970759,-8.74779648493556,-41.3886268973558));
#15383=CARTESIAN_POINT('Ctrl Pts',(-6.30401276338849,-8.70785255276022,
-41.473354491277));
#15384=CARTESIAN_POINT('Ctrl Pts',(-6.35993531645609,-8.6668165858521,-41.5570616078848));
#15385=CARTESIAN_POINT('Ctrl Pts',(-6.37627760345097,-8.65482461639544,
-41.5815233974147));
#15386=CARTESIAN_POINT('Ctrl Pts',(-6.39264992800991,-8.64273939524507,
-41.6058977286819));
#15387=CARTESIAN_POINT('Ctrl Pts',(-6.40905142809471,-8.63055964540428,
-41.6301805523162));
#15388=CARTESIAN_POINT('Ctrl Pts',(-6.47123616751939,-8.58438127353639,
-41.7222465860561));
#15389=CARTESIAN_POINT('Ctrl Pts',(-6.53391610437926,-8.53680207853486,
-41.8131519097605));
#15390=CARTESIAN_POINT('Ctrl Pts',(-6.59715617551305,-8.48765892208744,
-41.9028104104421));
#15391=CARTESIAN_POINT('Ctrl Pts',(-6.64315450337938,-8.45191413271376,
-41.9680244596425));
#15392=CARTESIAN_POINT('Ctrl Pts',(-6.68944896828638,-8.41534166164106,
-42.032577915456));
#15393=CARTESIAN_POINT('Ctrl Pts',(-6.7360609646428,-8.37787413518879,-42.0964212692318));
#15394=CARTESIAN_POINT('Ctrl Pts',(-6.79685557704122,-8.32900637739579,
-42.1796902182238));
#15395=CARTESIAN_POINT('Ctrl Pts',(-6.85815567166274,-8.27864483482428,
-42.261713048695));
#15396=CARTESIAN_POINT('Ctrl Pts',(-6.92001935262134,-8.22661679423917,
-42.3423866350749));
#15397=CARTESIAN_POINT('Ctrl Pts',(-6.98076429143663,-8.17552962818229,
-42.4216013211836));
#15398=CARTESIAN_POINT('Ctrl Pts',(-7.04205264230787,-8.12283573116821,
-42.4995151701438));
#15399=CARTESIAN_POINT('Ctrl Pts',(-7.10392919618789,-8.06835766777112,
-42.5759835346934));
#15400=CARTESIAN_POINT('Ctrl Pts',(-7.1363436199763,-8.03981898997807,-42.6160419707162));
#15401=CARTESIAN_POINT('Ctrl Pts',(-7.1689192886304,-8.01079045543132,-42.655702938772));
#15402=CARTESIAN_POINT('Ctrl Pts',(-7.20166145050655,-7.98124492776838,
-42.6949402656683));
#15403=CARTESIAN_POINT('Ctrl Pts',(-7.26062011123685,-7.92804243160559,
-42.7655947402625));
#15404=CARTESIAN_POINT('Ctrl Pts',(-7.32024875521799,-7.87304406860132,
-42.8350315342485));
#15405=CARTESIAN_POINT('Ctrl Pts',(-7.38032570970279,-7.81630681975916,
-42.9027542880909));
#15406=CARTESIAN_POINT('Ctrl Pts',(-7.4388878889716,-7.76100013907921,-42.9687694861833));
#15407=CARTESIAN_POINT('Ctrl Pts',(-7.49787602404359,-7.70404110593112,
-43.0331559083555));
#15408=CARTESIAN_POINT('Ctrl Pts',(-7.55709259594321,-7.64549410744107,
-43.0955009361251));
#15409=CARTESIAN_POINT('Ctrl Pts',(-7.6008485065959,-7.60223295346451,-43.1415685043279));
#15410=CARTESIAN_POINT('Ctrl Pts',(-7.64472929780332,-7.55810501353939,
-43.1865224376509));
#15411=CARTESIAN_POINT('Ctrl Pts',(-7.68865828488654,-7.51314073311559,
-43.2302138221607));
#15412=CARTESIAN_POINT('Ctrl Pts',(-7.73550259879265,-7.46519241910727,
-43.276804765109));
#15413=CARTESIAN_POINT('Ctrl Pts',(-7.78245593008502,-7.4162389338257,-43.3220139301321));
#15414=CARTESIAN_POINT('Ctrl Pts',(-7.82953376245117,-7.36619990654337,
-43.3657719702808));
#15415=CARTESIAN_POINT('Ctrl Pts',(-7.88858871032258,-7.30343040337868,
-43.4206625344818));
#15416=CARTESIAN_POINT('Ctrl Pts',(-7.94783714305809,-7.23894864602518,
-43.4732401474993));
#15417=CARTESIAN_POINT('Ctrl Pts',(-8.00729466189739,-7.17257434644111,
-43.5232677541091));
#15418=CARTESIAN_POINT('Ctrl Pts',(-8.06675218073669,-7.10620004685704,
-43.5732953607189));
#15419=CARTESIAN_POINT('Ctrl Pts',(-8.12641885383387,-7.03793330216102,
-43.6207732738916));
#15420=CARTESIAN_POINT('Ctrl Pts',(-8.18629907590924,-6.96757843036117,
-43.6654106856205));
#15421=CARTESIAN_POINT('Ctrl Pts',(-8.24126515827592,-6.90299731251927,
-43.7063848765085));
#15422=CARTESIAN_POINT('Ctrl Pts',(-8.29641393582101,-6.83664939601852,
-43.7449577655475));
#15423=CARTESIAN_POINT('Ctrl Pts',(-8.35154990804721,-6.76861619784635,
-43.7807474993288));
#15424=CARTESIAN_POINT('Ctrl Pts',(-8.38817263164103,-6.72342680675987,
-43.8045199563082));
#15425=CARTESIAN_POINT('Ctrl Pts',(-8.42478989207236,-6.67749412561543,
-43.8270654294201));
#15426=CARTESIAN_POINT('Ctrl Pts',(-8.46134684828446,-6.6308453090891,-43.8482841545959));
#15427=CARTESIAN_POINT('Ctrl Pts',(-8.51315982677914,-6.56472891489431,
-43.878357920717));
#15428=CARTESIAN_POINT('Ctrl Pts',(-8.56478254756177,-6.49724643102362,
-43.9056970712767));
#15429=CARTESIAN_POINT('Ctrl Pts',(-8.61592734856606,-6.42870112309732,
-43.9300233883366));
#15430=CARTESIAN_POINT('Ctrl Pts',(-8.63991916882605,-6.39654679508858,
-43.9414347657402));
#15431=CARTESIAN_POINT('Ctrl Pts',(-8.66380578479096,-6.36415902910658,
-43.9521837717434));
#15432=CARTESIAN_POINT('Ctrl Pts',(-8.68755748755692,-6.33157122947102,
-43.9622450359249));
#15433=CARTESIAN_POINT('Ctrl Pts',(-8.71003951524837,-6.30072544881144,
-43.9717684634522));
#15434=CARTESIAN_POINT('Ctrl Pts',(-8.73244740634611,-6.26963643100528,
-43.9806964803171));
#15435=CARTESIAN_POINT('Ctrl Pts',(-8.75476238684818,-6.23831993006387,
-43.9890041654457));
#15436=CARTESIAN_POINT('Ctrl Pts',(-8.81378476346969,-6.15548883313053,
-44.0109777145809));
#15437=CARTESIAN_POINT('Ctrl Pts',(-8.87227654185961,-6.07091644084465,
-44.0286851829401));
#15438=CARTESIAN_POINT('Ctrl Pts',(-8.93014977420608,-5.98455779150123,
-44.0417897287885));
#15439=CARTESIAN_POINT('Ctrl Pts',(-8.96103257271584,-5.93847436641655,
-44.0487826861988));
#15440=CARTESIAN_POINT('Ctrl Pts',(-8.99173501046696,-5.89188620680568,
-44.0544592798445));
#15441=CARTESIAN_POINT('Ctrl Pts',(-9.02210965563884,-5.84500106362589,
-44.0587554593272));
#15442=CARTESIAN_POINT('Ctrl Pts',(-9.02425298421215,-5.84169270343033,
-44.0590586109916));
#15443=CARTESIAN_POINT('Ctrl Pts',(-9.0263946863895,-5.83838286767396,-44.0593549098961));
#15444=CARTESIAN_POINT('Ctrl Pts',(-9.0285347129843,-5.8350716307914,-44.0596443429015));
#15445=CARTESIAN_POINT('Ctrl Pts',(-9.05887335223018,-5.78812902667531,
-44.0637475645898));
#15446=CARTESIAN_POINT('Ctrl Pts',(-9.08887701333448,-5.74090566264086,
-44.066488459587));
#15447=CARTESIAN_POINT('Ctrl Pts',(-9.11841089904989,-5.69361667178038,
-44.06784174946));
#15448=CARTESIAN_POINT('Ctrl Pts',(-9.1335134748262,-5.66943476850028,-44.0685337736336));
#15449=CARTESIAN_POINT('Ctrl Pts',(-9.14849342989083,-5.64523582718241,
-44.0688637450225));
#15450=CARTESIAN_POINT('Ctrl Pts',(-9.16333413070458,-5.62104938331968,
-44.0688333130625));
#15451=CARTESIAN_POINT('Ctrl Pts',(-9.27932019115726,-5.43202257284732,
-44.0685954750252));
#15452=CARTESIAN_POINT('Ctrl Pts',(-9.38822404812592,-5.24145243072908,
-44.0465840027153));
#15453=CARTESIAN_POINT('Ctrl Pts',(-9.49037895961188,-5.04946426357109,
-44.0034442093763));
#15454=CARTESIAN_POINT('Ctrl Pts',(-9.52019775455593,-4.9934233380307,-43.9908517981765));
#15455=CARTESIAN_POINT('Ctrl Pts',(-9.54944152478437,-4.93726132129649,
-43.9764593736512));
#15456=CARTESIAN_POINT('Ctrl Pts',(-9.57811856097544,-4.88098064194923,
-43.9602834423684));
#15457=CARTESIAN_POINT('Ctrl Pts',(-9.6047301766366,-4.82875349413803,-43.9452725582802));
#15458=CARTESIAN_POINT('Ctrl Pts',(-9.63080521238752,-4.77651667385336,
-43.9287441414904));
#15459=CARTESIAN_POINT('Ctrl Pts',(-9.65625625560094,-4.7244842804683,-43.9108030046276));
#15460=CARTESIAN_POINT('Ctrl Pts',(-9.6818871281723,-4.67208424196093,-43.8927351011291));
#15461=CARTESIAN_POINT('Ctrl Pts',(-9.70688517903262,-4.61989153984246,
-43.8732344536602));
#15462=CARTESIAN_POINT('Ctrl Pts',(-9.73117419853498,-4.56813204941783,
-43.8524589796889));
#15463=CARTESIAN_POINT('Ctrl Pts',(-9.74028176074262,-4.54872398814009,
-43.8446688784225));
#15464=CARTESIAN_POINT('Ctrl Pts',(-9.74928976254991,-4.52937690754481,
-43.8367000449069));
#15465=CARTESIAN_POINT('Ctrl Pts',(-9.75819464297145,-4.51010296781282,
-43.8285626112942));
#15466=CARTESIAN_POINT('Ctrl Pts',(-9.79687625799754,-4.42637953959631,
-43.793214683034));
#15467=CARTESIAN_POINT('Ctrl Pts',(-9.83381278158552,-4.34360625274378,
-43.7545078689066));
#15468=CARTESIAN_POINT('Ctrl Pts',(-9.86916355129727,-4.26172191436226,
-43.7127052463082));
#15469=CARTESIAN_POINT('Ctrl Pts',(-9.88520563768197,-4.22456301681685,
-43.6937353260407));
#15470=CARTESIAN_POINT('Ctrl Pts',(-9.90092094238166,-4.18758710591906,
-43.6741272004195));
#15471=CARTESIAN_POINT('Ctrl Pts',(-9.91632327429604,-4.15078809569386,
-43.6539021212315));
#15472=CARTESIAN_POINT('Ctrl Pts',(-9.92074536029069,-4.14022291708075,
-43.6480954005404));
#15473=CARTESIAN_POINT('Ctrl Pts',(-9.92514262036434,-4.12966998485355,
-43.6422375099564));
#15474=CARTESIAN_POINT('Ctrl Pts',(-9.9295151527142,-4.11912962069311,-43.6363292143049));
#15475=CARTESIAN_POINT('Ctrl Pts',(-9.96375695635676,-4.03658681688429,
-43.590060671645));
#15476=CARTESIAN_POINT('Ctrl Pts',(-9.9965137017754,-3.95469685147143,-43.5405520961091));
#15477=CARTESIAN_POINT('Ctrl Pts',(-10.027746094834,-3.87385088045541,-43.4883126421827));
#15478=CARTESIAN_POINT('Ctrl Pts',(-10.0550083068346,-3.80328184025716,
-43.4427137325806));
#15479=CARTESIAN_POINT('Ctrl Pts',(-10.0811094656341,-3.73350767058796,
-43.3950344466879));
#15480=CARTESIAN_POINT('Ctrl Pts',(-10.1060391066288,-3.66476105295963,
-43.3456209213211));
#15481=CARTESIAN_POINT('Ctrl Pts',(-10.1302917164194,-3.5978814339504,-43.2975493526471));
#15482=CARTESIAN_POINT('Ctrl Pts',(-10.1534368297526,-3.53198496973756,
-43.2478594105366));
#15483=CARTESIAN_POINT('Ctrl Pts',(-10.1755279180874,-3.46715135906702,
-43.1968184788605));
#15484=CARTESIAN_POINT('Ctrl Pts',(-10.2029132662501,-3.38677999057866,
-43.1335452863713));
#15485=CARTESIAN_POINT('Ctrl Pts',(-10.2287275664732,-3.3079046565932,-43.068093899653));
#15486=CARTESIAN_POINT('Ctrl Pts',(-10.2531383411246,-3.23042635910777,
-43.0007320410579));
#15487=CARTESIAN_POINT('Ctrl Pts',(-10.2557783156256,-3.22204724239941,
-42.9934469961721));
#15488=CARTESIAN_POINT('Ctrl Pts',(-10.2584018561637,-3.21368446191673,
-42.9861395599652));
#15489=CARTESIAN_POINT('Ctrl Pts',(-10.2610091614443,-3.20533788995137,
-42.9788100374481));
#15490=CARTESIAN_POINT('Ctrl Pts',(-10.2869627757751,-3.12225451978454,
-42.9058505715778));
#15491=CARTESIAN_POINT('Ctrl Pts',(-10.3113115241216,-3.04077434106176,
-42.8307166031143));
#15492=CARTESIAN_POINT('Ctrl Pts',(-10.3342333296945,-2.96077179059499,
-42.753640700006));
#15493=CARTESIAN_POINT('Ctrl Pts',(-10.3567452030602,-2.88220000098129,
-42.6779432177634));
#15494=CARTESIAN_POINT('Ctrl Pts',(-10.377880537689,-2.80505340505405,-42.6003724327715));
#15495=CARTESIAN_POINT('Ctrl Pts',(-10.397788145182,-2.72920873884206,-42.5210988743318));
#15496=CARTESIAN_POINT('Ctrl Pts',(-10.4182395170266,-2.65129242108953,
-42.4396600062182));
#15497=CARTESIAN_POINT('Ctrl Pts',(-10.4373951504249,-2.57475010585073,
-42.356424239593));
#15498=CARTESIAN_POINT('Ctrl Pts',(-10.4553967161989,-2.4994440912758,-42.2715232304453));
#15499=CARTESIAN_POINT('Ctrl Pts',(-10.4733982819729,-2.42413807670088,
-42.1866222212975));
#15500=CARTESIAN_POINT('Ctrl Pts',(-10.4902456755633,-2.35006832727967,
-42.1000558922966));
#15501=CARTESIAN_POINT('Ctrl Pts',(-10.5060622858798,-2.27709359605911,
-42.0119030752));
#15502=CARTESIAN_POINT('',(-10.5060622858798,2.2770935960591,-42.0119030752));
#15503=CARTESIAN_POINT('Ctrl Pts',(-10.5060622858798,-2.27709359605911,
-42.0119030752));
#15504=CARTESIAN_POINT('Ctrl Pts',(-10.5169211750016,-2.2269928159833,-41.9513817846856));
#15505=CARTESIAN_POINT('Ctrl Pts',(-10.5275918198861,-2.17603932438343,
-41.8916923371475));
#15506=CARTESIAN_POINT('Ctrl Pts',(-10.5380631093571,-2.12409833598685,
-41.8329130265209));
#15507=CARTESIAN_POINT('Ctrl Pts',(-10.5481652864803,-2.07398826442453,
-41.7762056831913));
#15508=CARTESIAN_POINT('Ctrl Pts',(-10.5580819092047,-2.02295908941791,
-41.7203453668008));
#15509=CARTESIAN_POINT('Ctrl Pts',(-10.5677951269423,-1.97088759165573,
-41.6654490466084));
#15510=CARTESIAN_POINT('Ctrl Pts',(-10.5774114727849,-1.91933541352523,
-41.611100218576));
#15511=CARTESIAN_POINT('Ctrl Pts',(-10.5868284809711,-1.86676161176197,
-41.5576959574735));
#15512=CARTESIAN_POINT('Ctrl Pts',(-10.5960207407409,-1.81304431243898,
-41.5053993769468));
#15513=CARTESIAN_POINT('Ctrl Pts',(-10.6089936823863,-1.7372336405342,-41.4315937508633));
#15514=CARTESIAN_POINT('Ctrl Pts',(-10.6215612237893,-1.6588909490796,-41.3597527153406));
#15515=CARTESIAN_POINT('Ctrl Pts',(-10.6335531768026,-1.57807254007726,
-41.2909134876665));
#15516=CARTESIAN_POINT('Ctrl Pts',(-10.6457596887228,-1.49580813562584,
-41.2208425949402));
#15517=CARTESIAN_POINT('Ctrl Pts',(-10.6573697537526,-1.41097862402483,
-41.1538819680966));
#15518=CARTESIAN_POINT('Ctrl Pts',(-10.6682028723582,-1.32364132243195,
-41.0911792922432));
#15519=CARTESIAN_POINT('Ctrl Pts',(-10.6697806490981,-1.31092118449275,
-41.0820470352182));
#15520=CARTESIAN_POINT('Ctrl Pts',(-10.6713419446356,-1.2981478476095,-41.0730051883889));
#15521=CARTESIAN_POINT('Ctrl Pts',(-10.6728862011302,-1.28532148543937,
-41.0640573883661));
#15522=CARTESIAN_POINT('Ctrl Pts',(-10.6781023652254,-1.24199681103724,
-41.0338336571583));
#15523=CARTESIAN_POINT('Ctrl Pts',(-10.6831272007389,-1.19804491020261,
-41.0046644056734));
#15524=CARTESIAN_POINT('Ctrl Pts',(-10.6879474118809,-1.15337770087377,
-40.976644281761));
#15525=CARTESIAN_POINT('Ctrl Pts',(-10.6933301180208,-1.10349804730097,
-40.9453543468218));
#15526=CARTESIAN_POINT('Ctrl Pts',(-10.6984568327903,-1.05272674189745,
-40.9154954419056));
#15527=CARTESIAN_POINT('Ctrl Pts',(-10.703300090004,-1.00093912690731,-40.8872409339168));
#15528=CARTESIAN_POINT('Ctrl Pts',(-10.7080905723239,-0.94971581931515,
-40.8592943031663));
#15529=CARTESIAN_POINT('Ctrl Pts',(-10.7126037747887,-0.897498241347043,
-40.8329170291832));
#15530=CARTESIAN_POINT('Ctrl Pts',(-10.7168049092765,-0.844163412723419,
-40.808327684429));
#15531=CARTESIAN_POINT('Ctrl Pts',(-10.7210060437642,-0.790828584099796,
-40.7837383396748));
#15532=CARTESIAN_POINT('Ctrl Pts',(-10.7248951650162,-0.73637652235252,
-40.7609365199596));
#15533=CARTESIAN_POINT('Ctrl Pts',(-10.7284285456406,-0.680681659397462,
-40.7401970252461));
#15534=CARTESIAN_POINT('Ctrl Pts',(-10.7305548947967,-0.647165110394726,
-40.7277162280239));
#15535=CARTESIAN_POINT('Ctrl Pts',(-10.7325374851499,-0.613428835245424,
-40.7160697181704));
#15536=CARTESIAN_POINT('Ctrl Pts',(-10.7343701088873,-0.579481117404477,
-40.7052989261484));
#15537=CARTESIAN_POINT('Ctrl Pts',(-10.7387885965857,-0.497632579372944,
-40.6793303592902));
#15538=CARTESIAN_POINT('Ctrl Pts',(-10.7423340227891,-0.414554739665019,
-40.6584535425089));
#15539=CARTESIAN_POINT('Ctrl Pts',(-10.7449224741416,-0.330365449223965,
-40.6432014555172));
#15540=CARTESIAN_POINT('Ctrl Pts',(-10.7453420295562,-0.316719423917338,
-40.6407292840096));
#15541=CARTESIAN_POINT('Ctrl Pts',(-10.745736463536,-0.303044203764577,
-40.6384047780912));
#15542=CARTESIAN_POINT('Ctrl Pts',(-10.7461054430156,-0.289340297214281,
-40.6362300776288));
#15543=CARTESIAN_POINT('Ctrl Pts',(-10.7480705739512,-0.216355288052297,
-40.6246479398935));
#15544=CARTESIAN_POINT('Ctrl Pts',(-10.7493119495664,-0.14241824380966,
-40.6173253496218));
#15545=CARTESIAN_POINT('Ctrl Pts',(-10.7497839186023,-0.0680262630204308,
-40.614541089547));
#15546=CARTESIAN_POINT('Ctrl Pts',(-10.7499255932274,-0.0456954421490946,
-40.6137053164929));
#15547=CARTESIAN_POINT('Ctrl Pts',(-10.7499979808866,-0.0233238925964778,
-40.6132782374545));
#15548=CARTESIAN_POINT('Ctrl Pts',(-10.749999956258,-0.000925701714180853,
-40.6132667624236));
#15549=CARTESIAN_POINT('Ctrl Pts',(-10.750000064608,0.000302849218660908,
-40.613266133013));
#15550=CARTESIAN_POINT('Ctrl Pts',(-10.7499999611065,0.00153120719642892,
-40.6132667505364));
#15551=CARTESIAN_POINT('Ctrl Pts',(-10.7499996458546,0.00275937048380377,
-40.6132686144898));
#15552=CARTESIAN_POINT('Ctrl Pts',(-10.7499763020177,0.0937026634470254,
-40.6134066369061));
#15553=CARTESIAN_POINT('Ctrl Pts',(-10.7488040773026,0.183579345376722,
-40.6203491177147));
#15554=CARTESIAN_POINT('Ctrl Pts',(-10.7465539700609,0.272461900589267,
-40.6336315852736));
#15555=CARTESIAN_POINT('Ctrl Pts',(-10.7459490926706,0.296355449772789,
-40.6372021992274));
#15556=CARTESIAN_POINT('Ctrl Pts',(-10.7452662792949,0.320177132210481,
-40.6412312609462));
#15557=CARTESIAN_POINT('Ctrl Pts',(-10.7445068169311,0.343928299168354,
-40.6457103741471));
#15558=CARTESIAN_POINT('Ctrl Pts',(-10.7431254287457,0.387129362169936,
-40.6538574454859));
#15559=CARTESIAN_POINT('Ctrl Pts',(-10.741485265122,0.430235670199365,-40.6635240587775));
#15560=CARTESIAN_POINT('Ctrl Pts',(-10.7395996435294,0.473061091575405,
-40.674624855102));
#15561=CARTESIAN_POINT('Ctrl Pts',(-10.7376799648323,0.516660003163934,
-40.685926148165));
#15562=CARTESIAN_POINT('Ctrl Pts',(-10.7355058809133,0.559967790910228,
-40.6987138561558));
#15563=CARTESIAN_POINT('Ctrl Pts',(-10.7331007175571,0.602790413091531,
-40.7128442814695));
#15564=CARTESIAN_POINT('Ctrl Pts',(-10.7316726009835,0.628217250027148,
-40.7212345201327));
#15565=CARTESIAN_POINT('Ctrl Pts',(-10.7301631907923,0.653473079836672,
-40.730097134421));
#15566=CARTESIAN_POINT('Ctrl Pts',(-10.7285788584156,0.67851765769429,-40.7393935351316));
#15567=CARTESIAN_POINT('Ctrl Pts',(-10.7249879199081,0.735281970761078,
-40.7604641158909));
#15568=CARTESIAN_POINT('Ctrl Pts',(-10.7210180162077,0.790886302064723,
-40.783725776146));
#15569=CARTESIAN_POINT('Ctrl Pts',(-10.7167121853542,0.845441367712903,
-40.8089128341746));
#15570=CARTESIAN_POINT('Ctrl Pts',(-10.712274675129,0.901664816770976,-40.8348701537593));
#15571=CARTESIAN_POINT('Ctrl Pts',(-10.7074803696864,0.956773839390786,
-40.8628725267494));
#15572=CARTESIAN_POINT('Ctrl Pts',(-10.7023673177639,1.01088733787075,-40.8926847844663));
#15573=CARTESIAN_POINT('Ctrl Pts',(-10.69775747029,1.05967521995343,-40.9195630487621));
#15574=CARTESIAN_POINT('Ctrl Pts',(-10.6928883872567,1.10765384988097,-40.9479133723767));
#15575=CARTESIAN_POINT('Ctrl Pts',(-10.6877820642804,1.15490889098301,-40.977599136389));
#15576=CARTESIAN_POINT('Ctrl Pts',(-10.6830090262702,1.19907963936724,-41.0053473381089));
#15577=CARTESIAN_POINT('Ctrl Pts',(-10.6780286317076,1.24261786862674,-41.0342600437575));
#15578=CARTESIAN_POINT('Ctrl Pts',(-10.6728534474259,1.28559264108763,-41.0642459908329));
#15579=CARTESIAN_POINT('Ctrl Pts',(-10.6660559159946,1.34203939750374,-41.1036321086305));
#15580=CARTESIAN_POINT('Ctrl Pts',(-10.658962501078,1.39718157663253,-41.1446412939523));
#15581=CARTESIAN_POINT('Ctrl Pts',(-10.6516162897416,1.45111909578012,-41.1869955273223));
#15582=CARTESIAN_POINT('Ctrl Pts',(-10.6441188346133,1.50616708051922,-41.2302217496076));
#15583=CARTESIAN_POINT('Ctrl Pts',(-10.6363580511712,1.55996028343958,-41.2748491853959));
#15584=CARTESIAN_POINT('Ctrl Pts',(-10.6283717818543,1.61260256544954,-41.3206366361582));
#15585=CARTESIAN_POINT('Ctrl Pts',(-10.6201468071409,1.66681829762756,-41.3677926497818));
#15586=CARTESIAN_POINT('Ctrl Pts',(-10.6116826613633,1.71981327495423,-41.4161791961904));
#15587=CARTESIAN_POINT('Ctrl Pts',(-10.603012462611,1.77169857534448,-41.465587270585));
#15588=CARTESIAN_POINT('Ctrl Pts',(-10.6006686230707,1.78572487648107,-41.4789438961576));
#15589=CARTESIAN_POINT('Ctrl Pts',(-10.5983096802437,1.79967006975955,-41.4923754677647));
#15590=CARTESIAN_POINT('Ctrl Pts',(-10.5959361902354,1.813536321744,-41.5058784916076));
#15591=CARTESIAN_POINT('Ctrl Pts',(-10.5866134040062,1.86800130899971,-41.5589167619592));
#15592=CARTESIAN_POINT('Ctrl Pts',(-10.5770540804843,1.92132307652416,-41.6131249930469));
#15593=CARTESIAN_POINT('Ctrl Pts',(-10.5672843422973,1.97362269097949,-41.6683345047717));
#15594=CARTESIAN_POINT('Ctrl Pts',(-10.5571735077314,2.02774827136858,-41.7254715773146));
#15595=CARTESIAN_POINT('Ctrl Pts',(-10.5468373130892,2.08077907582018,-41.7836811722096));
#15596=CARTESIAN_POINT('Ctrl Pts',(-10.5362955537602,2.13284690400159,-41.8428326535671));
#15597=CARTESIAN_POINT('Ctrl Pts',(-10.5263960333759,2.18174258738393,-41.898380430478));
#15598=CARTESIAN_POINT('Ctrl Pts',(-10.5163151222045,2.22978902446844,-41.9547595793156));
#15599=CARTESIAN_POINT('Ctrl Pts',(-10.5060622858798,2.27709359605911,-42.0119030752));
#15600=CARTESIAN_POINT('Ctrl Pts',(-10.5060622858798,2.27709359605911,-42.0119030752));
#15601=CARTESIAN_POINT('Ctrl Pts',(-10.4903858538268,2.34942157232421,-42.0992746181415));
#15602=CARTESIAN_POINT('Ctrl Pts',(-10.4736968030168,2.42282523877712,-42.1850875945395));
#15603=CARTESIAN_POINT('Ctrl Pts',(-10.4558750724622,2.49744213415037,-42.2692654755765));
#15604=CARTESIAN_POINT('Ctrl Pts',(-10.4383088490782,2.57098925957247,-42.3522365124096));
#15605=CARTESIAN_POINT('Ctrl Pts',(-10.4196422455203,2.64571509992633,-42.4336189548605));
#15606=CARTESIAN_POINT('Ctrl Pts',(-10.3997435370008,2.72174811674475,-42.5132910675444));
#15607=CARTESIAN_POINT('Ctrl Pts',(-10.3794106774459,2.79944002579496,-42.594701470439));
#15608=CARTESIAN_POINT('Ctrl Pts',(-10.3577915446787,2.8784968272504,-42.6743263559687));
#15609=CARTESIAN_POINT('Ctrl Pts',(-10.3347260481214,2.95905154530767,-42.7519828654194));
#15610=CARTESIAN_POINT('Ctrl Pts',(-10.3116605515641,3.03960626336494,-42.8296393748701));
#15611=CARTESIAN_POINT('Ctrl Pts',(-10.2871488217201,3.12165894477404,-42.90532756893));
#15612=CARTESIAN_POINT('Ctrl Pts',(-10.2610091614501,3.20533788993294,-42.9788100375568));
#15613=CARTESIAN_POINT('Ctrl Pts',(-10.2369004525634,3.28251530187875,-43.0465832001037));
#15614=CARTESIAN_POINT('Ctrl Pts',(-10.211405190032,3.36107882836898,-43.1124719480175));
#15615=CARTESIAN_POINT('Ctrl Pts',(-10.1843579213645,3.44112785947417,-43.1762137875333));
#15616=CARTESIAN_POINT('Ctrl Pts',(-10.181433339459,3.4497834450271,-43.1831061001274));
#15617=CARTESIAN_POINT('Ctrl Pts',(-10.1784905933341,3.45845639526925,-43.1899732648956));
#15618=CARTESIAN_POINT('Ctrl Pts',(-10.1755294601892,3.46714683325539,-43.1968149158649));
#15619=CARTESIAN_POINT('Ctrl Pts',(-10.1534379069393,3.53198190285271,-43.2478570977966));
#15620=CARTESIAN_POINT('Ctrl Pts',(-10.1302922806711,3.5978798779554,-43.2975482341483));
#15621=CARTESIAN_POINT('Ctrl Pts',(-10.1060391066289,3.6647610529594,-43.3456209213228));
#15622=CARTESIAN_POINT('Ctrl Pts',(-10.0774789910328,3.74351916049569,-43.4022304809757));
#15623=CARTESIAN_POINT('Ctrl Pts',(-10.0473808013863,3.82362678346992,-43.4565636983887));
#15624=CARTESIAN_POINT('Ctrl Pts',(-10.0157618677232,3.90473120961818,-43.5081008021272));
#15625=CARTESIAN_POINT('Ctrl Pts',(-9.98816221632845,3.97552594014595,-43.5530866992554));
#15626=CARTESIAN_POINT('Ctrl Pts',(-9.95940424479242,4.04707940133543,-43.5959421869829));
#15627=CARTESIAN_POINT('Ctrl Pts',(-9.9295151528399,4.1191296203901,-43.6363292172957));
#15628=CARTESIAN_POINT('Ctrl Pts',(-9.92514363536074,4.12966753811858,-43.6422361417758));
#15629=CARTESIAN_POINT('Ctrl Pts',(-9.92074740166516,4.14021801800824,-43.6480926845505));
#15630=CARTESIAN_POINT('Ctrl Pts',(-9.91632635362655,4.15078073859803,-43.653898081326));
#15631=CARTESIAN_POINT('Ctrl Pts',(-9.88238540720856,4.23187208400656,-43.6984668485442));
#15632=CARTESIAN_POINT('Ctrl Pts',(-9.84692571292298,4.31382280716079,-43.7400429324949));
#15633=CARTESIAN_POINT('Ctrl Pts',(-9.80979522522875,4.39669658013697,-43.7783856209135));
#15634=CARTESIAN_POINT('Ctrl Pts',(-9.79294577201636,4.4343038901135,-43.795785158993));
#15635=CARTESIAN_POINT('Ctrl Pts',(-9.7757520459721,4.47210120715835,-43.8125181941863));
#15636=CARTESIAN_POINT('Ctrl Pts',(-9.75819873711372,4.5100941063408,-43.8285588699776));
#15637=CARTESIAN_POINT('Ctrl Pts',(-9.73442906213716,4.56154189161422,-43.8502802247968));
#15638=CARTESIAN_POINT('Ctrl Pts',(-9.70992373940938,4.61351031126775,-43.8707967158355));
#15639=CARTESIAN_POINT('Ctrl Pts',(-9.6847544078432,4.66577026911174,-43.8899311961925));
#15640=CARTESIAN_POINT('Ctrl Pts',(-9.65977375931941,4.7176384577975,-43.9089222340446));
#15641=CARTESIAN_POINT('Ctrl Pts',(-9.63413899470648,4.76979381628853,-43.926551869351));
#15642=CARTESIAN_POINT('Ctrl Pts',(-9.60793275938919,4.82201931451656,-43.9426963378991));
#15643=CARTESIAN_POINT('Ctrl Pts',(-9.59807555103569,4.84166340345821,-43.9487689152193));
#15644=CARTESIAN_POINT('Ctrl Pts',(-9.58813762048344,4.86131748759562,-43.9546318746603));
#15645=CARTESIAN_POINT('Ctrl Pts',(-9.57812384114842,4.88097027922769,-43.9602804639433));
#15646=CARTESIAN_POINT('Ctrl Pts',(-9.47988016966834,5.07378083957379,-44.0156979173622));
#15647=CARTESIAN_POINT('Ctrl Pts',(-9.37498500801622,5.2652020058733,-44.0501809839947));
#15648=CARTESIAN_POINT('Ctrl Pts',(-9.26310468387546,5.45512072549868,-44.0630753330053));
#15649=CARTESIAN_POINT('Ctrl Pts',(-9.23044829916616,5.51055548419478,-44.0668390226898));
#15650=CARTESIAN_POINT('Ctrl Pts',(-9.1971967973383,5.56586196087343,-44.068763589347));
#15651=CARTESIAN_POINT('Ctrl Pts',(-9.16334192291166,5.62103668404923,-44.0688332970512));
#15652=CARTESIAN_POINT('Ctrl Pts',(-9.13431980327369,5.66833526199759,-44.0688930540393));
#15653=CARTESIAN_POINT('Ctrl Pts',(-9.10476428938528,5.71568116575354,-44.0675714534323));
#15654=CARTESIAN_POINT('Ctrl Pts',(-9.07480312871392,5.76285537335515,-44.0648683451568));
#15655=CARTESIAN_POINT('Ctrl Pts',(-9.05948004307237,5.78698175587688,-44.0634858900491));
#15656=CARTESIAN_POINT('Ctrl Pts',(-9.0440510769082,5.81106335134616,-44.0617428892334));
#15657=CARTESIAN_POINT('Ctrl Pts',(-9.02853471299321,5.83507163077762,-44.0596443418482));
#15658=CARTESIAN_POINT('Ctrl Pts',(-8.99820642947174,5.88199821160859,-44.0555425213169));
#15659=CARTESIAN_POINT('Ctrl Pts',(-8.96754046580899,5.92864274808946,-44.0500576047011));
#15660=CARTESIAN_POINT('Ctrl Pts',(-8.93668327281746,5.97479695215066,-44.0432501377108));
#15661=CARTESIAN_POINT('Ctrl Pts',(-8.93450940683793,5.9780484810259,-44.0427705567942));
#15662=CARTESIAN_POINT('Ctrl Pts',(-8.93233459747615,5.98129757948464,-44.0422844323533));
#15663=CARTESIAN_POINT('Ctrl Pts',(-8.93015889852948,5.98454417612995,-44.0417917948209));
#15664=CARTESIAN_POINT('Ctrl Pts',(-8.87228268877595,6.07090755315709,-44.0286870437247));
#15665=CARTESIAN_POINT('Ctrl Pts',(-8.81378786331539,6.15548448285379,-44.0109788675573));
#15666=CARTESIAN_POINT('Ctrl Pts',(-8.75476238687981,6.23831993001948,-43.9890041642549));
#15667=CARTESIAN_POINT('Ctrl Pts',(-8.73245078970821,6.26963168284721,-43.9806977386628));
#15668=CARTESIAN_POINT('Ctrl Pts',(-8.71004631052317,6.30071602093432,-43.9717711696744));
#15669=CARTESIAN_POINT('Ctrl Pts',(-8.68756771503179,6.33155719715214,-43.9622493672937));
#15670=CARTESIAN_POINT('Ctrl Pts',(-8.63693389294267,6.40102802464363,-43.9408011745944));
#15671=CARTESIAN_POINT('Ctrl Pts',(-8.58568689339014,6.46958806021716,-43.9162245598074));
#15672=CARTESIAN_POINT('Ctrl Pts',(-8.53411477764999,6.53692068556944,-43.8887772589389));
#15673=CARTESIAN_POINT('Ctrl Pts',(-8.50992046466342,6.56850881393301,-43.8759007542945));
#15674=CARTESIAN_POINT('Ctrl Pts',(-8.48565461088127,6.59982718080281,-43.8623930899239));
#15675=CARTESIAN_POINT('Ctrl Pts',(-8.46134684828156,6.63084530909281,-43.8482841546581));
#15676=CARTESIAN_POINT('Ctrl Pts',(-8.40630859605882,6.70107734140343,-43.8163383458011));
#15677=CARTESIAN_POINT('Ctrl Pts',(-8.35113317820789,6.76968547688455,-43.7813828522151));
#15678=CARTESIAN_POINT('Ctrl Pts',(-8.29600947450433,6.83657937895735,-43.7437667181145));
#15679=CARTESIAN_POINT('Ctrl Pts',(-8.25940112996534,6.8810044601857,-43.7187853706205));
#15680=CARTESIAN_POINT('Ctrl Pts',(-8.2228158170931,6.92467378380488,-43.6926316589512));
#15681=CARTESIAN_POINT('Ctrl Pts',(-8.18631127030155,6.96756410281872,-43.6654197758277));
#15682=CARTESIAN_POINT('Ctrl Pts',(-8.12642898534358,7.03792164813465,-43.6207812339838));
#15683=CARTESIAN_POINT('Ctrl Pts',(-8.06676026536866,7.10619090896555,-43.5733019776527));
#15684=CARTESIAN_POINT('Ctrl Pts',(-8.00730071472196,7.17256758947688,-43.5232728467746));
#15685=CARTESIAN_POINT('Ctrl Pts',(-7.94784116407525,7.23894426998821,-43.4732437158965));
#15686=CARTESIAN_POINT('Ctrl Pts',(-7.88859071458996,7.30342827304339,-43.4206643974427));
#15687=CARTESIAN_POINT('Ctrl Pts',(-7.82953376242379,7.36619990657248,-43.3657719705771));
#15688=CARTESIAN_POINT('Ctrl Pts',(-7.78246051217648,7.4162340635204,-43.322018189663));
#15689=CARTESIAN_POINT('Ctrl Pts',(-7.73551173823807,7.46518289020163,-43.2768135657473));
#15690=CARTESIAN_POINT('Ctrl Pts',(-7.68867196096474,7.51312673470195,-43.2302274255208));
#15691=CARTESIAN_POINT('Ctrl Pts',(-7.62941400081416,7.57378147288071,-43.1712903467852));
#15692=CARTESIAN_POINT('Ctrl Pts',(-7.57024340360777,7.63291386978282,-43.1100539400581));
#15693=CARTESIAN_POINT('Ctrl Pts',(-7.51134952911368,7.69045086718029,-43.0468902512885));
#15694=CARTESIAN_POINT('Ctrl Pts',(-7.4510109777538,7.74939925701512,-42.982177146375));
#15695=CARTESIAN_POINT('Ctrl Pts',(-7.39096291979704,7.80667305854691,-42.9154410888264));
#15696=CARTESIAN_POINT('Ctrl Pts',(-7.33141801291965,7.86220712589153,-42.8471352400235));
#15697=CARTESIAN_POINT('Ctrl Pts',(-7.28787285723929,7.90281915696019,-42.7971832126213));
#15698=CARTESIAN_POINT('Ctrl Pts',(-7.24459698068532,7.94250106993998,-42.7463928033134));
#15699=CARTESIAN_POINT('Ctrl Pts',(-7.20167632415047,7.98123150622077,-42.6949580898005));
#15700=CARTESIAN_POINT('Ctrl Pts',(-7.13930068922744,8.03751758730387,-42.6202091653556));
#15701=CARTESIAN_POINT('Ctrl Pts',(-7.07752996216333,8.0919282723007,-42.5439257142954));
#15702=CARTESIAN_POINT('Ctrl Pts',(-7.01632524907499,8.14464761374309,-42.4662769768287));
#15703=CARTESIAN_POINT('Ctrl Pts',(-6.95400229907961,8.19833016063715,-42.3872095629296));
#15704=CARTESIAN_POINT('Ctrl Pts',(-6.89226620628615,8.25025895340072,-42.3067264625329));
#15705=CARTESIAN_POINT('Ctrl Pts',(-6.83106473213676,8.30061305897572,-42.2249555224749));
#15706=CARTESIAN_POINT('Ctrl Pts',(-6.7992606944567,8.32678013898989,-42.1824623293798));
#15707=CARTESIAN_POINT('Ctrl Pts',(-6.76760085008768,8.35252173360003,-42.1396205349761));
#15708=CARTESIAN_POINT('Ctrl Pts',(-6.73607674834659,8.37786144795107,-42.0964428903666));
#15709=CARTESIAN_POINT('Ctrl Pts',(-6.67199336517252,8.42937297515064,-42.0086697456537));
#15710=CARTESIAN_POINT('Ctrl Pts',(-6.60851060515526,8.4791932576852,-41.9195563684028));
#15711=CARTESIAN_POINT('Ctrl Pts',(-6.5455713594808,8.52749545018427,-41.8292245834422));
#15712=CARTESIAN_POINT('Ctrl Pts',(-6.49978585110939,8.56263315187302,-41.7635122182526));
#15713=CARTESIAN_POINT('Ctrl Pts',(-6.45428772303884,8.59696718415172,-41.6971540009845));
#15714=CARTESIAN_POINT('Ctrl Pts',(-6.40905142763636,8.63055964574466,-41.6301805545832));
#15715=CARTESIAN_POINT('Ctrl Pts',(-6.35304742562662,8.67214820355701,-41.547265254082));
#15716=CARTESIAN_POINT('Ctrl Pts',(-6.29738512256274,8.71263450157332,-41.4632867948496));
#15717=CARTESIAN_POINT('Ctrl Pts',(-6.24209165713335,8.7520699926184,-41.3783888757593));
#15718=CARTESIAN_POINT('Ctrl Pts',(-6.18469410966926,8.7930061222578,-41.290260336469));
#15719=CARTESIAN_POINT('Ctrl Pts',(-6.12769384861597,8.83281008906891,-41.2011409061342));
#15720=CARTESIAN_POINT('Ctrl Pts',(-6.07110079547896,8.87154004988281,-41.1111391345468));
#15721=CARTESIAN_POINT('Ctrl Pts',(-6.05484968628221,8.88266164144722,-41.0852944674562));
#15722=CARTESIAN_POINT('Ctrl Pts',(-6.03863203884112,8.89369466753796,-41.0593767314042));
#15723=CARTESIAN_POINT('Ctrl Pts',(-6.02244782123308,8.90464048912287,-41.0333877658703));
#15724=CARTESIAN_POINT('Ctrl Pts',(-5.96789208360469,8.94153800156218,-40.9457809862758));
#15725=CARTESIAN_POINT('Ctrl Pts',(-5.91381192380442,8.97738468492173,-40.857526983766));
#15726=CARTESIAN_POINT('Ctrl Pts',(-5.86012825014004,9.01229190082103,-40.7685826949025));
#15727=CARTESIAN_POINT('Ctrl Pts',(-5.78173848263234,9.06326398137933,-40.6387048074699));
#15728=CARTESIAN_POINT('Ctrl Pts',(-5.70446841167726,9.1120548788626,-40.5078066310337));
#15729=CARTESIAN_POINT('Ctrl Pts',(-5.62824515844005,9.15889493533549,-40.3760464765598));
#15730=CARTESIAN_POINT('Ctrl Pts',(-5.5506816632265,9.2065585857537,-40.2419695685711));
#15731=CARTESIAN_POINT('Ctrl Pts',(-5.47420216130162,9.25220373229958,-40.1070075565167));
#15732=CARTESIAN_POINT('Ctrl Pts',(-5.39872201472086,9.29604069694951,-39.9712454668733));
#15733=CARTESIAN_POINT('Ctrl Pts',(-5.32192875420435,9.34064028504136,-39.833121549651));
#15734=CARTESIAN_POINT('Ctrl Pts',(-5.24616988273066,9.38336814459259,-39.6941694463143));
#15735=CARTESIAN_POINT('Ctrl Pts',(-5.1713497664352,9.4244226701412,-39.5544301784892));
#15736=CARTESIAN_POINT('Ctrl Pts',(-5.13294490279669,9.44549579236426,-39.4827025764554));
#15737=CARTESIAN_POINT('Ctrl Pts',(-5.09478727512359,9.46612767452138,-39.4107668025937));
#15738=CARTESIAN_POINT('Ctrl Pts',(-5.05686335325565,9.486342957516,-39.3386236125289));
#15739=CARTESIAN_POINT('Ctrl Pts',(-4.97902793754477,9.52783299541552,-39.1905562473193));
#15740=CARTESIAN_POINT('Ctrl Pts',(-4.90219178004792,9.56756126829927,-39.0416213059115));
#15741=CARTESIAN_POINT('Ctrl Pts',(-4.82630358622753,9.60569069322788,-38.8919330766784));
#15742=CARTESIAN_POINT('Ctrl Pts',(-4.73610193391763,9.65101180257367,-38.7140117831485));
#15743=CARTESIAN_POINT('Ctrl Pts',(-4.64723779752275,9.69407935976452,-38.5350724274354));
#15744=CARTESIAN_POINT('Ctrl Pts',(-4.55961797925815,9.7351250216472,-38.355165386151));
#15745=CARTESIAN_POINT('Ctrl Pts',(-4.47869953946941,9.77303141069736,-38.1890180763747));
#15746=CARTESIAN_POINT('Ctrl Pts',(-4.39884221195997,9.8092129796294,-38.0220450108315));
#15747=CARTESIAN_POINT('Ctrl Pts',(-4.3199665599412,9.84383312150183,-37.8542518249589));
#15748=CARTESIAN_POINT('Ctrl Pts',(-4.2188499945973,9.888215256524,-37.6391452589997));
#15749=CARTESIAN_POINT('Ctrl Pts',(-4.11934342920786,9.93003289724634,-37.4227359175084));
#15750=CARTESIAN_POINT('Ctrl Pts',(-4.02137300417359,9.96955084295721,-37.2051666039132));
#15751=CARTESIAN_POINT('Ctrl Pts',(-3.92418102109437,10.0087547915929,-36.9893260271463));
#15752=CARTESIAN_POINT('Ctrl Pts',(-3.82850078232874,10.0456952252387,-36.7723438791378));
#15753=CARTESIAN_POINT('Ctrl Pts',(-3.73425145270028,10.0806028780621,-36.5543157476452));
#15754=CARTESIAN_POINT('Ctrl Pts',(-3.6388698131308,10.1159299108691,-36.3336682296626));
#15755=CARTESIAN_POINT('Ctrl Pts',(-3.54495362434385,10.1491749111289,-36.1119496056389));
#15756=CARTESIAN_POINT('Ctrl Pts',(-3.45241105969329,10.1805508308907,-35.8892121412572));
#15757=CARTESIAN_POINT('Ctrl Pts',(-3.35986849504272,10.2119267506525,-35.6664746768756));
#15758=CARTESIAN_POINT('Ctrl Pts',(-3.26869949926948,10.2414334401001,-35.4427184156392));
#15759=CARTESIAN_POINT('Ctrl Pts',(-3.17880504329257,10.269259880679,-35.217947694751));
#15760=CARTESIAN_POINT('Ctrl Pts',(-3.11875845584136,10.2878470424735,-35.0678081271702));
#15761=CARTESIAN_POINT('Ctrl Pts',(-3.05925105749581,10.3056863347945,-34.9170987408756));
#15762=CARTESIAN_POINT('Ctrl Pts',(-3.00037766351568,10.3227975174792,-34.7661332394234));
#15763=CARTESIAN_POINT('Ctrl Pts',(-2.93300394142254,10.3423792672126,-34.5933708581017));
#15764=CARTESIAN_POINT('Ctrl Pts',(-2.86626401986577,10.3610642855877,-34.4197841784193));
#15765=CARTESIAN_POINT('Ctrl Pts',(-2.80032934319939,10.378855683455,-34.2458784964172));
#15766=CARTESIAN_POINT('Ctrl Pts',(-2.78727949791908,10.382376971512,-34.2114589412114));
#15767=CARTESIAN_POINT('Ctrl Pts',(-2.77426113533288,10.3858632617364,-34.1770267380782));
#15768=CARTESIAN_POINT('Ctrl Pts',(-2.76127549568886,10.3893145893709,-34.1425855826182));
#15769=CARTESIAN_POINT('Ctrl Pts',(-2.6314416794453,10.4238218643432,-33.7982339163321));
#15770=CARTESIAN_POINT('Ctrl Pts',(-2.50457200276917,10.4549409997331,-33.4522457849824));
#15771=CARTESIAN_POINT('Ctrl Pts',(-2.38057046165633,10.4830999538713,-33.1049548971784));
#15772=CARTESIAN_POINT('Ctrl Pts',(-2.36970090271685,10.4855682732884,-33.0745125434766));
#15773=CARTESIAN_POINT('Ctrl Pts',(-2.35885337846789,10.4880138159116,-33.0440601712045));
#15774=CARTESIAN_POINT('Ctrl Pts',(-2.34802782249455,10.4904368519567,-33.0135979999787));
#15775=CARTESIAN_POINT('Ctrl Pts',(-2.21770246908197,10.519606996168,-32.6468738113555));
#15776=CARTESIAN_POINT('Ctrl Pts',(-2.09055855127056,10.5455214163779,-32.2787518270953));
#15777=CARTESIAN_POINT('Ctrl Pts',(-1.96649166385433,10.5686065331645,-31.9094939632878));
#15778=CARTESIAN_POINT('Ctrl Pts',(-1.92802618510459,10.5757638020191,-31.7950099070721));
#15779=CARTESIAN_POINT('Ctrl Pts',(-1.88985642820042,10.582648729828,-31.6804166865482));
#15780=CARTESIAN_POINT('Ctrl Pts',(-1.85197914734771,10.5892730327154,-31.5657221242989));
#15781=CARTESIAN_POINT('Ctrl Pts',(-1.74502317759923,10.6079784076337,-31.2418533603832));
#15782=CARTESIAN_POINT('Ctrl Pts',(-1.64035044949552,10.6246161413583,-30.9170110061711));
#15783=CARTESIAN_POINT('Ctrl Pts',(-1.53788875472713,10.6394265906663,-30.5913659316414));
#15784=CARTESIAN_POINT('Ctrl Pts',(-1.41260154981738,10.6575363808806,-30.1931765275653));
#15785=CARTESIAN_POINT('Ctrl Pts',(-1.29061928900833,10.6729130832165,-29.7937918410448));
#15786=CARTESIAN_POINT('Ctrl Pts',(-1.17182931752389,10.685939629466,-29.3933438451799));
#15787=CARTESIAN_POINT('Ctrl Pts',(-1.06436790248444,10.697723882594,-29.0310850808448));
#15788=CARTESIAN_POINT('Ctrl Pts',(-0.95951868263359,10.7075839906085,-28.6679570012007));
#15789=CARTESIAN_POINT('Ctrl Pts',(-0.857192809199198,10.7157695937709,
-28.3040700635745));
#15790=CARTESIAN_POINT('Ctrl Pts',(-0.822247336604825,10.7185650721908,
-28.1797984538686));
#15791=CARTESIAN_POINT('Ctrl Pts',(-0.787596463964514,10.7211649655967,
-28.0554372461487));
#15792=CARTESIAN_POINT('Ctrl Pts',(-0.753236825127355,10.7235784272452,
-27.9309927285396));
#15793=CARTESIAN_POINT('Ctrl Pts',(-0.636205486739687,10.7317988467963,
-27.5071259783731));
#15794=CARTESIAN_POINT('Ctrl Pts',(-0.522567636184466,10.7378574576102,
-27.0822064813511));
#15795=CARTESIAN_POINT('Ctrl Pts',(-0.412205680124944,10.7420921052949,
-26.6564401459256));
#15796=CARTESIAN_POINT('Ctrl Pts',(-0.334985886452765,10.7450550703614,
-26.3585332426048));
#15797=CARTESIAN_POINT('Ctrl Pts',(-0.259459080010432,10.7471216957,-26.0605548690474));
#15798=CARTESIAN_POINT('Ctrl Pts',(-0.185425503965189,10.7483995045071,
-25.7619706855148));
#15799=CARTESIAN_POINT('Ctrl Pts',(-0.122586233044267,10.749484101228,-25.5085341584148));
#15800=CARTESIAN_POINT('Ctrl Pts',(-0.0608224949761656,10.75,-25.2546607352261));
#15801=CARTESIAN_POINT('Ctrl Pts',(1.14715432465305E-15,10.75,-25.));
#15802=CARTESIAN_POINT('',(10.5060622858798,2.27709359605911,-42.0119030752));
#15803=CARTESIAN_POINT('Ctrl Pts',(1.18948320324198E-15,10.75,-25.));
#15804=CARTESIAN_POINT('Ctrl Pts',(0.107236928162667,10.75,-25.4489956383632));
#15805=CARTESIAN_POINT('Ctrl Pts',(0.217860527654828,10.7483974074937,-25.8972288302672));
#15806=CARTESIAN_POINT('Ctrl Pts',(0.332035265413112,10.7448689509315,-26.3445236198006));
#15807=CARTESIAN_POINT('Ctrl Pts',(0.441369846116192,10.7414900746027,-26.772856447399));
#15808=CARTESIAN_POINT('Ctrl Pts',(0.55396105844135,10.7363452341562,-27.2003277454457));
#15809=CARTESIAN_POINT('Ctrl Pts',(0.669944681770897,10.729103761743,-27.6267852378145));
#15810=CARTESIAN_POINT('Ctrl Pts',(0.69753293567855,10.7273812808111,-27.7282238482195));
#15811=CARTESIAN_POINT('Ctrl Pts',(0.725313081382595,10.7255399552622,-27.8296051467404));
#15812=CARTESIAN_POINT('Ctrl Pts',(0.753286850732499,10.7235749134872,-27.9309272015895));
#15813=CARTESIAN_POINT('Ctrl Pts',(0.867733545684342,10.7155355057914,-28.3454574766542));
#15814=CARTESIAN_POINT('Ctrl Pts',(0.985408417913843,10.7054316754648,-28.7590760984061));
#15815=CARTESIAN_POINT('Ctrl Pts',(1.10644537549551,10.692907376999,-29.1716055675506));
#15816=CARTESIAN_POINT('Ctrl Pts',(1.22118601156182,10.6810345903645,-29.562675325346));
#15817=CARTESIAN_POINT('Ctrl Pts',(1.33894815037538,10.6669865555207,-29.9527656106568));
#15818=CARTESIAN_POINT('Ctrl Pts',(1.45983743180848,10.6504165882816,-30.3417420854264));
#15819=CARTESIAN_POINT('Ctrl Pts',(1.48571264641705,10.6468699425138,-30.4249988443635));
#15820=CARTESIAN_POINT('Ctrl Pts',(1.51173109034313,10.6432075943476,-30.5082046616496));
#15821=CARTESIAN_POINT('Ctrl Pts',(1.53789373804599,10.6394258703538,-30.5913583746403));
#15822=CARTESIAN_POINT('Ctrl Pts',(1.64034562245794,10.6246167900997,-30.916984996552));
#15823=CARTESIAN_POINT('Ctrl Pts',(1.74501002043019,10.6079804855204,-31.2418078298122));
#15824=CARTESIAN_POINT('Ctrl Pts',(1.85195771749001,10.5892767805306,-31.5656535771417));
#15825=CARTESIAN_POINT('Ctrl Pts',(1.97412810454714,10.5679108330552,-31.9355947856553));
#15826=CARTESIAN_POINT('Ctrl Pts',(2.09934183075205,10.543837289415,-32.3044816614734));
#15827=CARTESIAN_POINT('Ctrl Pts',(2.22770551319777,10.5166457094501,-32.6720516065798));
#15828=CARTESIAN_POINT('Ctrl Pts',(2.26750916253881,10.5082140090398,-32.7860295240449));
#15829=CARTESIAN_POINT('Ctrl Pts',(2.30761563827692,10.4994821320178,-32.899880823024));
#15830=CARTESIAN_POINT('Ctrl Pts',(2.34802797257454,10.4904368183652,-33.0135977355685));
#15831=CARTESIAN_POINT('Ctrl Pts',(2.47153733386496,10.4627922654998,-33.3611426987683));
#15832=CARTESIAN_POINT('Ctrl Pts',(2.59790667387361,10.4322221872737,-33.7074132218573));
#15833=CARTESIAN_POINT('Ctrl Pts',(2.72723242618058,10.3983029238487,-34.0520766794073));
#15834=CARTESIAN_POINT('Ctrl Pts',(2.73855742948338,10.3953326278058,-34.0822587175975));
#15835=CARTESIAN_POINT('Ctrl Pts',(2.74990510056545,10.3923366167857,-34.1124284238273));
#15836=CARTESIAN_POINT('Ctrl Pts',(2.76127550222649,10.3893145876333,-34.1425855701582));
#15837=CARTESIAN_POINT('Ctrl Pts',(2.82688668915726,10.3718764244496,-34.3166028321864));
#15838=CARTESIAN_POINT('Ctrl Pts',(2.89333478214233,10.353545519685,-34.4903953506847));
#15839=CARTESIAN_POINT('Ctrl Pts',(2.96045216056549,10.3343182822429,-34.6634673771716));
#15840=CARTESIAN_POINT('Ctrl Pts',(2.97372789147147,10.3305151594698,-34.6977008008388));
#15841=CARTESIAN_POINT('Ctrl Pts',(2.98702974707013,10.3266769758976,-34.7319058845362));
#15842=CARTESIAN_POINT('Ctrl Pts',(3.00035633927968,10.3228037152108,-34.7660785653831));
#15843=CARTESIAN_POINT('Ctrl Pts',(3.05923669243154,10.3056906413283,-34.9170623641498));
#15844=CARTESIAN_POINT('Ctrl Pts',(3.11875120969117,10.2878492854875,-35.067790011159));
#15845=CARTESIAN_POINT('Ctrl Pts',(3.17880504322561,10.2692598806997,-35.2179476948885));
#15846=CARTESIAN_POINT('Ctrl Pts',(3.26834234003258,10.2415439971999,-35.4418253777051));
#15847=CARTESIAN_POINT('Ctrl Pts',(3.35914405717775,10.2121611770426,-35.664696596617));
#15848=CARTESIAN_POINT('Ctrl Pts',(3.45130806413947,10.1809247273851,-35.8865571686193));
#15849=CARTESIAN_POINT('Ctrl Pts',(3.5428378271197,10.1499032372422,-36.1068909652874));
#15850=CARTESIAN_POINT('Ctrl Pts',(3.63571123956681,10.1170536586842,-36.32622788243));
#15851=CARTESIAN_POINT('Ctrl Pts',(3.7300172497872,10.0821701110365,-36.5445177725575));
#15852=CARTESIAN_POINT('Ctrl Pts',(3.82530348246398,10.0469239816542,-36.7650765811962));
#15853=CARTESIAN_POINT('Ctrl Pts',(3.92205232501441,10.009601592218,-36.9845664957216));
#15854=CARTESIAN_POINT('Ctrl Pts',(4.02034750426584,9.9699644333692,-37.2028890352372));
#15855=CARTESIAN_POINT('Ctrl Pts',(4.11864268351727,9.93032727452043,-37.4212115747528));
#15856=CARTESIAN_POINT('Ctrl Pts',(4.21848427264205,9.88837553750986,-37.6383666358546));
#15857=CARTESIAN_POINT('Ctrl Pts',(4.31994691208668,9.84384174532475,-37.8542100277662));
#15858=CARTESIAN_POINT('Ctrl Pts',(4.4053548532018,9.80635465134219,-38.0358999562699));
#15859=CARTESIAN_POINT('Ctrl Pts',(4.49191389406382,9.76703709863316,-38.2166288566652));
#15860=CARTESIAN_POINT('Ctrl Pts',(4.57972460013783,9.72568071370586,-38.3963878420291));
#15861=CARTESIAN_POINT('Ctrl Pts',(4.6608255353663,9.6874844430547,-38.5624111264386));
#15862=CARTESIAN_POINT('Ctrl Pts',(4.74299414110047,9.64754886738777,-38.7276065504812));
#15863=CARTESIAN_POINT('Ctrl Pts',(4.82630358598146,9.60569069335151,-38.8919330774156));
#15864=CARTESIAN_POINT('Ctrl Pts',(4.90218572876345,9.56756430872188,-39.0416093715923));
#15865=CARTESIAN_POINT('Ctrl Pts',(4.97901568325303,9.52783933124103,-39.1905324952375));
#15866=CARTESIAN_POINT('Ctrl Pts',(5.05684473081711,9.48635288415211,-39.3385881853721));
#15867=CARTESIAN_POINT('Ctrl Pts',(5.13087767175055,9.44688993576715,-39.4794224690444));
#15868=CARTESIAN_POINT('Ctrl Pts',(5.20580158441064,9.40584069224065,-39.6194691946357));
#15869=CARTESIAN_POINT('Ctrl Pts',(5.28171573049725,9.36301668766185,-39.7587113464906));
#15870=CARTESIAN_POINT('Ctrl Pts',(5.35632406157866,9.32092930768656,-39.8955583651507));
#15871=CARTESIAN_POINT('Ctrl Pts',(5.43188888911729,9.27712777578422,-40.0316282751385));
#15872=CARTESIAN_POINT('Ctrl Pts',(5.50849864130836,9.23141218451009,-40.1668597125731));
#15873=CARTESIAN_POINT('Ctrl Pts',(5.54813074309405,9.20776238908913,-40.2368182483959));
#15874=CARTESIAN_POINT('Ctrl Pts',(5.58804239379582,9.18359999168247,-40.3065516421872));
#15875=CARTESIAN_POINT('Ctrl Pts',(5.62824515816392,9.15889493550518,-40.3760464775971));
#15876=CARTESIAN_POINT('Ctrl Pts',(5.70446273045616,9.11205837004079,-40.5077968118102));
#15877=CARTESIAN_POINT('Ctrl Pts',(5.7817269628771,9.06327125490934,-40.6386852930296));
#15878=CARTESIAN_POINT('Ctrl Pts',(5.86011071648322,9.01230330186345,-40.7685536452058));
#15879=CARTESIAN_POINT('Ctrl Pts',(5.91380013799179,8.97739249715434,-40.8575077508697));
#15880=CARTESIAN_POINT('Ctrl Pts',(5.96788613468613,8.9415420249761,-40.9457714335191));
#15881=CARTESIAN_POINT('Ctrl Pts',(6.02244782126847,8.90464048909893,-41.0333877657161));
#15882=CARTESIAN_POINT('Ctrl Pts',(6.07897394762721,8.8664103497744,-41.1241586376426));
#15883=CARTESIAN_POINT('Ctrl Pts',(6.13590921669299,8.82711651296097,-41.2140642889579));
#15884=CARTESIAN_POINT('Ctrl Pts',(6.19324882975252,8.78670052824233,-41.3030092867015));
#15885=CARTESIAN_POINT('Ctrl Pts',(6.24844339663954,8.74779648524605,-41.3886268966795));
#15886=CARTESIAN_POINT('Ctrl Pts',(6.30401276283055,8.70785255316284,-41.4733544904255));
#15887=CARTESIAN_POINT('Ctrl Pts',(6.35993531577454,8.66681658635222,-41.5570616068614));
#15888=CARTESIAN_POINT('Ctrl Pts',(6.37627760299589,8.65482461673137,-41.5815233967342));
#15889=CARTESIAN_POINT('Ctrl Pts',(6.39264992778209,8.64273939541427,-41.6058977283417));
#15890=CARTESIAN_POINT('Ctrl Pts',(6.40905142809488,8.63055964540417,-41.6301805523135));
#15891=CARTESIAN_POINT('Ctrl Pts',(6.47123616750745,8.58438127354527,-41.7222465860356));
#15892=CARTESIAN_POINT('Ctrl Pts',(6.53391610435516,8.53680207855314,-41.8131519097231));
#15893=CARTESIAN_POINT('Ctrl Pts',(6.59715617547662,8.48765892211572,-41.9028104103885));
#15894=CARTESIAN_POINT('Ctrl Pts',(6.64315450335493,8.45191413273301,-41.9680244596069));
#15895=CARTESIAN_POINT('Ctrl Pts',(6.6894489682741,8.41534166165083,-42.0325779154381));
#15896=CARTESIAN_POINT('Ctrl Pts',(6.73606096464285,8.37787413518862,-42.0964212692311));
#15897=CARTESIAN_POINT('Ctrl Pts',(6.79685557701873,8.32900637741371,-42.1796902181925));
#15898=CARTESIAN_POINT('Ctrl Pts',(6.85815567161734,8.27864483486139,-42.261713048634));
#15899=CARTESIAN_POINT('Ctrl Pts',(6.92001935255261,8.22661679429675,-42.3423866349852));
#15900=CARTESIAN_POINT('Ctrl Pts',(6.98076429133924,8.17552962826482,-42.4216013210581));
#15901=CARTESIAN_POINT('Ctrl Pts',(7.04205264218131,8.12283573127723,-42.4995151699838));
#15902=CARTESIAN_POINT('Ctrl Pts',(7.10392919603158,8.06835766790845,-42.5759835345004));
#15903=CARTESIAN_POINT('Ctrl Pts',(7.13634361987152,8.03981899007116,-42.6160419705888));
#15904=CARTESIAN_POINT('Ctrl Pts',(7.16891928857766,8.01079045547862,-42.655702938709));
#15905=CARTESIAN_POINT('Ctrl Pts',(7.20166145050638,7.98124492776824,-42.6949402656682));
#15906=CARTESIAN_POINT('Ctrl Pts',(7.26062011125617,7.92804243158788,-42.7655947402859));
#15907=CARTESIAN_POINT('Ctrl Pts',(7.32024875525727,7.87304406856483,-42.8350315342943));
#15908=CARTESIAN_POINT('Ctrl Pts',(7.38032570976224,7.81630681970278,-42.9027542881581));
#15909=CARTESIAN_POINT('Ctrl Pts',(7.43888788904424,7.76100013900957,-42.9687694862639));
#15910=CARTESIAN_POINT('Ctrl Pts',(7.49787602412951,7.70404110584752,-43.0331559084488));
#15911=CARTESIAN_POINT('Ctrl Pts',(7.5570925960424,7.64549410734287,-43.0955009362299));
#15912=CARTESIAN_POINT('Ctrl Pts',(7.60084850666218,7.60223295339776,-43.1415685043963));
#15913=CARTESIAN_POINT('Ctrl Pts',(7.64472929783644,7.55810501350542,-43.1865224376846));
#15914=CARTESIAN_POINT('Ctrl Pts',(7.68865828488642,7.51314073311568,-43.2302138221615));
#15915=CARTESIAN_POINT('Ctrl Pts',(7.7355025987926,7.46519241910731,-43.2768047651101));
#15916=CARTESIAN_POINT('Ctrl Pts',(7.78245593008508,7.41623893382565,-43.3220139301323));
#15917=CARTESIAN_POINT('Ctrl Pts',(7.82953376245136,7.36619990654318,-43.3657719702781));
#15918=CARTESIAN_POINT('Ctrl Pts',(7.88858871032279,7.30343040337846,-43.4206625344753));
#15919=CARTESIAN_POINT('Ctrl Pts',(7.94783714305828,7.238948646025,-43.4732401474933));
#15920=CARTESIAN_POINT('Ctrl Pts',(8.00729466189754,7.172574346441,-43.5232677541047));
#15921=CARTESIAN_POINT('Ctrl Pts',(8.06675218073681,7.10620004685699,-43.5732953607162));
#15922=CARTESIAN_POINT('Ctrl Pts',(8.12641885383395,7.03793330216104,-43.6207732738916));
#15923=CARTESIAN_POINT('Ctrl Pts',(8.18629907590927,6.96757843036124,-43.6654106856205));
#15924=CARTESIAN_POINT('Ctrl Pts',(8.24126515839428,6.90299731238031,-43.7063848765967));
#15925=CARTESIAN_POINT('Ctrl Pts',(8.29641393605819,6.83664939573324,-43.744957765715));
#15926=CARTESIAN_POINT('Ctrl Pts',(8.35154990840288,6.76861619740753,-43.7807474995614));
#15927=CARTESIAN_POINT('Ctrl Pts',(8.38817263187795,6.72342680646271,-43.8045199564559));
#15928=CARTESIAN_POINT('Ctrl Pts',(8.42478989219045,6.67749412546476,-43.8270654294899));
#15929=CARTESIAN_POINT('Ctrl Pts',(8.46134684828429,6.63084530908934,-43.8482841545948));
#15930=CARTESIAN_POINT('Ctrl Pts',(8.51315982689053,6.56472891475219,-43.8783579207774));
#15931=CARTESIAN_POINT('Ctrl Pts',(8.56478254778382,6.49724643073336,-43.9056970713917));
#15932=CARTESIAN_POINT('Ctrl Pts',(8.61592734889603,6.42870112265509,-43.9300233884923));
#15933=CARTESIAN_POINT('Ctrl Pts',(8.63991916904507,6.39654679479161,-43.9414347658381));
#15934=CARTESIAN_POINT('Ctrl Pts',(8.66380578489985,6.36415902895718,-43.9521837717895));
#15935=CARTESIAN_POINT('Ctrl Pts',(8.6875574875569,6.33157122947104,-43.9622450359249));
#15936=CARTESIAN_POINT('Ctrl Pts',(8.7100395152484,6.30072544881139,-43.9717684634522));
#15937=CARTESIAN_POINT('Ctrl Pts',(8.73244740634613,6.26963643100526,-43.9806964803169));
#15938=CARTESIAN_POINT('Ctrl Pts',(8.75476238684806,6.23831993006402,-43.9890041654444));
#15939=CARTESIAN_POINT('Ctrl Pts',(8.81378476346905,6.15548883313143,-44.0109777145769));
#15940=CARTESIAN_POINT('Ctrl Pts',(8.87227654185962,6.07091644084457,-44.0286851829401));
#15941=CARTESIAN_POINT('Ctrl Pts',(8.93014977420605,5.98455779150124,-44.0417897287885));
#15942=CARTESIAN_POINT('Ctrl Pts',(8.96103257271427,5.93847436641886,-44.0487826861984));
#15943=CARTESIAN_POINT('Ctrl Pts',(8.99173501046401,5.89188620681016,-44.0544592798447));
#15944=CARTESIAN_POINT('Ctrl Pts',(9.02210965563433,5.84500106363286,-44.0587554593269));
#15945=CARTESIAN_POINT('Ctrl Pts',(9.02425298420913,5.841692703435,-44.0590586109915));
#15946=CARTESIAN_POINT('Ctrl Pts',(9.02639468638797,5.83838286767633,-44.0593549098961));
#15947=CARTESIAN_POINT('Ctrl Pts',(9.02853471298425,5.83507163079148,-44.0596443429017));
#15948=CARTESIAN_POINT('Ctrl Pts',(9.05887335222645,5.7881290266811,-44.0637475645889));
#15949=CARTESIAN_POINT('Ctrl Pts',(9.08887701332726,5.74090566265223,-44.066488459586));
#15950=CARTESIAN_POINT('Ctrl Pts',(9.11841089903929,5.6936166717973,-44.0678417494594));
#15951=CARTESIAN_POINT('Ctrl Pts',(9.13351347481917,5.66943476851156,-44.0685337736334));
#15952=CARTESIAN_POINT('Ctrl Pts',(9.14849342988732,5.64523582718803,-44.0688637450226));
#15953=CARTESIAN_POINT('Ctrl Pts',(9.16333413070452,5.62104938331967,-44.0688333130625));
#15954=CARTESIAN_POINT('Ctrl Pts',(9.27932019108639,5.43202257296252,-44.0685954750253));
#15955=CARTESIAN_POINT('Ctrl Pts',(9.38822404799286,5.24145243096134,-44.0465840027421));
#15956=CARTESIAN_POINT('Ctrl Pts',(9.49037895942472,5.04946426392216,-44.0034442094552));
#15957=CARTESIAN_POINT('Ctrl Pts',(9.52019775443346,4.99342333826522,-43.9908517982367));
#15958=CARTESIAN_POINT('Ctrl Pts',(9.54944152472417,4.93726132141394,-43.976459373685));
#15959=CARTESIAN_POINT('Ctrl Pts',(9.57811856097516,4.88098064194911,-43.9602834423684));
#15960=CARTESIAN_POINT('Ctrl Pts',(9.60473017663623,4.8287534941381,-43.9452725582802));
#15961=CARTESIAN_POINT('Ctrl Pts',(9.63080521238708,4.77651667385361,-43.9287441414905));
#15962=CARTESIAN_POINT('Ctrl Pts',(9.65625625560043,4.72448428046875,-43.9108030046278));
#15963=CARTESIAN_POINT('Ctrl Pts',(9.6818871281714,4.67208424196225,-43.8927351011296));
#15964=CARTESIAN_POINT('Ctrl Pts',(9.70688517903134,4.61989153984466,-43.873234453661));
#15965=CARTESIAN_POINT('Ctrl Pts',(9.73117419853334,4.5681320494209,-43.8524589796902));
#15966=CARTESIAN_POINT('Ctrl Pts',(9.74028176074149,4.54872398814212,-43.8446688784234));
#15967=CARTESIAN_POINT('Ctrl Pts',(9.74928976254928,4.5293769075458,-43.8367000449073));
#15968=CARTESIAN_POINT('Ctrl Pts',(9.7581946429713,4.51010296781278,-43.8285626112942));
#15969=CARTESIAN_POINT('Ctrl Pts',(9.79687625800233,4.4263795395857,-43.7932146830296));
#15970=CARTESIAN_POINT('Ctrl Pts',(9.83381278159481,4.34360625272283,-43.7545078688968));
#15971=CARTESIAN_POINT('Ctrl Pts',(9.86916355131065,4.26172191433118,-43.7127052462923));
#15972=CARTESIAN_POINT('Ctrl Pts',(9.88520563769071,4.22456301679624,-43.6937353260297));
#15973=CARTESIAN_POINT('Ctrl Pts',(9.90092094238594,4.18758710590883,-43.6741272004138));
#15974=CARTESIAN_POINT('Ctrl Pts',(9.91632327429603,4.15078809569389,-43.6539021212314));
#15975=CARTESIAN_POINT('Ctrl Pts',(9.92074536029067,4.14022291708081,-43.6480954005403));
#15976=CARTESIAN_POINT('Ctrl Pts',(9.92514262036429,4.12966998485364,-43.6422375099563));
#15977=CARTESIAN_POINT('Ctrl Pts',(9.92951515271414,4.11912962069325,-43.6363292143048));
#15978=CARTESIAN_POINT('Ctrl Pts',(9.96375695633186,4.03658681694431,-43.5900606716785));
#15979=CARTESIAN_POINT('Ctrl Pts',(9.99651370172761,3.95469685159093,-43.5405520961867));
#15980=CARTESIAN_POINT('Ctrl Pts',(10.0277460947657,3.87385088063219,-43.4883126423055));
#15981=CARTESIAN_POINT('Ctrl Pts',(10.0550083067909,3.80328184037399,-43.4427137326716));
#15982=CARTESIAN_POINT('Ctrl Pts',(10.0811094656132,3.73350767064565,-43.3950344467413));
#15983=CARTESIAN_POINT('Ctrl Pts',(10.106039106629,3.66476105295902,-43.3456209213272));
#15984=CARTESIAN_POINT('Ctrl Pts',(10.1302917164198,3.5978814339494,-43.2975493526476));
#15985=CARTESIAN_POINT('Ctrl Pts',(10.1534368297528,3.53198496973714,-43.2478594105363));
#15986=CARTESIAN_POINT('Ctrl Pts',(10.1755279180874,3.46715135906705,-43.1968184788605));
#15987=CARTESIAN_POINT('Ctrl Pts',(10.2029132663665,3.3867799902371,-43.1335452861024));
#15988=CARTESIAN_POINT('Ctrl Pts',(10.2287275666923,3.30790465592359,-43.0680938991004));
#15989=CARTESIAN_POINT('Ctrl Pts',(10.2531383414356,3.23042635812073,-43.0007320402055));
#15990=CARTESIAN_POINT('Ctrl Pts',(10.2557783158317,3.22204724174239,-42.993446995604));
#15991=CARTESIAN_POINT('Ctrl Pts',(10.2584018562662,3.21368446158842,-42.9861395596833));
#15992=CARTESIAN_POINT('Ctrl Pts',(10.2610091614446,3.20533788995049,-42.9788100374539));
#15993=CARTESIAN_POINT('Ctrl Pts',(10.2869627757754,3.12225451978362,-42.9058505715865));
#15994=CARTESIAN_POINT('Ctrl Pts',(10.3113115241219,3.04077434106045,-42.8307166031248));
#15995=CARTESIAN_POINT('Ctrl Pts',(10.3342333296949,2.96077179059331,-42.7536407000173));
#15996=CARTESIAN_POINT('Ctrl Pts',(10.3567452030436,2.88220000103875,-42.6779432178331));
#15997=CARTESIAN_POINT('Ctrl Pts',(10.3778805376574,2.80505340516852,-42.6003724329015));
#15998=CARTESIAN_POINT('Ctrl Pts',(10.3977881451373,2.72920873901186,-42.521098874524));
#15999=CARTESIAN_POINT('Ctrl Pts',(10.4182395169913,2.65129242122844,-42.4396600063825));
#16000=CARTESIAN_POINT('Ctrl Pts',(10.437395150398,2.57475010596009,-42.3564242397273));
#16001=CARTESIAN_POINT('Ctrl Pts',(10.4553967161795,2.4994440913569,-42.2715232305475));
#16002=CARTESIAN_POINT('Ctrl Pts',(10.4733982819609,2.42413807675371,-42.1866222213677));
#16003=CARTESIAN_POINT('Ctrl Pts',(10.4902456755578,2.35006832730552,-42.1000558923328));
#16004=CARTESIAN_POINT('Ctrl Pts',(10.5060622858798,2.27709359605912,-42.0119030752));
#16005=CARTESIAN_POINT('Ctrl Pts',(10.5060622858798,2.27709359605911,-42.0119030752));
#16006=CARTESIAN_POINT('Ctrl Pts',(10.5169067394724,2.22705941867769,-41.9514622401426));
#16007=CARTESIAN_POINT('Ctrl Pts',(10.5275633885531,2.1761749151871,-41.891851215819));
#16008=CARTESIAN_POINT('Ctrl Pts',(10.538021234015,2.12430565161473,-41.8331476931717));
#16009=CARTESIAN_POINT('Ctrl Pts',(10.5481140632636,2.0742468108728,-41.7764931334421));
#16010=CARTESIAN_POINT('Ctrl Pts',(10.5580217184636,2.02327075551396,-41.720683755564));
#16011=CARTESIAN_POINT('Ctrl Pts',(10.5677264286351,1.97125463207302,-41.6658361080088));
#16012=CARTESIAN_POINT('Ctrl Pts',(10.577366504854,1.91958493913805,-41.6113537490803));
#16013=CARTESIAN_POINT('Ctrl Pts',(10.5868063647818,1.86688899827979,-41.5578200279073));
#16014=CARTESIAN_POINT('Ctrl Pts',(10.596020405635,1.81304425509015,-41.5053993769448));
#16015=CARTESIAN_POINT('Ctrl Pts',(10.6089510763027,1.7374803789945,-41.4318340233089));
#16016=CARTESIAN_POINT('Ctrl Pts',(10.6214790124672,1.6594009572013,-41.3602207649006));
#16017=CARTESIAN_POINT('Ctrl Pts',(10.6334356950941,1.57886173480814,-41.2915861316767));
#16018=CARTESIAN_POINT('Ctrl Pts',(10.645584702412,1.49702702924925,-41.2218475020484));
#16019=CARTESIAN_POINT('Ctrl Pts',(10.6571438559943,1.41265274997818,-41.1551841633644));
#16020=CARTESIAN_POINT('Ctrl Pts',(10.6679353251557,1.32579537129823,-41.0927266082373));
#16021=CARTESIAN_POINT('Ctrl Pts',(10.6696041593524,1.3123634129981,-41.0830679322705));
#16022=CARTESIAN_POINT('Ctrl Pts',(10.6712546338859,1.29887206832203,-41.0735099376932));
#16023=CARTESIAN_POINT('Ctrl Pts',(10.6728860907067,1.28532154205633,-41.0640569152563));
#16024=CARTESIAN_POINT('Ctrl Pts',(10.6780427035461,1.24249183499117,-41.0341783574857));
#16025=CARTESIAN_POINT('Ctrl Pts',(10.683012291943,1.19904941834963,-41.0053284196112));
#16026=CARTESIAN_POINT('Ctrl Pts',(10.6877820649516,1.1549088847714,-40.9775991836193));
#16027=CARTESIAN_POINT('Ctrl Pts',(10.6931787645224,1.10496663423098,-40.9462252889483));
#16028=CARTESIAN_POINT('Ctrl Pts',(10.6983198661932,1.05413110185778,-40.9162884155456));
#16029=CARTESIAN_POINT('Ctrl Pts',(10.7031774103224,1.0022768629987,-40.8879610482626));
#16030=CARTESIAN_POINT('Ctrl Pts',(10.7079950829908,0.950848251617642,-40.859866196318));
#16031=CARTESIAN_POINT('Ctrl Pts',(10.7125338736272,0.898417599532796,-40.8333542553596));
#16032=CARTESIAN_POINT('Ctrl Pts',(10.7167580227179,0.844860405407882,-40.8086447312429));
#16033=CARTESIAN_POINT('Ctrl Pts',(10.7209821718086,0.791303211282969,-40.7839352071263));
#16034=CARTESIAN_POINT('Ctrl Pts',(10.7248917369913,0.736619490821813,-40.7610277021678));
#16035=CARTESIAN_POINT('Ctrl Pts',(10.7284416967453,0.680682389925007,-40.7401983449226));
#16036=CARTESIAN_POINT('Ctrl Pts',(10.7325618263942,0.6157610601505,-40.7160235208966));
#16037=CARTESIAN_POINT('Ctrl Pts',(10.7361457670398,0.549937828478586,-40.6949585895212));
#16038=CARTESIAN_POINT('Ctrl Pts',(10.7391417726632,0.483347761177844,-40.677326442336));
#16039=CARTESIAN_POINT('Ctrl Pts',(10.7420813231653,0.418012481349758,-40.6600265458647));
#16040=CARTESIAN_POINT('Ctrl Pts',(10.7444548707266,0.351938987296829,-40.6460314697351));
#16041=CARTESIAN_POINT('Ctrl Pts',(10.7462224401773,0.285256656119436,-40.635597438802));
#16042=CARTESIAN_POINT('Ctrl Pts',(10.7479495066408,0.220102317863198,-40.6254024985715));
#16043=CARTESIAN_POINT('Ctrl Pts',(10.7490980470938,0.154366722172408,-40.6186073686596));
#16044=CARTESIAN_POINT('Ctrl Pts',(10.7496394673345,0.0881723560645576,
-40.6154020700289));
#16045=CARTESIAN_POINT('Ctrl Pts',(10.7498716753067,0.0597824689281062,
-40.6140273598879));
#16046=CARTESIAN_POINT('Ctrl Pts',(10.7499923177763,0.0313082169392265,
-40.6133123467264));
#16047=CARTESIAN_POINT('Ctrl Pts',(10.7499996458547,0.0027593703269405,
-40.6132691037546));
#16048=CARTESIAN_POINT('Ctrl Pts',(10.749999802738,0.00214818153665405,
-40.6132681779862));
#16049=CARTESIAN_POINT('Ctrl Pts',(10.7499999071778,0.0015369585373491,
-40.6132675611916));
#16050=CARTESIAN_POINT('Ctrl Pts',(10.7499999591687,0.000925701661712846,
-40.613267253393));
#16051=CARTESIAN_POINT('Ctrl Pts',(10.7499999854151,0.000617123089545347,
-40.6132670980082));
#16052=CARTESIAN_POINT('Ctrl Pts',(10.7499999982932,0.000308555866768263,
-40.6132670215285));
#16053=CARTESIAN_POINT('Ctrl Pts',(10.7499999978076,2.23887749120318E-14,
-40.6132670239265));
#16054=CARTESIAN_POINT('Ctrl Pts',(1.18962879315414E-15,10.75,-25.));
#16055=CARTESIAN_POINT('Ctrl Pts',(1.18962879315414E-15,10.75,-25.));
#16056=CARTESIAN_POINT('Ctrl Pts',(1.18962879315414E-15,10.75,-25.));
#16057=CARTESIAN_POINT('Ctrl Pts',(-1.15016131432461,10.7499999999999,-25.006648030988));
#16058=CARTESIAN_POINT('Ctrl Pts',(-0.697561178987416,10.75,-25.5161421426786));
#16059=CARTESIAN_POINT('Ctrl Pts',(-0.245046068214511,10.75,-26.0262609450199));
#16060=CARTESIAN_POINT('Ctrl Pts',(-2.19083677072206,10.7494908638043,-24.9349427226934));
#16061=CARTESIAN_POINT('Ctrl Pts',(-1.34420969092897,10.7106820856761,-25.9683034993218));
#16062=CARTESIAN_POINT('Ctrl Pts',(-0.496527090382069,10.7416099797658,
-27.0012225209746));
#16063=CARTESIAN_POINT('Ctrl Pts',(-4.09261732542435,10.7476618345468,-24.7051472725922));
#16064=CARTESIAN_POINT('Ctrl Pts',(-2.54392000481286,10.5691405118102,-26.7758668839508));
#16065=CARTESIAN_POINT('Ctrl Pts',(-1.00994300948562,10.7055471241071,-28.8607675866442));
#16066=CARTESIAN_POINT('Ctrl Pts',(-4.95428344625941,10.7463421754083,-24.5465223290547));
#16067=CARTESIAN_POINT('Ctrl Pts',(-3.09790700297864,10.4667447449637,-27.1319561423712));
#16068=CARTESIAN_POINT('Ctrl Pts',(-1.27181081709599,10.6778869683601,-29.7457578698046));
#16069=CARTESIAN_POINT('Ctrl Pts',(-6.53601418471601,10.7430838699301,-24.1823266589109));
#16070=CARTESIAN_POINT('Ctrl Pts',(-4.12206177843065,10.2129395806112,-27.7692699064427));
#16071=CARTESIAN_POINT('Ctrl Pts',(-1.80395268087478,10.6009682382658,-31.4369952413258));
#16072=CARTESIAN_POINT('Ctrl Pts',(-7.25607013368073,10.7411450400571,-23.9764398761692));
#16073=CARTESIAN_POINT('Ctrl Pts',(-4.59251650314103,10.0612557981022,-28.0504746562229));
#16074=CARTESIAN_POINT('Ctrl Pts',(-2.07423302930113,10.5517189359563,-32.2432082848296));
#16075=CARTESIAN_POINT('Ctrl Pts',(-8.25213517452978,10.7379037306827,-23.6494263197586));
#16076=CARTESIAN_POINT('Ctrl Pts',(-5.23953949895351,9.8065491815586,-28.4251360768657));
#16077=CARTESIAN_POINT('Ctrl Pts',(-2.48491499500444,10.4597980983582,-33.398810870255));
#16078=CARTESIAN_POINT('Ctrl Pts',(-8.57010480087051,10.7367676447231,-23.5372843849539));
#16079=CARTESIAN_POINT('Ctrl Pts',(-5.44573262677527,9.71694384002046,-28.542284806436));
#16080=CARTESIAN_POINT('Ctrl Pts',(-2.62268926997625,10.4261480597686,-33.7750338413325));
#16081=CARTESIAN_POINT('Ctrl Pts',(-9.18102606498638,10.7344050046021,-23.30863371451));
#16082=CARTESIAN_POINT('Ctrl Pts',(-5.83934908124202,9.53003678683028,-28.7619697819756));
#16083=CARTESIAN_POINT('Ctrl Pts',(-2.89985851712548,10.3524819706059,-34.5101434304204));
#16084=CARTESIAN_POINT('Ctrl Pts',(-9.47464373380329,10.7331752085148,-23.191823577973));
#16085=CARTESIAN_POINT('Ctrl Pts',(-6.02717999588007,9.43244730398067,-28.8647092882211));
#16086=CARTESIAN_POINT('Ctrl Pts',(-3.03960350979001,10.312348987489,-34.8698754329709));
#16087=CARTESIAN_POINT('Ctrl Pts',(-10.8743639584978,10.7269099708188,-22.6058840900476));
#16088=CARTESIAN_POINT('Ctrl Pts',(-6.91554393551079,8.93206015782835,-29.3412703833179));
#16089=CARTESIAN_POINT('Ctrl Pts',(-3.73556853847291,10.0969166520402,-36.610324947681));
#16090=CARTESIAN_POINT('Ctrl Pts',(-11.786715064346,10.7215232478652,-22.1318450209703));
#16091=CARTESIAN_POINT('Ctrl Pts',(-7.45662740722064,8.49731281061401,-29.6013587996896));
#16092=CARTESIAN_POINT('Ctrl Pts',(-4.28614638191611,9.87708772192581,-37.8266979161691));
#16093=CARTESIAN_POINT('Ctrl Pts',(-12.9727671076994,10.7138050072996,-21.4442712536845));
#16094=CARTESIAN_POINT('Ctrl Pts',(-8.07505242268525,7.8660244748673,-29.8593172169878));
#16095=CARTESIAN_POINT('Ctrl Pts',(-5.09636724548306,9.46999968678062,-39.4245954567256));
#16096=CARTESIAN_POINT('Ctrl Pts',(-13.3368506180522,10.7112891987338,-21.218445186463));
#16097=CARTESIAN_POINT('Ctrl Pts',(-8.2491495137034,7.65808992648553,-29.922901554541));
#16098=CARTESIAN_POINT('Ctrl Pts',(-5.36385054816499,9.32136836042159,-39.9190359944887));
#16099=CARTESIAN_POINT('Ctrl Pts',(-13.8463351446538,10.7076931453776,-20.8854998552494));
#16100=CARTESIAN_POINT('Ctrl Pts',(-8.46819971826319,7.35863129856602,-29.9878091014236));
#16101=CARTESIAN_POINT('Ctrl Pts',(-5.76043976597223,9.07765988049979,-40.6045618673054));
#16102=CARTESIAN_POINT('Ctrl Pts',(-14.0100297822138,10.7065239150771,-20.7754673024019));
#16103=CARTESIAN_POINT('Ctrl Pts',(-8.53427798096343,7.26071615271009,-30.0043537934624));
#16104=CARTESIAN_POINT('Ctrl Pts',(-5.89186327262027,8.99295832117412,-40.8236913089009));
#16105=CARTESIAN_POINT('Ctrl Pts',(-14.326557040794,10.7042582843347,-20.5572849348335));
#16106=CARTESIAN_POINT('Ctrl Pts',(-8.65359144673208,7.07010518902838,-30.0276372056063));
#16107=CARTESIAN_POINT('Ctrl Pts',(-6.15303145469329,8.81632327601373,-41.2430881438711));
#16108=CARTESIAN_POINT('Ctrl Pts',(-14.478708980816,10.70316683247,-20.44959270127));
#16109=CARTESIAN_POINT('Ctrl Pts',(-8.70651740632404,6.97784314538739,-30.0342812550096));
#16110=CARTESIAN_POINT('Ctrl Pts',(-6.2822285175318,8.72473808032737,-41.4424366493996));
#16111=CARTESIAN_POINT('Ctrl Pts',(-15.2075066075735,10.6979795227471,-19.9216990174728));
#16112=CARTESIAN_POINT('Ctrl Pts',(-8.94085821143954,6.53572588791244,-30.0442270217656));
#16113=CARTESIAN_POINT('Ctrl Pts',(-6.9162933700514,8.25388281284964,-42.3814019788264));
#16114=CARTESIAN_POINT('Ctrl Pts',(-15.6958872062974,10.6946691527437,-19.5294610636527));
#16115=CARTESIAN_POINT('Ctrl Pts',(-9.02988049743652,6.24831397587878,-29.9786352046968));
#16116=CARTESIAN_POINT('Ctrl Pts',(-7.39039954503943,7.83295516260822,-42.9577462277717));
#16117=CARTESIAN_POINT('Ctrl Pts',(-16.3468106290142,10.691138463815,-18.9727916173314));
#16118=CARTESIAN_POINT('Ctrl Pts',(-9.10237201213877,5.93389687773062,-29.7948677586647));
#16119=CARTESIAN_POINT('Ctrl Pts',(-8.04909500484054,7.13282851376216,-43.5698483134323));
#16120=CARTESIAN_POINT('Ctrl Pts',(-16.5497974875563,10.6901975107843,-18.7924848319928));
#16121=CARTESIAN_POINT('Ctrl Pts',(-9.11615528018351,5.84830420961477,-29.7188377297072));
#16122=CARTESIAN_POINT('Ctrl Pts',(-8.25987706424781,6.88793250317559,-43.7313745857345));
#16123=CARTESIAN_POINT('Ctrl Pts',(-16.838428413657,10.6891335560231,-18.527932522204));
#16124=CARTESIAN_POINT('Ctrl Pts',(-9.13155934276341,5.74903975065829,-29.5835434645598));
#16125=CARTESIAN_POINT('Ctrl Pts',(-8.56208087001509,6.50230282257902,-43.9067575462197));
#16126=CARTESIAN_POINT('Ctrl Pts',(-16.931739932865,10.688837856098,-18.4409474186566));
#16127=CARTESIAN_POINT('Ctrl Pts',(-9.13580403755556,5.72089613947525,-29.5349142032813));
#16128=CARTESIAN_POINT('Ctrl Pts',(-8.66022380779681,6.37099391565298,-43.9538118068058));
#16129=CARTESIAN_POINT('Ctrl Pts',(-17.1115634445619,10.6883619233172,-18.270761756668));
#16130=CARTESIAN_POINT('Ctrl Pts',(-9.14417010468671,5.67448452401008,-29.4318726265361));
#16131=CARTESIAN_POINT('Ctrl Pts',(-8.84930077011382,6.10564621923683,-44.0242038964093));
#16132=CARTESIAN_POINT('Ctrl Pts',(-17.1983679656057,10.6881805558801,-18.1872937563323));
#16133=CARTESIAN_POINT('Ctrl Pts',(-9.14830611568215,5.65612786905982,-29.3773294151916));
#16134=CARTESIAN_POINT('Ctrl Pts',(-8.94054219798206,5.97122136470856,-44.0477302440176));
#16135=CARTESIAN_POINT('Ctrl Pts',(-17.6191726876552,10.6875284847955,-17.7768657002981));
#16136=CARTESIAN_POINT('Ctrl Pts',(-9.17281269728736,5.58625383845738,-29.0892695495114));
#16137=CARTESIAN_POINT('Ctrl Pts',(-9.38050433358122,5.29047337500718,-44.1073526930303));
#16138=CARTESIAN_POINT('Ctrl Pts',(-17.9141135504146,10.6878308215939,-17.4708062072169));
#16139=CARTESIAN_POINT('Ctrl Pts',(-9.20577389365999,5.60207456542975,-28.8138270066121));
#16140=CARTESIAN_POINT('Ctrl Pts',(-9.68088377276871,4.71847711576912,-43.9723394445427));
#16141=CARTESIAN_POINT('Ctrl Pts',(-18.2589538640075,10.6887007240517,-17.0967280701274));
#16142=CARTESIAN_POINT('Ctrl Pts',(-9.31430913574479,5.66760812797665,-28.3986430019926));
#16143=CARTESIAN_POINT('Ctrl Pts',(-9.99167371036611,3.96929102897446,-43.5523436135201));
#16144=CARTESIAN_POINT('Ctrl Pts',(-18.3268647339594,10.6888993216382,-17.0221379112497));
#16145=CARTESIAN_POINT('Ctrl Pts',(-9.33939465884606,5.68300852364718,-28.3116880707622));
#16146=CARTESIAN_POINT('Ctrl Pts',(-10.0507078465264,3.8173439659334,-43.4552961639041));
#16147=CARTESIAN_POINT('Ctrl Pts',(-18.4599063361282,10.6893257513556,-16.8742773574252));
#16148=CARTESIAN_POINT('Ctrl Pts',(-9.39669476979905,5.71674608902978,-28.130888942994));
#16149=CARTESIAN_POINT('Ctrl Pts',(-10.1613705280412,3.51217769515325,-43.2359489845917));
#16150=CARTESIAN_POINT('Ctrl Pts',(-18.525020225263,10.6895533451493,-16.801031713128));
#16151=CARTESIAN_POINT('Ctrl Pts',(-9.42887151311381,5.73505897199891,-28.0371197976092));
#16152=CARTESIAN_POINT('Ctrl Pts',(-10.2130004334533,3.35902467638586,-43.1137730065137));
#16153=CARTESIAN_POINT('Ctrl Pts',(-18.7174485368953,10.6902545953255,-16.5820822167333));
#16154=CARTESIAN_POINT('Ctrl Pts',(-9.53687563692295,5.79224969484422,-27.7441005175946));
#16155=CARTESIAN_POINT('Ctrl Pts',(-10.3572302487592,2.89731244717209,-42.708321547074));
#16156=CARTESIAN_POINT('Ctrl Pts',(-18.8415676478173,10.6907456279116,-16.43750807407));
#16157=CARTESIAN_POINT('Ctrl Pts',(-9.62413492807353,5.83327722471964,-27.5336716867507));
#16158=CARTESIAN_POINT('Ctrl Pts',(-10.4389331022223,2.58709663538484,-42.3866080951754));
#16159=CARTESIAN_POINT('Ctrl Pts',(-18.9640555125017,10.6911940224261,-16.2915944549513));
#16160=CARTESIAN_POINT('Ctrl Pts',(-9.72768081900659,5.87165951671932,-27.3036545666179));
#16161=CARTESIAN_POINT('Ctrl Pts',(-10.5064904280787,2.27511733549709,-42.0095150580924));
#16162=CARTESIAN_POINT('',(-17.2858341932293,9.77439024390244,-18.4545876051761));
#16163=CARTESIAN_POINT('Origin',(-49.598387070549,10.75,-42.0119030752));
#16164=CARTESIAN_POINT('Ctrl Pts',(-17.2858341932293,9.77439024390244,-18.4545876051761));
#16165=CARTESIAN_POINT('Ctrl Pts',(-17.230849614275,9.81433280796118,-18.5283533855738));
#16166=CARTESIAN_POINT('Ctrl Pts',(-17.1734819746949,9.85746553470479,-18.598137817752));
#16167=CARTESIAN_POINT('Ctrl Pts',(-17.0519080073572,9.93927316613436,-18.7329980624538));
#16168=CARTESIAN_POINT('Ctrl Pts',(-16.9877799937368,9.97756355387077,-18.7983427112246));
#16169=CARTESIAN_POINT('Ctrl Pts',(-16.7876064605023,10.0797362530432,-18.9927736277449));
#16170=CARTESIAN_POINT('Ctrl Pts',(-16.644430688312,10.1320778149371,-19.1203515704376));
#16171=CARTESIAN_POINT('Ctrl Pts',(-16.200446986055,10.2641590938576,-19.5007895704327));
#16172=CARTESIAN_POINT('Ctrl Pts',(-15.8905894180578,10.3204314322063,-19.7454341656197));
#16173=CARTESIAN_POINT('Ctrl Pts',(-14.9458920693911,10.4612218351731,-20.4514044399693));
#16174=CARTESIAN_POINT('Ctrl Pts',(-14.2895068016006,10.5142230477087,-20.8884604785083));
#16175=CARTESIAN_POINT('Ctrl Pts',(-12.9348288042002,10.5988273843319,-21.7028449453777));
#16176=CARTESIAN_POINT('Ctrl Pts',(-12.2340573634712,10.6275795411286,-22.0806151123365));
#16177=CARTESIAN_POINT('Ctrl Pts',(-10.8051035470393,10.672309925593,-22.7688021724106));
#16178=CARTESIAN_POINT('Ctrl Pts',(-10.0759536654712,10.6880415610146,-23.0799285438411));
#16179=CARTESIAN_POINT('Ctrl Pts',(-7.84464084215434,10.7247738680017,-23.9142122954436));
#16180=CARTESIAN_POINT('Ctrl Pts',(-6.30784220188913,10.7354998258494,-24.3342560266836));
#16181=CARTESIAN_POINT('Ctrl Pts',(-3.96162521204357,10.7451589131064,-24.7482204101398));
#16182=CARTESIAN_POINT('Ctrl Pts',(-3.1741229733078,10.7471212251943,-24.8500338800463));
#16183=CARTESIAN_POINT('Ctrl Pts',(-1.98574081627447,10.7489410804811,-24.9478353565518));
#16184=CARTESIAN_POINT('Ctrl Pts',(-1.58913075295951,10.749354887983,-24.9712158778548));
#16185=CARTESIAN_POINT('Ctrl Pts',(-0.794943421248679,10.7498845226873,
-24.9995000067156));
#16186=CARTESIAN_POINT('Ctrl Pts',(-0.396138629816618,10.75,-25.0040317725612));
#16187=CARTESIAN_POINT('Ctrl Pts',(4.08240831242321E-16,10.75,-25.));
#16188=CARTESIAN_POINT('Ctrl Pts',(-19.0763027194419,10.75,-16.1584242596923));
#16189=CARTESIAN_POINT('Ctrl Pts',(-9.72158531033335,5.89651617104406,-27.202410868965));
#16190=CARTESIAN_POINT('Ctrl Pts',(-10.5060622858798,2.27709359605911,-42.0119030752));
#16191=CARTESIAN_POINT('Ctrl Pts',(-19.2216718028992,9.00616861666823,-15.9868045152475));
#16192=CARTESIAN_POINT('Ctrl Pts',(-10.054211023792,4.97457944704813,-27.0105294870454));
#16193=CARTESIAN_POINT('Ctrl Pts',(-10.5861279548367,1.90768633652585,-41.5656624370341));
#16194=CARTESIAN_POINT('Ctrl Pts',(-19.3319171300942,7.24098469274974,-15.8521571440323));
#16195=CARTESIAN_POINT('Ctrl Pts',(-10.3116563320604,4.01333959595937,-26.8528714213347));
#16196=CARTESIAN_POINT('Ctrl Pts',(-10.6468390893589,1.53380463935034,-41.2156085744383));
#16197=CARTESIAN_POINT('Ctrl Pts',(-19.4806014076805,3.66349219259715,-15.6690802167518));
#16198=CARTESIAN_POINT('Ctrl Pts',(-10.6587854631624,2.04350040512538,-26.6371988427526));
#16199=CARTESIAN_POINT('Ctrl Pts',(-10.7287253073072,0.776010661486689,
-40.7396085636003));
#16200=CARTESIAN_POINT('Ctrl Pts',(-19.5190486552012,1.85116909998969,-15.6207150822312));
#16201=CARTESIAN_POINT('Ctrl Pts',(-10.7495724464151,1.0318365325806,-26.578717448758));
#16202=CARTESIAN_POINT('Ctrl Pts',(-10.7498997026982,0.392119563051999,
-40.6138592138001));
#16203=CARTESIAN_POINT('Ctrl Pts',(-19.5192754939424,-0.446508782486855,
-15.6204316264581));
#16204=CARTESIAN_POINT('Ctrl Pts',(-10.75010500077,-0.248881490684448,-26.5783781675765));
#16205=CARTESIAN_POINT('Ctrl Pts',(-10.7500246316438,-0.0945806780637169,
-40.6131222287912));
#16206=CARTESIAN_POINT('Ctrl Pts',(-19.5169052717251,-0.907660808398219,
-15.6233948374126));
#16207=CARTESIAN_POINT('Ctrl Pts',(-10.7445382243028,-0.505954113601866,
-26.5819274926781));
#16208=CARTESIAN_POINT('Ctrl Pts',(-10.7487192580301,-0.192263126902217,
-40.6208265772774));
#16209=CARTESIAN_POINT('Ctrl Pts',(-19.507413247859,-1.82424936484475,-15.6352449935534));
#16210=CARTESIAN_POINT('Ctrl Pts',(-10.7222613599582,-1.01646923646727,
-26.5960974937392));
#16211=CARTESIAN_POINT('Ctrl Pts',(-10.7434916310807,-0.386417353144324,
-40.6516369832341));
#16212=CARTESIAN_POINT('Ctrl Pts',(-19.5002954912967,-2.28081367063997,
-15.6441267958189));
#16213=CARTESIAN_POINT('Ctrl Pts',(-10.705556116365,-1.27059431610894,-26.6067148813092));
#16214=CARTESIAN_POINT('Ctrl Pts',(-10.7395716055577,-0.483128018904318,
-40.6747296691341));
#16215=CARTESIAN_POINT('Ctrl Pts',(-19.4719617901058,-3.64544085441919,
-15.6794009404326));
#16216=CARTESIAN_POINT('Ctrl Pts',(-10.6391149691374,-2.02907825197536,
-26.6487780897149));
#16217=CARTESIAN_POINT('Ctrl Pts',(-10.7239671336519,-0.772186979014334,
-40.7664424451148));
#16218=CARTESIAN_POINT('Ctrl Pts',(-19.4437719857229,-4.54843815679108,
-15.7144269835628));
#16219=CARTESIAN_POINT('Ctrl Pts',(-10.5730189889065,-2.52952302522724,
-26.6904822440918));
#16220=CARTESIAN_POINT('Ctrl Pts',(-10.708441911361,-0.963462269665953,
-40.8575101572862));
#16221=CARTESIAN_POINT('Ctrl Pts',(-19.3321340685403,-7.23816397108207,
-15.851893583229));
#16222=CARTESIAN_POINT('Ctrl Pts',(-10.3121595644709,-4.01182480387595,
-26.8525659713277));
#16223=CARTESIAN_POINT('Ctrl Pts',(-10.6469585658025,-1.53320714658219,
-41.2149233163493));
#16224=CARTESIAN_POINT('Ctrl Pts',(-19.221715988843,-9.00563856695385,-15.9867523502327));
#16225=CARTESIAN_POINT('Ctrl Pts',(-10.0543097325788,-4.97430585631275,
-27.0104725449986));
#16226=CARTESIAN_POINT('Ctrl Pts',(-10.5861513134396,-1.90757856452286,
-41.5655322494524));
#16227=CARTESIAN_POINT('Ctrl Pts',(-19.0763027194419,-10.75,-16.1584242596923));
#16228=CARTESIAN_POINT('Ctrl Pts',(-9.72158531033335,-5.89651617104406,
-27.202410868965));
#16229=CARTESIAN_POINT('Ctrl Pts',(-10.5060622858798,-2.27709359605911,
-42.0119030752));
#16230=CARTESIAN_POINT('',(-17.2858341932293,-9.77439024390244,-18.4545876051761));
#16231=CARTESIAN_POINT('Origin',(-49.598387070549,-10.75,-42.0119030752));
#16232=CARTESIAN_POINT('Origin',(-58.1890816870435,-11.0623060839995,-60.5701599251957));
#16233=CARTESIAN_POINT('Origin',(-58.6872612779838,11.078510305597,-61.1099570363713));
#16234=CARTESIAN_POINT('Ctrl Pts',(2.51461494246785E-15,-10.75,-25.));
#16235=CARTESIAN_POINT('Ctrl Pts',(2.51461494246785E-15,-10.75,-25.));
#16236=CARTESIAN_POINT('Ctrl Pts',(2.51461494246785E-15,-10.75,-25.));
#16237=CARTESIAN_POINT('Ctrl Pts',(-0.245046068214529,-10.75,-26.02626094502));
#16238=CARTESIAN_POINT('Ctrl Pts',(-0.697525526200558,-10.7499999999999,
-25.5161823339491));
#16239=CARTESIAN_POINT('Ctrl Pts',(-1.15008999541957,-10.7499999999998,
-25.006728315021));
#16240=CARTESIAN_POINT('Ctrl Pts',(-0.496527090381411,-10.7416099797658,
-27.0012225209746));
#16241=CARTESIAN_POINT('Ctrl Pts',(-1.34414287446072,-10.7106845234903,
-25.9683849165885));
#16242=CARTESIAN_POINT('Ctrl Pts',(-2.19070342017083,-10.7494847515439,
-24.9351054852879));
#16243=CARTESIAN_POINT('Ctrl Pts',(-1.00994300948628,-10.7055471241071,
-28.8607675866442));
#16244=CARTESIAN_POINT('Ctrl Pts',(-2.54379890564962,-10.5691512803725,
-26.7760314755534));
#16245=CARTESIAN_POINT('Ctrl Pts',(-4.09237376553143,-10.7476337608733,
-24.7054729298822));
#16246=CARTESIAN_POINT('Ctrl Pts',(-1.27181081710183,-10.6778869683592,
-29.7457578698046));
#16247=CARTESIAN_POINT('Ctrl Pts',(-3.09776268237128,-10.4667614320226,
-27.1321627171777));
#16248=CARTESIAN_POINT('Ctrl Pts',(-4.95399181836562,-10.7462982550018,
-24.5469284888288));
#16249=CARTESIAN_POINT('Ctrl Pts',(-1.80395268086896,-10.6009682382667,
-31.4369952413258));
#16250=CARTESIAN_POINT('Ctrl Pts',(-4.1218780716154,-10.2129703313243,-27.7695605683977));
#16251=CARTESIAN_POINT('Ctrl Pts',(-6.53563598592608,-10.7430008167255,
-24.1828886339226));
#16252=CARTESIAN_POINT('Ctrl Pts',(-2.0742330292986,-10.5517189359568,-32.2432082848296));
#16253=CARTESIAN_POINT('Ctrl Pts',(-4.59231660856942,-10.0612947297469,
-28.0508074641415));
#16254=CARTESIAN_POINT('Ctrl Pts',(-7.25565349765545,-10.74103869806,-23.9770771433437));
#16255=CARTESIAN_POINT('Ctrl Pts',(-2.48491499500571,-10.4597980983579,
-33.398810870255));
#16256=CARTESIAN_POINT('Ctrl Pts',(-5.23932024815341,-9.80660117606759,
-28.4255319501264));
#16257=CARTESIAN_POINT('Ctrl Pts',(-8.25166520613066,-10.7377584476419,
-23.6501713397551));
#16258=CARTESIAN_POINT('Ctrl Pts',(-2.62268926997313,-10.4261480597694,
-33.7750338413325));
#16259=CARTESIAN_POINT('Ctrl Pts',(-5.44550771521678,-9.71700034224351,
-28.5427016989824));
#16260=CARTESIAN_POINT('Ctrl Pts',(-8.56961785539663,-10.7366087113668,
-23.5380644380174));
#16261=CARTESIAN_POINT('Ctrl Pts',(-2.8998585171286,-10.352481970605,-34.5101434304204));
#16262=CARTESIAN_POINT('Ctrl Pts',(-5.83911442424541,-9.53010244192036,
-28.7624286537232));
#16263=CARTESIAN_POINT('Ctrl Pts',(-9.18050627770339,-10.7342176806201,
-23.3094819695874));
#16264=CARTESIAN_POINT('Ctrl Pts',(-3.03960350979062,-10.3123489874888,
-34.8698754329709));
#16265=CARTESIAN_POINT('Ctrl Pts',(-6.02694125129918,-9.43251761908732,
-28.8651891758106));
#16266=CARTESIAN_POINT('Ctrl Pts',(-9.47410804388434,-10.7329731051953,
-23.1927050755687));
#16267=CARTESIAN_POINT('Ctrl Pts',(-3.73556853847047,-10.096916652041,-36.610324947681));
#16268=CARTESIAN_POINT('Ctrl Pts',(-6.91528845193507,-8.93215374399242,
-29.3418543891044));
#16269=CARTESIAN_POINT('Ctrl Pts',(-10.8737520539574,-10.7266325617244,
-22.6069251727742));
#16270=CARTESIAN_POINT('Ctrl Pts',(-4.28614638192033,-9.87708772192369,
-37.8266979161691));
#16271=CARTESIAN_POINT('Ctrl Pts',(-7.45637148838566,-8.49742418500439,
-29.6020227428502));
#16272=CARTESIAN_POINT('Ctrl Pts',(-11.7860488689348,-10.7211810659044,
-22.1329942424813));
#16273=CARTESIAN_POINT('Ctrl Pts',(-5.09636724548095,-9.46999968678168,
-39.4245954567256));
#16274=CARTESIAN_POINT('Ctrl Pts',(-8.07481027122082,-7.86615486962916,
-29.8600948238844));
#16275=CARTESIAN_POINT('Ctrl Pts',(-12.9720188517199,-10.7133699539135,
-21.4455569030438));
#16276=CARTESIAN_POINT('Ctrl Pts',(-5.36385054816499,-9.32136836042159,
-39.9190359944887));
#16277=CARTESIAN_POINT('Ctrl Pts',(-8.24891439361641,-7.65822546536235,
-29.923716129418));
#16278=CARTESIAN_POINT('Ctrl Pts',(-13.336075167167,-10.7108238610927,-21.2197719228705));
#16279=CARTESIAN_POINT('Ctrl Pts',(-5.76043976597223,-9.07765988049979,
-40.6045618673054));
#16280=CARTESIAN_POINT('Ctrl Pts',(-8.46797828136676,-7.35877187836447,
-29.9886773248984));
#16281=CARTESIAN_POINT('Ctrl Pts',(-13.8455182954065,-10.7071844997807,
-20.8868823819796));
#16282=CARTESIAN_POINT('Ctrl Pts',(-5.89186327261934,-8.99295832117475,
-40.8236913089009));
#16283=CARTESIAN_POINT('Ctrl Pts',(-8.53406163310364,-7.26085798014581,
-30.0052396273611));
#16284=CARTESIAN_POINT('Ctrl Pts',(-14.0091990745616,-10.7060011844055,
-20.776867424868));
#16285=CARTESIAN_POINT('Ctrl Pts',(-6.15303145469421,-8.81632327601311,
-41.2430881438711));
#16286=CARTESIAN_POINT('Ctrl Pts',(-8.65338623383247,-7.07024849551272,
-30.0285576215158));
#16287=CARTESIAN_POINT('Ctrl Pts',(-14.3256984012058,-10.7037082528389,
-20.5587183768881));
#16288=CARTESIAN_POINT('Ctrl Pts',(-6.28222851753179,-8.72473808032737,
-41.4424366493996));
#16289=CARTESIAN_POINT('Ctrl Pts',(-8.70631822275726,-6.97798667315792,
-30.0352185678562));
#16290=CARTESIAN_POINT('Ctrl Pts',(-14.4778363196157,-10.7026036448698,
-20.4510417956705));
#16291=CARTESIAN_POINT('Ctrl Pts',(-6.91629337005139,-8.25388281284964,
-42.3814019788264));
#16292=CARTESIAN_POINT('Ctrl Pts',(-8.94069092645878,-6.5358678551081,-30.0452464131274));
#16293=CARTESIAN_POINT('Ctrl Pts',(-15.2065644724196,-10.6973537837553,
-19.9232209063353));
#16294=CARTESIAN_POINT('Ctrl Pts',(-7.39039954503927,-7.83295516260838,
-42.9577462277717));
#16295=CARTESIAN_POINT('Ctrl Pts',(-9.02974446998217,-6.24844545337749,
-29.9797120796148));
#16296=CARTESIAN_POINT('Ctrl Pts',(-15.6948891167241,-10.6940034243733,
-19.5310256649458));
#16297=CARTESIAN_POINT('Ctrl Pts',(-8.04909500484061,-7.13282851376207,
-43.5698483134323));
#16298=CARTESIAN_POINT('Ctrl Pts',(-9.10228415266927,-5.93399688698298,
-29.7960168032289));
#16299=CARTESIAN_POINT('Ctrl Pts',(-16.345731657509,-10.6904299419629,-18.9744035104728));
#16300=CARTESIAN_POINT('Ctrl Pts',(-8.25987706425041,-6.88793250317227,
-43.7313745857345));
#16301=CARTESIAN_POINT('Ctrl Pts',(-9.1160837358347,-5.84839107335997,-29.7200085149803));
#16302=CARTESIAN_POINT('Ctrl Pts',(-16.5486921356379,-10.6894775511536,
-18.7941096148084));
#16303=CARTESIAN_POINT('Ctrl Pts',(-8.56208087001378,-6.50230282258068,
-43.9067575462197));
#16304=CARTESIAN_POINT('Ctrl Pts',(-9.13151165542614,-5.74910282786052,
-29.5847428705483));
#16305=CARTESIAN_POINT('Ctrl Pts',(-16.8372849488646,-10.6884006034147,
-18.529572922268));
#16306=CARTESIAN_POINT('Ctrl Pts',(-8.66022380779591,-6.37099391565426,
-43.9538118068058));
#16307=CARTESIAN_POINT('Ctrl Pts',(-9.13576418532011,-5.72095061576736,
-29.5361224647812));
#16308=CARTESIAN_POINT('Ctrl Pts',(-16.9305840510713,-10.6881012790773,
-18.4425923757168));
#16309=CARTESIAN_POINT('Ctrl Pts',(-8.84930077011471,-6.10564621923558,
-44.0242038964093));
#16310=CARTESIAN_POINT('Ctrl Pts',(-9.1441453635236,-5.67452070085838,-29.4330970036618));
#16311=CARTESIAN_POINT('Ctrl Pts',(-17.1103836503878,-10.687619483155,-18.2724145576342));
#16312=CARTESIAN_POINT('Ctrl Pts',(-8.94054219798145,-5.9712213647095,-44.0477302440176));
#16313=CARTESIAN_POINT('Ctrl Pts',(-9.14828867272208,-5.6561543229398,-29.3785610783257));
#16314=CARTESIAN_POINT('Ctrl Pts',(-17.1971766337535,-10.6874358631681,
-18.1889498635026));
#16315=CARTESIAN_POINT('Ctrl Pts',(-9.38050433358363,-5.29047337500344,
-44.1073526930303));
#16316=CARTESIAN_POINT('Ctrl Pts',(-9.17283018205915,-5.58622893784892,
-29.0905338638653));
#16317=CARTESIAN_POINT('Ctrl Pts',(-17.617926090303,-10.6867755856068,-17.7785353917849));
#16318=CARTESIAN_POINT('Ctrl Pts',(-9.68088377276682,-4.71847711577368,
-43.9723394445427));
#16319=CARTESIAN_POINT('Ctrl Pts',(-9.20581394722617,-5.60200007483861,
-28.8151049264038));
#16320=CARTESIAN_POINT('Ctrl Pts',(-17.9128300606806,-10.6870812437168,
-17.4724781108102));
#16321=CARTESIAN_POINT('Ctrl Pts',(-9.99167371036658,-3.96929102897332,
-43.5523436135201));
#16322=CARTESIAN_POINT('Ctrl Pts',(-9.31436628119189,-5.66746485048706,
-28.3999214347156));
#16323=CARTESIAN_POINT('Ctrl Pts',(-18.2576364829922,-10.6879611969071,
-17.0983927329858));
#16324=CARTESIAN_POINT('Ctrl Pts',(-10.0507078465267,-3.81734396593254,
-43.4552961639041));
#16325=CARTESIAN_POINT('Ctrl Pts',(-9.33945467389634,-5.68285111346893,
-28.3129657699404));
#16326=CARTESIAN_POINT('Ctrl Pts',(-18.3255411664155,-10.6881620996133,
-17.0238006013664));
#16327=CARTESIAN_POINT('Ctrl Pts',(-10.1613705280408,-3.51217769515411,
-43.2359489845917));
#16328=CARTESIAN_POINT('Ctrl Pts',(-9.39675929232103,-5.71656006988305,
-28.1321634919568));
#16329=CARTESIAN_POINT('Ctrl Pts',(-18.4585717202441,-10.6885934908853,
-16.8759350652419));
#16330=CARTESIAN_POINT('Ctrl Pts',(-10.2130004334533,-3.35902467638586,
-43.1137730065137));
#16331=CARTESIAN_POINT('Ctrl Pts',(-9.42893767629744,-5.73485848711403,
-28.0383919345897));
#16332=CARTESIAN_POINT('Ctrl Pts',(-18.5236807436346,-10.6888237382775,
-16.8026864178631));
#16333=CARTESIAN_POINT('Ctrl Pts',(-10.3585730211466,-2.89301392934481,
-42.7045468142075));
#16334=CARTESIAN_POINT('Ctrl Pts',(-9.53795019632931,-5.79253740708886,
-27.7426353598479));
#16335=CARTESIAN_POINT('Ctrl Pts',(-18.7178877505159,-10.6895397759366,
-16.5816878126578));
#16336=CARTESIAN_POINT('Ctrl Pts',(-10.4412106172238,-2.57843802588067,
-42.3776190357652));
#16337=CARTESIAN_POINT('Ctrl Pts',(-9.62664120342293,-5.83414789935946,
-27.529049966199));
#16338=CARTESIAN_POINT('Ctrl Pts',(-18.8436728020004,-10.6900438114354,
-16.4351079573943));
#16339=CARTESIAN_POINT('Ctrl Pts',(-10.509310471686,-2.26205520316976,-41.9936955835997));
#16340=CARTESIAN_POINT('Ctrl Pts',(-9.73208854795376,-5.87295961154644,
-27.2952574763174));
#16341=CARTESIAN_POINT('Ctrl Pts',(-18.9678208706686,-10.690502528869,-16.2871078568861));
#16342=CARTESIAN_POINT('Ctrl Pts',(0.,-10.75,-25.));
#16343=CARTESIAN_POINT('Ctrl Pts',(-1.58979632319829,-10.75,-25.0161723660006));
#16344=CARTESIAN_POINT('Ctrl Pts',(-3.17967643758472,-10.7483783455921,
-24.8861937318557));
#16345=CARTESIAN_POINT('Ctrl Pts',(-6.30793928508339,-10.7354991807564,
-24.3342319030052));
#16346=CARTESIAN_POINT('Ctrl Pts',(-7.8447242833345,-10.7247729855381,-23.9141859389712));
#16347=CARTESIAN_POINT('Ctrl Pts',(-10.0760168613864,-10.6880402750731,
-23.0799024938186));
#16348=CARTESIAN_POINT('Ctrl Pts',(-10.8051602308081,-10.6723084956847,
-22.768776762151));
#16349=CARTESIAN_POINT('Ctrl Pts',(-12.2341014639979,-10.6275778161729,
-22.0805919845415));
#16350=CARTESIAN_POINT('Ctrl Pts',(-12.9348666409598,-10.5988255131215,
-21.7028235613396));
#16351=CARTESIAN_POINT('Ctrl Pts',(-14.289532661915,-10.5142209407928,-20.8884435700559));
#16352=CARTESIAN_POINT('Ctrl Pts',(-14.9459122468717,-10.461219629094,-20.4513902261967));
#16353=CARTESIAN_POINT('Ctrl Pts',(-15.8906015391955,-10.3204292252429,
-19.7454246750972));
#16354=CARTESIAN_POINT('Ctrl Pts',(-16.200456592374,-10.2641568661887,-19.5007816886992));
#16355=CARTESIAN_POINT('Ctrl Pts',(-16.6444363232276,-10.1320758235242,
-19.1203465671852));
#16356=CARTESIAN_POINT('Ctrl Pts',(-16.7876108033257,-10.0797343600817,
-18.9927696062974));
#16357=CARTESIAN_POINT('Ctrl Pts',(-16.987782528413,-9.97756209826158,-18.7983401508663));
#16358=CARTESIAN_POINT('Ctrl Pts',(-17.0519099637413,-9.93927191795146,
-18.732995983382));
#16359=CARTESIAN_POINT('Ctrl Pts',(-17.1734828765201,-9.85746485958505,
-18.5981367262514));
#16360=CARTESIAN_POINT('Ctrl Pts',(-17.2308500451718,-9.81433249494389,
-18.5283528074946));
#16361=CARTESIAN_POINT('Ctrl Pts',(-17.2858341932293,-9.77439024390244,
-18.4545876051761));
#16362=CARTESIAN_POINT('Ctrl Pts',(1.18948320324198E-15,10.75,-25.));
#16363=CARTESIAN_POINT('Ctrl Pts',(1.18948320324198E-15,10.75,-25.));
#16364=CARTESIAN_POINT('Ctrl Pts',(1.18948320324198E-15,10.75,-25.));
#16365=CARTESIAN_POINT('Ctrl Pts',(0.245046068213596,10.75,-26.0262609450161));
#16366=CARTESIAN_POINT('Ctrl Pts',(0.697525526338158,10.7499999999999,-25.5161823337686));
#16367=CARTESIAN_POINT('Ctrl Pts',(1.15008999572769,10.7499999999998,-25.0067283146802));
#16368=CARTESIAN_POINT('Ctrl Pts',(0.496527090381721,10.7416099797658,-27.00122252098));
#16369=CARTESIAN_POINT('Ctrl Pts',(1.34414287478967,10.7106845238825,-25.9683849162194));
#16370=CARTESIAN_POINT('Ctrl Pts',(2.19070342072973,10.749484751575,-24.9351054845997));
#16371=CARTESIAN_POINT('Ctrl Pts',(1.00994300948597,10.7055471241071,-28.8607675866388));
#16372=CARTESIAN_POINT('Ctrl Pts',(2.54379890611781,10.5691512799226,-26.7760314748787));
#16373=CARTESIAN_POINT('Ctrl Pts',(4.09237376657161,10.7476337609872,-24.7054729284982));
#16374=CARTESIAN_POINT('Ctrl Pts',(1.27181081709597,10.6778869683601,-29.7457578698098));
#16375=CARTESIAN_POINT('Ctrl Pts',(3.0977626829763,10.4667614319515,-27.1321627163013));
#16376=CARTESIAN_POINT('Ctrl Pts',(4.95399181959426,10.7462982551885,-24.5469284871057));
#16377=CARTESIAN_POINT('Ctrl Pts',(1.80395268087472,10.6009682382658,-31.4369952413203));
#16378=CARTESIAN_POINT('Ctrl Pts',(4.12187807240196,10.2129703311935,-27.7695605671644));
#16379=CARTESIAN_POINT('Ctrl Pts',(6.53563598753902,10.7430008170775,-24.1828886315384));
#16380=CARTESIAN_POINT('Ctrl Pts',(2.07423302929861,10.5517189359568,-32.2432082848239));
#16381=CARTESIAN_POINT('Ctrl Pts',(4.59231660943448,10.0612947296318,-28.0508074627162));
#16382=CARTESIAN_POINT('Ctrl Pts',(7.25565349942215,10.7410386985122,-23.9770771406387));
#16383=CARTESIAN_POINT('Ctrl Pts',(2.48491499500549,10.459798098358,-33.3988108702572));
#16384=CARTESIAN_POINT('Ctrl Pts',(5.23932024907478,9.80660117582193,-28.4255319484534));
#16385=CARTESIAN_POINT('Ctrl Pts',(8.2516652081245,10.7377584482577,-23.6501713365951));
#16386=CARTESIAN_POINT('Ctrl Pts',(2.62268926997547,10.4261480597688,-33.7750338413453));
#16387=CARTESIAN_POINT('Ctrl Pts',(5.445507716182,9.7170003420557,-28.5427016972242));
#16388=CARTESIAN_POINT('Ctrl Pts',(8.56961785745803,10.736608712042,-23.5380644347089));
#16389=CARTESIAN_POINT('Ctrl Pts',(2.89985851712585,10.3524819706058,-34.5101434304064));
#16390=CARTESIAN_POINT('Ctrl Pts',(5.83911442522935,9.53010244159021,-28.7624286517655));
#16391=CARTESIAN_POINT('Ctrl Pts',(9.18050627991221,10.7342176814138,-23.309481965988));
#16392=CARTESIAN_POINT('Ctrl Pts',(3.03960350978844,10.3123489874894,-34.8698754329864));
#16393=CARTESIAN_POINT('Ctrl Pts',(6.02694125231312,9.43251761880773,-28.8651891737879));
#16394=CARTESIAN_POINT('Ctrl Pts',(9.47410804615325,10.7329731060527,-23.1927050718314));
#16395=CARTESIAN_POINT('Ctrl Pts',(3.73556853847811,10.0969166520386,-36.6103249476162));
#16396=CARTESIAN_POINT('Ctrl Pts',(6.91528845301335,8.93215374352083,-29.3418543865727));
#16397=CARTESIAN_POINT('Ctrl Pts',(10.8737520565665,10.7266325629012,-22.6069251683481));
#16398=CARTESIAN_POINT('Ctrl Pts',(4.28614638192447,9.87708772192159,-37.826697916169));
#16399=CARTESIAN_POINT('Ctrl Pts',(7.45637148948174,8.49742418453718,-29.602022740049));
#16400=CARTESIAN_POINT('Ctrl Pts',(11.7860488717805,10.7211810673495,-22.1329942376077));
#16401=CARTESIAN_POINT('Ctrl Pts',(5.0963672454787,9.4699996867828,-39.4245954567253));
#16402=CARTESIAN_POINT('Ctrl Pts',(8.07481027224274,7.86615486907342,-29.8600948205774));
#16403=CARTESIAN_POINT('Ctrl Pts',(12.9720188548844,10.7133699557624,-21.4455568975883));
#16404=CARTESIAN_POINT('Ctrl Pts',(5.36385054816428,9.32136836042203,-39.9190359944775));
#16405=CARTESIAN_POINT('Ctrl Pts',(8.24891439461379,7.65822546479542,-29.9237161259567));
#16406=CARTESIAN_POINT('Ctrl Pts',(13.3360751704533,10.7108238630695,-21.2197719172396));
#16407=CARTESIAN_POINT('Ctrl Pts',(5.76043976597216,9.07765988049985,-40.6045618673102));
#16408=CARTESIAN_POINT('Ctrl Pts',(8.46797828230607,7.35877187776432,-29.9886773212175));
#16409=CARTESIAN_POINT('Ctrl Pts',(13.8455182988732,10.7071845019373,-20.8868823761153));
#16410=CARTESIAN_POINT('Ctrl Pts',(5.89186327262075,8.99295832117378,-40.8236913089109));
#16411=CARTESIAN_POINT('Ctrl Pts',(8.53406163401868,7.26085797953908,-30.0052396236136));
#16412=CARTESIAN_POINT('Ctrl Pts',(14.0091990780795,10.7060011866232,-20.776867418932));
#16413=CARTESIAN_POINT('Ctrl Pts',(6.15303145469192,8.81632327601466,-41.2430881438596));
#16414=CARTESIAN_POINT('Ctrl Pts',(8.65338623470555,7.0702484949104,-30.0285576176001));
#16415=CARTESIAN_POINT('Ctrl Pts',(14.3256984048538,10.7037082551722,-20.558718370803));
#16416=CARTESIAN_POINT('Ctrl Pts',(6.28222851753279,8.72473808032663,-41.4424366493991));
#16417=CARTESIAN_POINT('Ctrl Pts',(8.70631822359822,6.97798667254651,-30.0352185638796));
#16418=CARTESIAN_POINT('Ctrl Pts',(14.477836323313,10.7026036472603,-20.4510417895244));
#16419=CARTESIAN_POINT('Ctrl Pts',(6.91629337004597,8.25388281285371,-42.3814019788258));
#16420=CARTESIAN_POINT('Ctrl Pts',(8.9406909271843,6.53586785451668,-30.0452464088025));
#16421=CARTESIAN_POINT('Ctrl Pts',(15.2065644764352,10.6973537864051,-19.9232208998721));
#16422=CARTESIAN_POINT('Ctrl Pts',(7.39039954503924,7.83295516260841,-42.9577462278353));
#16423=CARTESIAN_POINT('Ctrl Pts',(9.02974447053307,6.24844545280141,-29.9797120750833));
#16424=CARTESIAN_POINT('Ctrl Pts',(15.6948891209362,10.6940034271962,-19.531025658328));
#16425=CARTESIAN_POINT('Ctrl Pts',(8.04909500484054,7.13282851376216,-43.5698483134004));
#16426=CARTESIAN_POINT('Ctrl Pts',(9.10228415305519,5.93399688656796,-29.7960167983354));
#16427=CARTESIAN_POINT('Ctrl Pts',(16.3457316620975,10.6904299449694,-18.974403503624));
#16428=CARTESIAN_POINT('Ctrl Pts',(8.25987706424816,6.88793250317514,-43.7313745857451));
#16429=CARTESIAN_POINT('Ctrl Pts',(9.11608373612093,5.84839107297692,-29.720008510016));
#16430=CARTESIAN_POINT('Ctrl Pts',(16.5486921403279,10.689477554208,-18.7941096079141));
#16431=CARTESIAN_POINT('Ctrl Pts',(8.56208087001458,6.50230282257969,-43.9067575462143));
#16432=CARTESIAN_POINT('Ctrl Pts',(9.13151165563714,5.74910282760032,-29.5847428654585));
#16433=CARTESIAN_POINT('Ctrl Pts',(16.8372849537151,10.6884006065242,-18.529572915309));
#16434=CARTESIAN_POINT('Ctrl Pts',(8.66022380779703,6.37099391565267,-43.9538118068111));
#16435=CARTESIAN_POINT('Ctrl Pts',(9.13576418549185,5.72095061553692,-29.5361224596565));
#16436=CARTESIAN_POINT('Ctrl Pts',(16.9305840559707,10.6881012822043,-18.4425923687403));
#16437=CARTESIAN_POINT('Ctrl Pts',(8.8493007701133,6.10564621923756,-44.0242038964039));
#16438=CARTESIAN_POINT('Ctrl Pts',(9.1441453636259,5.67452070070428,-29.433096998466));
#16439=CARTESIAN_POINT('Ctrl Pts',(17.1103836553971,10.6876194863027,-18.2724145506196));
#16440=CARTESIAN_POINT('Ctrl Pts',(8.94054219798202,5.97122136470861,-44.0477302440229));
#16441=CARTESIAN_POINT('Ctrl Pts',(9.14828867279214,5.65615432282493,-29.3785610731016));
#16442=CARTESIAN_POINT('Ctrl Pts',(17.1971766388057,10.6874358663274,-18.1889498564782));
#16443=CARTESIAN_POINT('Ctrl Pts',(9.38050433358115,5.2904733750073,-44.107352693009));
#16444=CARTESIAN_POINT('Ctrl Pts',(9.17283018200081,5.58622893796518,-29.090533858496));
#16445=CARTESIAN_POINT('Ctrl Pts',(17.6179260955997,10.6867755888011,-17.7785353846934));
#16446=CARTESIAN_POINT('Ctrl Pts',(9.68088377276865,4.71847711576924,-43.9723394445427));
#16447=CARTESIAN_POINT('Ctrl Pts',(9.20581394705623,5.6020000751546,-28.8151049209875));
#16448=CARTESIAN_POINT('Ctrl Pts',(17.9128300661226,10.6870812468964,-17.4724781037204));
#16449=CARTESIAN_POINT('Ctrl Pts',(9.99167371036606,3.96929102897458,-43.5523436135202));
#16450=CARTESIAN_POINT('Ctrl Pts',(9.31436628094941,5.66746485109492,-28.3999214292906));
#16451=CARTESIAN_POINT('Ctrl Pts',(18.2576364885818,10.6879612000447,-17.0983927259223));
#16452=CARTESIAN_POINT('Ctrl Pts',(10.0507078465258,3.8173439659351,-43.4552961639203));
#16453=CARTESIAN_POINT('Ctrl Pts',(9.33945467363902,5.68285111414041,-28.3129657645239));
#16454=CARTESIAN_POINT('Ctrl Pts',(18.3255411720261,10.6881621027409,-17.0238005943171));
#16455=CARTESIAN_POINT('Ctrl Pts',(10.1613705280416,3.51217769515195,-43.2359489845758));
#16456=CARTESIAN_POINT('Ctrl Pts',(9.39675929204993,5.71656007066854,-28.1321634865455));
#16457=CARTESIAN_POINT('Ctrl Pts',(18.4585717259105,10.688593493992,-16.8759350582039));
#16458=CARTESIAN_POINT('Ctrl Pts',(10.2130004334529,3.35902467638717,-43.1137730065085));
#16459=CARTESIAN_POINT('Ctrl Pts',(9.42893767601802,5.73485848796525,-28.0383919291859));
#16460=CARTESIAN_POINT('Ctrl Pts',(18.523680749316,10.688823741373,-16.802686410844));
#16461=CARTESIAN_POINT('Ctrl Pts',(10.3585730208717,2.89301393022493,-42.7045468149934));
#16462=CARTESIAN_POINT('Ctrl Pts',(9.53795019582644,5.79253740801612,-27.742635355066));
#16463=CARTESIAN_POINT('Ctrl Pts',(18.7178877558875,10.6895397789956,-16.5816878060987));
#16464=CARTESIAN_POINT('Ctrl Pts',(10.4412106167598,2.57843802764464,-42.3776190376175));
#16465=CARTESIAN_POINT('Ctrl Pts',(9.62664120261532,5.83414790030021,-27.5290499620756));
#16466=CARTESIAN_POINT('Ctrl Pts',(18.8436728070495,10.6900438144683,-16.4351079512893));
#16467=CARTESIAN_POINT('Ctrl Pts',(10.5093104711087,2.26205520585223,-41.9936955868538));
#16468=CARTESIAN_POINT('Ctrl Pts',(9.73208854678316,5.87295961250848,-27.2952574730422));
#16469=CARTESIAN_POINT('Ctrl Pts',(18.9678208753932,10.6905025318783,-16.2871078512552));
#16470=CARTESIAN_POINT('',(17.2858341932211,9.77439024389776,-18.4545876051875));
#16471=CARTESIAN_POINT('Ctrl Pts',(4.08240831242321E-16,10.75,-25.));
#16472=CARTESIAN_POINT('Ctrl Pts',(1.58979632319949,10.75,-25.016172365722));
#16473=CARTESIAN_POINT('Ctrl Pts',(3.17967643758184,10.7483783455921,-24.8861937318559));
#16474=CARTESIAN_POINT('Ctrl Pts',(6.30793928507803,10.7354991807564,-24.3342319030064));
#16475=CARTESIAN_POINT('Ctrl Pts',(7.84472428332795,10.7247729855381,-23.9141859389731));
#16476=CARTESIAN_POINT('Ctrl Pts',(10.0760168613779,10.6880402750733,-23.079902493822));
#16477=CARTESIAN_POINT('Ctrl Pts',(10.8051602307991,10.6723084956849,-22.768776762155));
#16478=CARTESIAN_POINT('Ctrl Pts',(12.2341014639881,10.6275778161733,-22.0805919845467));
#16479=CARTESIAN_POINT('Ctrl Pts',(12.9348666409494,10.598825513122,-21.7028235613454));
#16480=CARTESIAN_POINT('Ctrl Pts',(14.2895326619036,10.5142209407937,-20.8884435700631));
#16481=CARTESIAN_POINT('Ctrl Pts',(14.94591224686,10.4612196290951,-20.4513902262047));
#16482=CARTESIAN_POINT('Ctrl Pts',(15.8906015391836,10.3204292252449,-19.7454246751064));
#16483=CARTESIAN_POINT('Ctrl Pts',(16.200456592362,10.2641568661912,-19.5007816887089));
#16484=CARTESIAN_POINT('Ctrl Pts',(16.6444363232158,10.1320758235282,-19.1203465671956));
#16485=CARTESIAN_POINT('Ctrl Pts',(16.7876108033141,10.0797343600865,-18.9927696063079));
#16486=CARTESIAN_POINT('Ctrl Pts',(16.9877825284021,9.9775620982677,-18.7983401508771));
#16487=CARTESIAN_POINT('Ctrl Pts',(17.0519099637308,9.93927191795807,-18.732995983393));
#16488=CARTESIAN_POINT('Ctrl Pts',(17.1734828765102,9.85746485959219,-18.598136726263));
#16489=CARTESIAN_POINT('Ctrl Pts',(17.2308500451622,9.81433249495098,-18.5283528075066));
#16490=CARTESIAN_POINT('Ctrl Pts',(17.2858341932211,9.77439024389776,-18.4545876051875));
#16491=CARTESIAN_POINT('Origin',(49.598387070549,10.75,-42.0119030752));
#16492=CARTESIAN_POINT('Ctrl Pts',(10.5060622858798,2.27709359605911,-42.0119030752));
#16493=CARTESIAN_POINT('Ctrl Pts',(9.72158531033336,5.89651617104406,-27.202410868965));
#16494=CARTESIAN_POINT('Ctrl Pts',(19.0763027194419,10.75,-16.1584242596923));
#16495=CARTESIAN_POINT('Ctrl Pts',(10.5861279548434,1.90768633649479,-41.5656624370432));
#16496=CARTESIAN_POINT('Ctrl Pts',(10.054211023759,4.97457944703935,-27.0105294870069));
#16497=CARTESIAN_POINT('Ctrl Pts',(19.2216718028963,9.00616861666905,-15.9868045152509));
#16498=CARTESIAN_POINT('Ctrl Pts',(10.6468390893591,1.5338046393487,-41.2156085744635));
#16499=CARTESIAN_POINT('Ctrl Pts',(10.311656332032,4.01333959595599,-26.8528714213348));
#16500=CARTESIAN_POINT('Ctrl Pts',(19.3319171300874,7.2409846927467,-15.8521571440408));
#16501=CARTESIAN_POINT('Ctrl Pts',(10.728725307307,0.776010661488396,-40.7396085635752));
#16502=CARTESIAN_POINT('Ctrl Pts',(10.6587854631906,2.04350040512914,-26.6371988427527));
#16503=CARTESIAN_POINT('Ctrl Pts',(19.4806014076874,3.66349219260051,-15.6690802167434));
#16504=CARTESIAN_POINT('Ctrl Pts',(10.7498997026982,0.392119563052058,-40.6138592138001));
#16505=CARTESIAN_POINT('Ctrl Pts',(10.7495724464119,1.03183653258076,-26.578717448758));
#16506=CARTESIAN_POINT('Ctrl Pts',(19.5190486552012,1.85116909998997,-15.6207150822312));
#16507=CARTESIAN_POINT('Ctrl Pts',(10.7500246316439,-0.094580678063645,
-40.6131222287913));
#16508=CARTESIAN_POINT('Ctrl Pts',(10.7501050007708,-0.248881490684259,
-26.5783781675765));
#16509=CARTESIAN_POINT('Ctrl Pts',(19.5192754939424,-0.446508782486515,
-15.6204316264581));
#16510=CARTESIAN_POINT('Ctrl Pts',(10.7487192580301,-0.19226312690224,-40.6208265772758));
#16511=CARTESIAN_POINT('Ctrl Pts',(10.744538224302,-0.505954113601848,-26.5819274926781));
#16512=CARTESIAN_POINT('Ctrl Pts',(19.5169052717251,-0.90766080839821,-15.6233948374125));
#16513=CARTESIAN_POINT('Ctrl Pts',(10.7434916310807,-0.386417353144142,
-40.6516369832357));
#16514=CARTESIAN_POINT('Ctrl Pts',(10.722261359959,-1.01646923646688,-26.5960974937392));
#16515=CARTESIAN_POINT('Ctrl Pts',(19.5074132478589,-1.82424936484402,-15.6352449935534));
#16516=CARTESIAN_POINT('Ctrl Pts',(10.7395716055577,-0.483128018904152,
-40.6747296691341));
#16517=CARTESIAN_POINT('Ctrl Pts',(10.7055561163698,-1.27059431610844,-26.6067148813108));
#16518=CARTESIAN_POINT('Ctrl Pts',(19.500295491297,-2.280813670639,-15.6441267958185));
#16519=CARTESIAN_POINT('Ctrl Pts',(10.7239671336519,-0.772186979014415,
-40.7664424451147));
#16520=CARTESIAN_POINT('Ctrl Pts',(10.6391149691279,-2.02907825197572,-26.6487780897117));
#16521=CARTESIAN_POINT('Ctrl Pts',(19.4719617901052,-3.64544085441996,-15.6794009404334));
#16522=CARTESIAN_POINT('Ctrl Pts',(10.708441911361,-0.963462269665522,-40.8575101572767));
#16523=CARTESIAN_POINT('Ctrl Pts',(10.5730189889097,-2.52952302522834,-26.690482244076));
#16524=CARTESIAN_POINT('Ctrl Pts',(19.4437719857254,-4.54843815679182,-15.7144269835597));
#16525=CARTESIAN_POINT('Ctrl Pts',(10.6469585658024,-1.53320714658275,-41.2149233163682));
#16526=CARTESIAN_POINT('Ctrl Pts',(10.3121595644647,-4.01182480387279,-26.8525659713593));
#16527=CARTESIAN_POINT('Ctrl Pts',(19.3321340685354,-7.23816397107918,-15.851893583235));
#16528=CARTESIAN_POINT('Ctrl Pts',(10.5861513134375,-1.90757856453282,-41.5655322494299));
#16529=CARTESIAN_POINT('Ctrl Pts',(10.0543097325423,-4.97430585629965,-27.0104725449811));
#16530=CARTESIAN_POINT('Ctrl Pts',(19.2217159888502,-9.00563856695809,-15.9867523502243));
#16531=CARTESIAN_POINT('Ctrl Pts',(10.50606228588,-2.27709359605839,-42.0119030751991));
#16532=CARTESIAN_POINT('Ctrl Pts',(9.72158531033401,-5.89651617104224,-27.2024108689646));
#16533=CARTESIAN_POINT('Ctrl Pts',(19.0763027194422,-10.7499999999966,-16.158424259692));
#16534=CARTESIAN_POINT('Origin',(58.1890815764933,11.0623060762929,-60.5701598045158));
#16535=CARTESIAN_POINT('',(17.2858341932297,-9.77439024390216,-18.4545876051755));
#16536=CARTESIAN_POINT('Origin',(58.687261606127,-11.0785103164459,-61.1099573921991));
#16537=CARTESIAN_POINT('Origin',(49.5983870705491,-10.7499999999994,-42.0119030751999));
#16538=CARTESIAN_POINT('Ctrl Pts',(2.5146574731546E-15,-10.75,-25.));
#16539=CARTESIAN_POINT('Ctrl Pts',(2.5146574731546E-15,-10.75,-25.));
#16540=CARTESIAN_POINT('Ctrl Pts',(2.5146574731546E-15,-10.75,-25.));
#16541=CARTESIAN_POINT('Ctrl Pts',(1.15016130072756,-10.7499999999999,-25.0066480462939));
#16542=CARTESIAN_POINT('Ctrl Pts',(0.697561172183379,-10.75,-25.5161421503232));
#16543=CARTESIAN_POINT('Ctrl Pts',(0.245046068221819,-10.75,-26.0262609450183));
#16544=CARTESIAN_POINT('Ctrl Pts',(2.1908367452987,-10.7494908626442,-24.9349427537218));
#16545=CARTESIAN_POINT('Ctrl Pts',(1.34420967820515,-10.7106820865303,-25.9683035148595));
#16546=CARTESIAN_POINT('Ctrl Pts',(0.496527090381256,-10.7416099797658,
-27.001222520974));
#16547=CARTESIAN_POINT('Ctrl Pts',(4.09261727898974,-10.7476618291889,-24.7051473346811));
#16548=CARTESIAN_POINT('Ctrl Pts',(2.5439199817105,-10.5691405134721,-26.7758669153147));
#16549=CARTESIAN_POINT('Ctrl Pts',(1.00994300948646,-10.7055471241071,-28.8607675866448));
#16550=CARTESIAN_POINT('Ctrl Pts',(4.95428339066113,-10.746342167033,-24.5465224064888));
#16551=CARTESIAN_POINT('Ctrl Pts',(3.09790697546993,-10.4667447480452,-27.1319561817229));
#16552=CARTESIAN_POINT('Ctrl Pts',(1.27181081709445,-10.6778869683603,-29.7457578698038));
#16553=CARTESIAN_POINT('Ctrl Pts',(6.53601411261396,-10.7430838540963,-24.182326766051));
#16554=CARTESIAN_POINT('Ctrl Pts',(4.12206174340227,-10.2129395865731,-27.7692699618903));
#16555=CARTESIAN_POINT('Ctrl Pts',(1.8039526808771,-10.6009682382655,-31.4369952413291));
#16556=CARTESIAN_POINT('Ctrl Pts',(7.25607005425798,-10.7411450197821,-23.976439997658));
#16557=CARTESIAN_POINT('Ctrl Pts',(4.59251646503464,-10.0612558055132,-28.0504747196604));
#16558=CARTESIAN_POINT('Ctrl Pts',(2.07423302930479,-10.5517189359555,-32.2432082848164));
#16559=CARTESIAN_POINT('Ctrl Pts',(8.25213508492983,-10.7379037029823,-23.6494264617979));
#16560=CARTESIAN_POINT('Ctrl Pts',(5.23953945715423,-9.80654919147577,-28.4251361523469));
#16561=CARTESIAN_POINT('Ctrl Pts',(2.48491499500436,-10.4597980983582,-33.3988108702665));
#16562=CARTESIAN_POINT('Ctrl Pts',(8.57010470803834,-10.7367676144205,-23.5372845336702));
#16563=CARTESIAN_POINT('Ctrl Pts',(5.44573258389908,-9.71694385081973,-28.5422848859336));
#16564=CARTESIAN_POINT('Ctrl Pts',(2.6226892699774,-10.4261480597683,-33.7750338413409));
#16565=CARTESIAN_POINT('Ctrl Pts',(9.18102596589203,-10.7344049688864,-23.3086338762266));
#16566=CARTESIAN_POINT('Ctrl Pts',(5.83934903650617,-9.53003679931801,-28.7619698694455));
#16567=CARTESIAN_POINT('Ctrl Pts',(2.89985851712777,-10.3524819706052,-34.5101434304211));
#16568=CARTESIAN_POINT('Ctrl Pts',(9.47464363167845,-10.7331751699807,-23.19182374603));
#16569=CARTESIAN_POINT('Ctrl Pts',(6.02717995036764,-9.43244731739938,-28.8647093797186));
#16570=CARTESIAN_POINT('Ctrl Pts',(3.03960350978804,-10.3123489874896,-34.8698754329789));
#16571=CARTESIAN_POINT('Ctrl Pts',(10.8743638418358,-10.7269099179295,-22.6058842885203));
#16572=CARTESIAN_POINT('Ctrl Pts',(6.9155438867963,-8.93206017561179,-29.3412704946376));
#16573=CARTESIAN_POINT('Ctrl Pts',(3.73556853848941,-10.096916652035,-36.6103249476706));
#16574=CARTESIAN_POINT('Ctrl Pts',(11.7867149373558,-10.7215231826189,-22.1318452400645));
#16575=CARTESIAN_POINT('Ctrl Pts',(7.45662735841948,-8.49731283179493,-29.60135892625));
#16576=CARTESIAN_POINT('Ctrl Pts',(4.28614638190404,-9.87708772193193,-37.8266979161703));
#16577=CARTESIAN_POINT('Ctrl Pts',(12.9727669650347,-10.7138049243545,-21.444271498791));
#16578=CARTESIAN_POINT('Ctrl Pts',(8.07505237652506,-7.86602449975255,-29.85931736525));
#16579=CARTESIAN_POINT('Ctrl Pts',(5.0963672454905,-9.46999968677684,-39.4245954567278));
#16580=CARTESIAN_POINT('Ctrl Pts',(13.3368504702101,-10.7112891100125,-21.2184454394017));
#16581=CARTESIAN_POINT('Ctrl Pts',(8.24914946888037,-7.65808995232061,-29.9229017098166));
#16582=CARTESIAN_POINT('Ctrl Pts',(5.36385054816107,-9.32136836042409,-39.9190359944892));
#16583=CARTESIAN_POINT('Ctrl Pts',(13.8463349889244,-10.7076930483989,-20.8855001188216));
#16584=CARTESIAN_POINT('Ctrl Pts',(8.46819967604661,-7.35863132536776,-29.9878092669635));
#16585=CARTESIAN_POINT('Ctrl Pts',(5.76043976597773,-9.07765988049636,-40.6045618673112));
#16586=CARTESIAN_POINT('Ctrl Pts',(14.0100296238394,-10.7065238154119,-20.775467569332));
#16587=CARTESIAN_POINT('Ctrl Pts',(8.53427793972743,-7.26071617975511,-30.0043539623503));
#16588=CARTESIAN_POINT('Ctrl Pts',(5.89186327262587,-8.99295832117042,-40.8236913089118));
#16589=CARTESIAN_POINT('Ctrl Pts',(14.3265568770982,-10.7042581794669,-20.5572852081084));
#16590=CARTESIAN_POINT('Ctrl Pts',(8.65359140760035,-7.07010521633929,-30.027637381082));
#16591=CARTESIAN_POINT('Ctrl Pts',(6.15303145469467,-8.81632327601274,-41.2430881438715));
#16592=CARTESIAN_POINT('Ctrl Pts',(14.4787088144407,-10.7031667250934,-20.4495929775344));
#16593=CARTESIAN_POINT('Ctrl Pts',(8.70651736835601,-6.97784317275147,-30.0342814337065));
#16594=CARTESIAN_POINT('Ctrl Pts',(6.28222851753718,-8.72473808032344,-41.4424366494097));
#16595=CARTESIAN_POINT('Ctrl Pts',(15.2075064279654,-10.6979794034415,-19.9216993076092));
#16596=CARTESIAN_POINT('Ctrl Pts',(8.94085817952484,-6.53572591496858,-30.044227216124));
#16597=CARTESIAN_POINT('Ctrl Pts',(6.91629337004194,-8.25388281285646,-42.3814019788038));
#16598=CARTESIAN_POINT('Ctrl Pts',(15.6958870160119,-10.6946690258152,-19.5294613619358));
#16599=CARTESIAN_POINT('Ctrl Pts',(9.02988047150279,-6.24831400094229,-29.9786354100043));
#16600=CARTESIAN_POINT('Ctrl Pts',(7.3903995450421,-7.83295516260545,-42.9577462278144));
#16601=CARTESIAN_POINT('Ctrl Pts',(16.3468104233022,-10.6911383287306,-18.9727919246318));
#16602=CARTESIAN_POINT('Ctrl Pts',(9.10237199538834,-5.93389689679846,-29.794867977731));
#16603=CARTESIAN_POINT('Ctrl Pts',(8.04909500484009,-7.1328285137626,-43.5698483134118));
#16604=CARTESIAN_POINT('Ctrl Pts',(16.5497972768245,-10.6901973735152,-18.7924851417449));
#16605=CARTESIAN_POINT('Ctrl Pts',(9.11615526654625,-5.84830422616559,-29.7188379529152));
#16606=CARTESIAN_POINT('Ctrl Pts',(8.25987706424758,-6.88793250317606,-43.7313745857247));
#16607=CARTESIAN_POINT('Ctrl Pts',(16.8384281956481,-10.6891334162825,-18.5279328349385));
#16608=CARTESIAN_POINT('Ctrl Pts',(9.13155933367056,-5.74903976268807,-29.5835436932285));
#16609=CARTESIAN_POINT('Ctrl Pts',(8.562080870018,-6.50230282257525,-43.9067575462262));
#16610=CARTESIAN_POINT('Ctrl Pts',(16.931739712492,-10.6888377156648,-18.4409477322578));
#16611=CARTESIAN_POINT('Ctrl Pts',(9.13580402995641,-5.72089614985896,-29.5349144336253));
#16612=CARTESIAN_POINT('Ctrl Pts',(8.66022380779769,-6.37099391565181,-43.9538118068063));
#16613=CARTESIAN_POINT('Ctrl Pts',(17.1115632196287,-10.6883617817664,-18.2707620717659));
#16614=CARTESIAN_POINT('Ctrl Pts',(9.14417009997117,-5.67448453090892,-29.4318728599763));
#16615=CARTESIAN_POINT('Ctrl Pts',(8.84930077011531,-6.10564621923469,-44.0242038964098));
#16616=CARTESIAN_POINT('Ctrl Pts',(17.1983677384727,-10.6881804139003,-18.1872940720597));
#16617=CARTESIAN_POINT('Ctrl Pts',(9.14830611234615,-5.65612787409654,-29.3773296500064));
#16618=CARTESIAN_POINT('Ctrl Pts',(8.94054219798304,-5.97122136470706,-44.0477302440178));
#16619=CARTESIAN_POINT('Ctrl Pts',(17.6191724499837,-10.6875283412504,-17.7768660186183));
#16620=CARTESIAN_POINT('Ctrl Pts',(9.17281270066304,-5.58625383373677,-29.0892697905663));
#16621=CARTESIAN_POINT('Ctrl Pts',(9.38050433357937,-5.29047337500995,-44.10735269303));
#16622=CARTESIAN_POINT('Ctrl Pts',(17.914113305695,-10.6878306786809,-17.4708065259734));
#16623=CARTESIAN_POINT('Ctrl Pts',(9.20577390128042,-5.60207455122545,-28.8138272502701));
#16624=CARTESIAN_POINT('Ctrl Pts',(9.68088377276778,-4.71847711577154,-43.9723394445637));
#16625=CARTESIAN_POINT('Ctrl Pts',(18.2589536128454,-10.6887005830597,-17.0967283874812));
#16626=CARTESIAN_POINT('Ctrl Pts',(9.31430914664379,-5.66760810066136,-28.3986432457214));
#16627=CARTESIAN_POINT('Ctrl Pts',(9.99167371036688,-3.96929102897253,-43.5523436135141));
#16628=CARTESIAN_POINT('Ctrl Pts',(18.3268644816129,-10.6888991810849,-17.0221382282332));
#16629=CARTESIAN_POINT('Ctrl Pts',(9.33939467029628,-5.68300849364225,-28.311688314363));
#16630=CARTESIAN_POINT('Ctrl Pts',(10.0507078465264,-3.81734396593362,-43.4552961639137));
#16631=CARTESIAN_POINT('Ctrl Pts',(18.4599060816778,-10.6893256117491,-16.8742776734556));
#16632=CARTESIAN_POINT('Ctrl Pts',(9.39669478209269,-5.71674605355984,-28.1308891859807));
#16633=CARTESIAN_POINT('Ctrl Pts',(10.1613705280424,-3.51217769514969,-43.2359489845797));
#16634=CARTESIAN_POINT('Ctrl Pts',(18.5250199698833,-10.6895532060488,-16.8010320285879));
#16635=CARTESIAN_POINT('Ctrl Pts',(9.42887152573738,-5.7350589337783,-28.0371200401392));
#16636=CARTESIAN_POINT('Ctrl Pts',(10.2130004334531,-3.35902467638656,-43.1137730065023));
#16637=CARTESIAN_POINT('Ctrl Pts',(18.7174482790971,-10.6902544577855,-16.582082530172));
#16638=CARTESIAN_POINT('Ctrl Pts',(9.53687565009856,-5.79224964827862,-27.7441007582841));
#16639=CARTESIAN_POINT('Ctrl Pts',(10.35723024876,-2.89731244716951,-42.7083215470959));
#16640=CARTESIAN_POINT('Ctrl Pts',(18.8415673889002,-10.6907454914663,-16.437508385761));
#16641=CARTESIAN_POINT('Ctrl Pts',(9.62413494120418,-5.83327717253747,-27.5336719255695));
#16642=CARTESIAN_POINT('Ctrl Pts',(10.4389331022241,-2.58709663537585,-42.3866080951755));
#16643=CARTESIAN_POINT('Ctrl Pts',(18.9640552529202,-10.6911938869776,-16.2915947644372));
#16644=CARTESIAN_POINT('Ctrl Pts',(9.72768083152049,-5.87165945892117,-27.3036548029488));
#16645=CARTESIAN_POINT('Ctrl Pts',(10.5064904280776,-2.27511733550195,-42.0095150580982));
#16646=CARTESIAN_POINT('Ctrl Pts',(17.2858341932297,-9.77439024390216,-18.4545876051755));
#16647=CARTESIAN_POINT('Ctrl Pts',(17.2308496142754,-9.81433280796087,-18.5283533855733));
#16648=CARTESIAN_POINT('Ctrl Pts',(17.1734819746953,-9.85746553470452,-18.5981378177516));
#16649=CARTESIAN_POINT('Ctrl Pts',(17.0519080073576,-9.93927316613411,-18.7329980624534));
#16650=CARTESIAN_POINT('Ctrl Pts',(16.9877799937373,-9.97756355387054,-18.7983427112242));
#16651=CARTESIAN_POINT('Ctrl Pts',(16.7876064605028,-10.0797362530431,-18.9927736277445));
#16652=CARTESIAN_POINT('Ctrl Pts',(16.6444306883125,-10.1320778149369,-19.1203515704373));
#16653=CARTESIAN_POINT('Ctrl Pts',(16.2004469860554,-10.2641590938575,-19.5007895704323));
#16654=CARTESIAN_POINT('Ctrl Pts',(15.8905894180583,-10.3204314322062,-19.7454341656193));
#16655=CARTESIAN_POINT('Ctrl Pts',(14.9458920693915,-10.4612218351731,-20.451404439969));
#16656=CARTESIAN_POINT('Ctrl Pts',(14.289506801601,-10.5142230477086,-20.888460478508));
#16657=CARTESIAN_POINT('Ctrl Pts',(12.9348288042006,-10.5988273843318,-21.7028449453775));
#16658=CARTESIAN_POINT('Ctrl Pts',(12.2340573634716,-10.6275795411285,-22.0806151123363));
#16659=CARTESIAN_POINT('Ctrl Pts',(10.8051035470397,-10.672309925593,-22.7688021724104));
#16660=CARTESIAN_POINT('Ctrl Pts',(10.0759536654715,-10.6880415610146,-23.0799285438409));
#16661=CARTESIAN_POINT('Ctrl Pts',(7.8446408421546,-10.7247738680017,-23.9142122954435));
#16662=CARTESIAN_POINT('Ctrl Pts',(6.30784220188933,-10.7354998258494,-24.3342560266836));
#16663=CARTESIAN_POINT('Ctrl Pts',(3.9616252120437,-10.7451589131064,-24.7482204101398));
#16664=CARTESIAN_POINT('Ctrl Pts',(3.1741229733079,-10.7471212251943,-24.8500338800462));
#16665=CARTESIAN_POINT('Ctrl Pts',(1.98574081627453,-10.7489410804811,-24.9478353565517));
#16666=CARTESIAN_POINT('Ctrl Pts',(1.58913075295958,-10.749354887983,-24.971215877855));
#16667=CARTESIAN_POINT('Ctrl Pts',(0.794943421248738,-10.7498845226873,
-24.999500006716));
#16668=CARTESIAN_POINT('Ctrl Pts',(0.39613862981597,-10.75,-25.0040317726262));
#16669=CARTESIAN_POINT('Ctrl Pts',(0.,-10.75,-25.));
#16670=CARTESIAN_POINT('Origin',(0.,-5.75,0.));
#16671=CARTESIAN_POINT('',(-2.44929359829471E-15,-5.75,20.));
#16672=CARTESIAN_POINT('Origin',(0.,-5.75,0.));
#16673=CARTESIAN_POINT('',(-2.44929359829471E-15,-5.75,20.));
#16674=CARTESIAN_POINT('Origin',(0.,-5.75,0.));
#16675=CARTESIAN_POINT('Ctrl Pts',(16.4780203712966,-10.75,-17.8656547184251));
#16676=CARTESIAN_POINT('Ctrl Pts',(17.2666005308027,-10.75,-18.4405653935864));
#16677=CARTESIAN_POINT('Ctrl Pts',(17.2858341932296,-9.77439024390242,-18.4545876051757));
#16678=CARTESIAN_POINT('Ctrl Pts',(16.420186402265,-10.75,-17.9449830848012));
#16679=CARTESIAN_POINT('Ctrl Pts',(17.1646987553025,-10.75,-18.501481536098));
#16680=CARTESIAN_POINT('Ctrl Pts',(17.2188661426269,-9.82303803508069,-18.5444300755199));
#16681=CARTESIAN_POINT('Ctrl Pts',(16.3609340347876,-10.75,-18.0226389830102));
#16682=CARTESIAN_POINT('Ctrl Pts',(17.0565699547852,-10.75,-18.5602973050013));
#16683=CARTESIAN_POINT('Ctrl Pts',(17.1454229102231,-9.87836276842019,-18.6315395728602));
#16684=CARTESIAN_POINT('Ctrl Pts',(16.2394647608978,-10.75,-18.1745295246658));
#16685=CARTESIAN_POINT('Ctrl Pts',(16.8540047055405,-10.75,-18.6788326359785));
#16686=CARTESIAN_POINT('Ctrl Pts',(16.9922413943603,-9.97582686527392,-18.7950045725018));
#16687=CARTESIAN_POINT('Ctrl Pts',(16.1773081113179,-10.75,-18.2488221735799));
#16688=CARTESIAN_POINT('Ctrl Pts',(16.7583976671104,-10.75,-18.7391027373329));
#16689=CARTESIAN_POINT('Ctrl Pts',(16.9133187470164,-10.0176700000188,-18.8718344001156));
#16690=CARTESIAN_POINT('Ctrl Pts',(15.9875644144504,-10.75,-18.4678954650283));
#16691=CARTESIAN_POINT('Ctrl Pts',(16.4909861673415,-10.75,-18.9187569933654));
#16692=CARTESIAN_POINT('Ctrl Pts',(16.6765372063047,-10.1240114260747,-19.0935506433098));
#16693=CARTESIAN_POINT('Ctrl Pts',(15.8568225101407,-10.75,-18.6090096240716));
#16694=CARTESIAN_POINT('Ctrl Pts',(16.3229486004118,-10.75,-19.0436478681492));
#16695=CARTESIAN_POINT('Ctrl Pts',(16.5179814662752,-10.1729273502795,-19.2306007925836));
#16696=CARTESIAN_POINT('Ctrl Pts',(15.456057039199,-10.75,-19.022427441683));
#16697=CARTESIAN_POINT('Ctrl Pts',(15.8403045574758,-10.75,-19.4059080219916));
#16698=CARTESIAN_POINT('Ctrl Pts',(16.0415174065678,-10.2970310354253,-19.6286372648659));
#16699=CARTESIAN_POINT('Ctrl Pts',(15.1775121139788,-10.75,-19.2848278240102));
#16700=CARTESIAN_POINT('Ctrl Pts',(15.5212812150563,-10.75,-19.6505377189956));
#16701=CARTESIAN_POINT('Ctrl Pts',(15.7216572711278,-10.3488754024673,-19.8754301022883));
#16702=CARTESIAN_POINT('Ctrl Pts',(14.3174283733583,-10.75,-20.0436150917603));
#16703=CARTESIAN_POINT('Ctrl Pts',(14.580705202477,-10.75,-20.3431259159941));
#16704=CARTESIAN_POINT('Ctrl Pts',(14.7498205235968,-10.4800501520616,-20.5861008531719));
#16705=CARTESIAN_POINT('Ctrl Pts',(13.7112218641371,-10.75,-20.511333897607));
#16706=CARTESIAN_POINT('Ctrl Pts',(13.9284252758013,-10.75,-20.791177099007));
#16707=CARTESIAN_POINT('Ctrl Pts',(14.0859782414513,-10.5295463004069,-21.0183499982909));
#16708=CARTESIAN_POINT('Ctrl Pts',(12.4444282590119,-10.75,-21.3835719658819));
#16709=CARTESIAN_POINT('Ctrl Pts',(12.5993509724745,-10.75,-21.6142534710468));
#16710=CARTESIAN_POINT('Ctrl Pts',(12.7203223126435,-10.6086489117044,-21.8215270095858));
#16711=CARTESIAN_POINT('Ctrl Pts',(11.7822109370052,-10.75,-21.7877736287731));
#16712=CARTESIAN_POINT('Ctrl Pts',(11.9106547115043,-10.75,-21.9998133945429));
#16713=CARTESIAN_POINT('Ctrl Pts',(12.017568252458,-10.6355424608103,-22.1915948020144));
#16714=CARTESIAN_POINT('Ctrl Pts',(10.4276042052761,-10.75,-22.5220998589813));
#16715=CARTESIAN_POINT('Ctrl Pts',(10.5179685506165,-10.75,-22.6958229564124));
#16716=CARTESIAN_POINT('Ctrl Pts',(10.5948532243949,-10.6772804141921,-22.8609639240682));
#16717=CARTESIAN_POINT('Ctrl Pts',(9.73251018538536,-10.75,-22.8541153700672));
#16718=CARTESIAN_POINT('Ctrl Pts',(9.80642247244757,-10.75,-23.0117088133705));
#16719=CARTESIAN_POINT('Ctrl Pts',(9.87204995901033,-10.6919698658214,-23.1619487822205));
#16720=CARTESIAN_POINT('Ctrl Pts',(7.59539354894044,-10.75,-23.7477563831948));
#16721=CARTESIAN_POINT('Ctrl Pts',(7.63899237205308,-10.75,-23.8550327053113));
#16722=CARTESIAN_POINT('Ctrl Pts',(7.66543048577482,-10.7263148678223,-23.9669915332414));
#16723=CARTESIAN_POINT('Ctrl Pts',(6.11513874037308,-10.75,-24.2011081296479));
#16724=CARTESIAN_POINT('Ctrl Pts',(6.13861428587886,-10.7499999999906,-24.2845436650543));
#16725=CARTESIAN_POINT('Ctrl Pts',(6.15722358267718,-10.73636285653,-24.3678462428209));
#16726=CARTESIAN_POINT('Ctrl Pts',(3.08771028814334,-10.75,-24.8194092303925));
#16727=CARTESIAN_POINT('Ctrl Pts',(3.09355332608923,-10.7500000000094,-24.8560196583317));
#16728=CARTESIAN_POINT('Ctrl Pts',(3.09482729538435,-10.7484649507037,-24.8935813777596));
#16729=CARTESIAN_POINT('Ctrl Pts',(1.54655171301311,-10.75,-24.9814490353809));
#16730=CARTESIAN_POINT('Ctrl Pts',(1.54684319067375,-10.75,-24.9985607643983));
#16731=CARTESIAN_POINT('Ctrl Pts',(1.54703957001439,-10.75,-25.0156741335565));
#16732=CARTESIAN_POINT('Ctrl Pts',(0.,-10.75,-25.));
#16733=CARTESIAN_POINT('Ctrl Pts',(0.,-10.75,-25.));
#16734=CARTESIAN_POINT('Ctrl Pts',(0.,-10.75,-25.));
#16735=CARTESIAN_POINT('Origin',(16.4780203712966,-9.75,-17.8656547184251));
#16736=CARTESIAN_POINT('Ctrl Pts',(18.3893975112955,-10.75,-15.4217398231055));
#16737=CARTESIAN_POINT('Ctrl Pts',(19.1556224075994,-10.75,-16.064312315735));
#16738=CARTESIAN_POINT('Ctrl Pts',(19.1556224075994,-9.74999999999999,-16.064312315735));
#16739=CARTESIAN_POINT('Ctrl Pts',(17.7244639958846,-10.75,-16.214628749746));
#16740=CARTESIAN_POINT('Ctrl Pts',(18.5021835427803,-10.75,-16.8319676033546));
#16741=CARTESIAN_POINT('Ctrl Pts',(18.505450860098,-9.75743449038258,-16.8395985788077));
#16742=CARTESIAN_POINT('Ctrl Pts',(17.0876217955067,-10.75,-17.0294907556045));
#16743=CARTESIAN_POINT('Ctrl Pts',(17.8730318352358,-10.75,-17.623535138591));
#16744=CARTESIAN_POINT('Ctrl Pts',(17.8824917699952,-9.76550892523746,-17.6365459729584));
#16745=CARTESIAN_POINT('Ctrl Pts',(16.4780203712966,-10.75,-17.8656547184251));
#16746=CARTESIAN_POINT('Ctrl Pts',(17.2666005308027,-10.75,-18.4405653935864));
#16747=CARTESIAN_POINT('Ctrl Pts',(17.2858341932296,-9.77439024390236,-18.4545876051756));
#16748=CARTESIAN_POINT('Origin',(18.3893975112954,-9.75,-15.4217398231056));
#16749=CARTESIAN_POINT('Origin',(0.,-9.75,0.));
#16750=CARTESIAN_POINT('Origin',(-18.3893975112944,-9.75,-15.4217398231068));
#16751=CARTESIAN_POINT('Ctrl Pts',(-16.4780203712963,-10.75,-17.8656547184255));
#16752=CARTESIAN_POINT('Ctrl Pts',(-17.2666005308023,-10.75,-18.4405653935868));
#16753=CARTESIAN_POINT('Ctrl Pts',(-17.2858341932293,-9.77439024390244,
-18.4545876051761));
#16754=CARTESIAN_POINT('Ctrl Pts',(-17.0876217955269,-10.75,-17.0294907556188));
#16755=CARTESIAN_POINT('Ctrl Pts',(-17.8730318353556,-10.75,-17.6235351386676));
#16756=CARTESIAN_POINT('Ctrl Pts',(-17.8824917699965,-9.76550892511618,
-17.6365459729617));
#16757=CARTESIAN_POINT('Ctrl Pts',(-17.724463995877,-10.75,-16.2146287497442));
#16758=CARTESIAN_POINT('Ctrl Pts',(-18.5021835427599,-10.7499999999973,
-16.8319676033585));
#16759=CARTESIAN_POINT('Ctrl Pts',(-18.5054508600972,-9.75743449038529,
-16.8395985788087));
#16760=CARTESIAN_POINT('Ctrl Pts',(-18.3893975112945,-10.75,-15.4217398231068));
#16761=CARTESIAN_POINT('Ctrl Pts',(-19.1556224075984,-10.75,-16.0643123157362));
#16762=CARTESIAN_POINT('Ctrl Pts',(-19.1556224075984,-9.75,-16.0643123157362));
#16763=CARTESIAN_POINT('Origin',(-16.4780203712963,-9.75,-17.8656547184255));
#16764=CARTESIAN_POINT('Ctrl Pts',(-5.35841952801743E-40,-10.75,-25.));
#16765=CARTESIAN_POINT('Ctrl Pts',(-5.35841952801743E-40,-10.75,-25.));
#16766=CARTESIAN_POINT('Ctrl Pts',(-5.35841952801743E-40,-10.75,-25.));
#16767=CARTESIAN_POINT('Ctrl Pts',(-1.55042841078198,-10.75,-24.9814045184011));
#16768=CARTESIAN_POINT('Ctrl Pts',(-1.55072583154171,-10.75,-24.998585080049));
#16769=CARTESIAN_POINT('Ctrl Pts',(-1.55092559030133,-10.75,-25.0157668478768));
#16770=CARTESIAN_POINT('Ctrl Pts',(-3.07944423838035,-10.75,-24.8200362535366));
#16771=CARTESIAN_POINT('Ctrl Pts',(-3.08524485674213,-10.7499999999987,
-24.8565651264907));
#16772=CARTESIAN_POINT('Ctrl Pts',(-3.08654552726842,-10.7484627964799,
-24.8940268047827));
#16773=CARTESIAN_POINT('Ctrl Pts',(-5.33854036060754,-10.75,-24.3602374464479));
#16774=CARTESIAN_POINT('Ctrl Pts',(-5.3557332742001,-10.7500000000007,-24.4319952968947));
#16775=CARTESIAN_POINT('Ctrl Pts',(-5.37162508811807,-10.7394784010279,
-24.5032449016001));
#16776=CARTESIAN_POINT('Ctrl Pts',(-6.08590968694707,-10.75,-24.1707865634184));
#16777=CARTESIAN_POINT('Ctrl Pts',(-6.1094282435196,-10.7499999999987,-24.2548405732474));
#16778=CARTESIAN_POINT('Ctrl Pts',(-6.13034393953452,-10.7353379259098,
-24.3384029005633));
#16779=CARTESIAN_POINT('Ctrl Pts',(-7.56885814939832,-10.75,-23.7165457546288));
#16780=CARTESIAN_POINT('Ctrl Pts',(-7.60772303658771,-10.7500000000013,
-23.8278999852315));
#16781=CARTESIAN_POINT('Ctrl Pts',(-7.64328958394848,-10.7230487971063,
-23.9369917727021));
#16782=CARTESIAN_POINT('Ctrl Pts',(-8.29448746489639,-10.75,-23.4547722125325));
#16783=CARTESIAN_POINT('Ctrl Pts',(-8.343770430558,-10.7500000000007,-23.5802417303107));
#16784=CARTESIAN_POINT('Ctrl Pts',(-8.38736583248543,-10.7150024615342,
-23.7030917074376));
#16785=CARTESIAN_POINT('Ctrl Pts',(-9.71223839813022,-10.75,-22.8632329101288));
#16786=CARTESIAN_POINT('Ctrl Pts',(-9.78574594442074,-10.7499999999993,
-23.0204047949222));
#16787=CARTESIAN_POINT('Ctrl Pts',(-9.85107461164577,-10.692321177143,-23.1702735598621));
#16788=CARTESIAN_POINT('Ctrl Pts',(-10.4047291096027,-10.75,-22.5333929349819));
#16789=CARTESIAN_POINT('Ctrl Pts',(-10.4945435000878,-10.7499999999993,
-22.7066109051832));
#16790=CARTESIAN_POINT('Ctrl Pts',(-10.5710496564742,-10.677775627927,-22.8713056754172));
#16791=CARTESIAN_POINT('Ctrl Pts',(-11.7557843148556,-10.75,-21.8031670890272));
#16792=CARTESIAN_POINT('Ctrl Pts',(-11.8833543298829,-10.7500000000007,
-22.0144907873188));
#16793=CARTESIAN_POINT('Ctrl Pts',(-11.989696301555,-10.6364601057527,-22.2057694542664));
#16794=CARTESIAN_POINT('Ctrl Pts',(-12.41441707146,-10.75,-21.4029231633718));
#16795=CARTESIAN_POINT('Ctrl Pts',(-12.5682277181088,-10.7499999999993,
-21.6325922237354));
#16796=CARTESIAN_POINT('Ctrl Pts',(-12.6883191844485,-10.6100667089293,
-21.8393995383973));
#16797=CARTESIAN_POINT('Ctrl Pts',(-13.6941367871331,-10.75,-20.5243628920851));
#16798=CARTESIAN_POINT('Ctrl Pts',(-13.9104000254228,-10.7500000000007,
-20.8034739165238));
#16799=CARTESIAN_POINT('Ctrl Pts',(-14.0673658616455,-10.5308667062636,
-21.0305204614681));
#16800=CARTESIAN_POINT('Ctrl Pts',(-14.3061796724473,-10.75,-20.0529523054155));
#16801=CARTESIAN_POINT('Ctrl Pts',(-14.5687361887894,-10.75,-20.3518360674549));
#16802=CARTESIAN_POINT('Ctrl Pts',(-14.7373892678267,-10.4812146028895,
-20.5949120467487));
#16803=CARTESIAN_POINT('Ctrl Pts',(-15.1723199996605,-10.75,-19.2896963078701));
#16804=CARTESIAN_POINT('Ctrl Pts',(-15.5155349295134,-10.75,-19.6550871682641));
#16805=CARTESIAN_POINT('Ctrl Pts',(-15.7157951752577,-10.3496720503833,
-19.8801300237897));
#16806=CARTESIAN_POINT('Ctrl Pts',(-15.452535977331,-10.75,-19.0259122646854));
#16807=CARTESIAN_POINT('Ctrl Pts',(-15.8363472416202,-10.75,-19.4091372131905));
#16808=CARTESIAN_POINT('Ctrl Pts',(-16.0374978185796,-10.2976793876105,
-19.6320606736257));
#16809=CARTESIAN_POINT('Ctrl Pts',(-15.8551923244479,-10.75,-18.6107640482246));
#16810=CARTESIAN_POINT('Ctrl Pts',(-16.3210408269098,-10.75,-19.0453117612741));
#16811=CARTESIAN_POINT('Ctrl Pts',(-16.5161004001834,-10.1732729614044,
-19.2323970231278));
#16812=CARTESIAN_POINT('Ctrl Pts',(-15.9864615716645,-10.75,-18.4691305151303));
#16813=CARTESIAN_POINT('Ctrl Pts',(-16.4896849140115,-10.75,-18.9199442477269));
#16814=CARTESIAN_POINT('Ctrl Pts',(-16.6752619096529,-10.1242452909551,
-19.0948558730444));
#16815=CARTESIAN_POINT('Ctrl Pts',(-16.1767927349458,-10.75,-18.2494361858635));
#16816=CARTESIAN_POINT('Ctrl Pts',(-16.7578253325221,-10.75,-18.7397668697928));
#16817=CARTESIAN_POINT('Ctrl Pts',(-16.9127359309499,-10.0176850161698,
-18.8725266064876));
#16818=CARTESIAN_POINT('Ctrl Pts',(-16.2391104423901,-10.75,-18.174963720535));
#16819=CARTESIAN_POINT('Ctrl Pts',(-16.8536585339569,-10.75,-18.6793495841847));
#16820=CARTESIAN_POINT('Ctrl Pts',(-16.9918520227291,-9.97575786108518,
-18.7955142959009));
#16821=CARTESIAN_POINT('Ctrl Pts',(-16.4192374533764,-10.75,-17.9497511291255));
#16822=CARTESIAN_POINT('Ctrl Pts',(-17.160271716382,-10.75,-18.4999634281549));
#16823=CARTESIAN_POINT('Ctrl Pts',(-17.2189763207791,-9.83124367041143,
-18.5531344920881));
#16824=CARTESIAN_POINT('Ctrl Pts',(-16.5326524480039,-10.75,-17.7942078342577));
#16825=CARTESIAN_POINT('Ctrl Pts',(-17.390066786921,-10.75,-18.3836903792569));
#16826=CARTESIAN_POINT('Ctrl Pts',(-17.3570580545225,-9.71022120413227,
-18.3720918508499));
#16827=CARTESIAN_POINT('Ctrl Pts',(-16.640726582166,-10.75,-17.6325831459554));
#16828=CARTESIAN_POINT('Ctrl Pts',(-17.5392115108332,-10.75,-18.2500344325275));
#16829=CARTESIAN_POINT('Ctrl Pts',(-17.4577990624194,-9.66415958091025,
-18.190604719098));
#16830=CARTESIAN_POINT('Ctrl Pts',(6.03940677783316E-16,10.75,-25.));
#16831=CARTESIAN_POINT('Ctrl Pts',(6.03940677783316E-16,10.75,-25.));
#16832=CARTESIAN_POINT('Ctrl Pts',(6.03940677783316E-16,10.75,-25.));
#16833=CARTESIAN_POINT('Ctrl Pts',(0.77551876936987,10.75,-24.990698606333));
#16834=CARTESIAN_POINT('Ctrl Pts',(0.775625402192565,10.75,-24.9992899262904));
#16835=CARTESIAN_POINT('Ctrl Pts',(0.775729285272185,10.75,-25.0078813851305));
#16836=CARTESIAN_POINT('Ctrl Pts',(1.54921288772271,10.75,-24.9460692154471));
#16837=CARTESIAN_POINT('Ctrl Pts',(1.55044130692443,10.7500000000249,-24.9639270378186));
#16838=CARTESIAN_POINT('Ctrl Pts',(1.55122662830252,10.7495696386015,-24.9818302943601));
#16839=CARTESIAN_POINT('Ctrl Pts',(3.09087304220801,10.75,-24.7816780284712));
#16840=CARTESIAN_POINT('Ctrl Pts',(3.09605488960405,10.7499999999752,-24.8197202989179));
#16841=CARTESIAN_POINT('Ctrl Pts',(3.10078026619678,10.747267815588,-24.8577117264916));
#16842=CARTESIAN_POINT('Ctrl Pts',(3.85256422917062,10.75,-24.6633151125848));
#16843=CARTESIAN_POINT('Ctrl Pts',(3.86111871633922,10.7499999999973,-24.712078758921));
#16844=CARTESIAN_POINT('Ctrl Pts',(3.86850703318997,10.7454111698887,-24.7608678209163));
#16845=CARTESIAN_POINT('Ctrl Pts',(6.10952281364908,10.75,-24.2020255484112));
#16846=CARTESIAN_POINT('Ctrl Pts',(6.13294958208081,10.7500000000053,-24.2853845753718));
#16847=CARTESIAN_POINT('Ctrl Pts',(6.15155990520288,10.7363778606325,-24.3686028672562));
#16848=CARTESIAN_POINT('Ctrl Pts',(7.5775794845246,10.75,-23.7541652338085));
#16849=CARTESIAN_POINT('Ctrl Pts',(7.62096600221208,10.75,-23.8610830094627));
#16850=CARTESIAN_POINT('Ctrl Pts',(7.64716672681317,10.726508702728,-23.9727170011077));
#16851=CARTESIAN_POINT('Ctrl Pts',(9.72149591099175,10.75,-22.8592338757647));
#16852=CARTESIAN_POINT('Ctrl Pts',(9.79518731370962,10.75,-23.0165595755935));
#16853=CARTESIAN_POINT('Ctrl Pts',(9.86061355528561,10.6921924563451,-23.1665834858966));
#16854=CARTESIAN_POINT('Ctrl Pts',(10.4190640908032,10.75,-22.5262337182939));
#16855=CARTESIAN_POINT('Ctrl Pts',(10.5091983832299,10.7500000000007,-22.6997672275432));
#16856=CARTESIAN_POINT('Ctrl Pts',(10.585964436799,10.6774671158219,-22.8647134299696));
#16857=CARTESIAN_POINT('Ctrl Pts',(11.7684524650003,10.75,-21.7957196072559));
#16858=CARTESIAN_POINT('Ctrl Pts',(11.8964128840459,10.7499999999993,-22.0073671320669));
#16859=CARTESIAN_POINT('Ctrl Pts',(12.0030386260281,10.6360415664677,-22.1988562680654));
#16860=CARTESIAN_POINT('Ctrl Pts',(12.4221781820695,10.75,-21.3975520043717));
#16861=CARTESIAN_POINT('Ctrl Pts',(12.576137264646,10.75,-21.6275792716514));
#16862=CARTESIAN_POINT('Ctrl Pts',(12.6966279179313,10.6096487571098,-21.8343422634894));
#16863=CARTESIAN_POINT('Ctrl Pts',(13.684782342616,10.75,-20.530827861331));
#16864=CARTESIAN_POINT('Ctrl Pts',(13.9003194774231,10.75,-20.8096148861702));
#16865=CARTESIAN_POINT('Ctrl Pts',(14.0571943009162,10.5315720187492,-21.0363561860875));
#16866=CARTESIAN_POINT('Ctrl Pts',(14.294089112681,10.75,-20.0629435906517));
#16867=CARTESIAN_POINT('Ctrl Pts',(14.5557034416343,10.75,-20.3609974720801));
#16868=CARTESIAN_POINT('Ctrl Pts',(14.7238617885168,10.4827239049414,-20.6040773940109));
#16869=CARTESIAN_POINT('Ctrl Pts',(15.1661919626405,10.75,-19.2954210789481));
#16870=CARTESIAN_POINT('Ctrl Pts',(15.5085221078731,10.75,-19.6602020075858));
#16871=CARTESIAN_POINT('Ctrl Pts',(15.7086678083383,10.3510274540215,-19.8854122863091));
#16872=CARTESIAN_POINT('Ctrl Pts',(15.450317409084,10.75,-19.0281667232991));
#16873=CARTESIAN_POINT('Ctrl Pts',(15.8336640610588,10.75,-19.4109514699529));
#16874=CARTESIAN_POINT('Ctrl Pts',(16.0347782735401,10.2985349668086,-19.6341135503095));
#16875=CARTESIAN_POINT('Ctrl Pts',(15.8555452026401,10.75,-18.6104166452363));
#16876=CARTESIAN_POINT('Ctrl Pts',(16.3213284001396,10.75,-19.0448335078672));
#16877=CARTESIAN_POINT('Ctrl Pts',(16.5164212277897,10.1734575195196,-19.2319798190006));
#16878=CARTESIAN_POINT('Ctrl Pts',(15.987345897022,10.75,-18.4681633272427));
#16879=CARTESIAN_POINT('Ctrl Pts',(16.4906809550653,10.7500000000002,-18.9189415895965));
#16880=CARTESIAN_POINT('Ctrl Pts',(16.6762580682836,10.1241735884936,-19.0938318798831));
#16881=CARTESIAN_POINT('Ctrl Pts',(16.1778522854737,10.75,-18.2481860733963));
#16882=CARTESIAN_POINT('Ctrl Pts',(16.7592036816611,10.7499999999999,-18.7385719233192));
#16883=CARTESIAN_POINT('Ctrl Pts',(16.9140010589,10.0173451034587,-18.8711855370801));
#16884=CARTESIAN_POINT('Ctrl Pts',(16.2401220962037,10.75,-18.1737303235091));
#16885=CARTESIAN_POINT('Ctrl Pts',(16.8550468116417,10.75,-18.6781983255835));
#16886=CARTESIAN_POINT('Ctrl Pts',(16.9930765400665,9.97534637831806,-18.7941646549338));
#16887=CARTESIAN_POINT('Ctrl Pts',(16.3614947681369,10.75,-18.0219148278828));
#16888=CARTESIAN_POINT('Ctrl Pts',(17.0575602016681,10.75,-18.5597436355989));
#16889=CARTESIAN_POINT('Ctrl Pts',(17.1461237747635,9.87786543139612,-18.6307398467417));
#16890=CARTESIAN_POINT('Ctrl Pts',(16.4205359348328,10.75,-17.9445036454283));
#16891=CARTESIAN_POINT('Ctrl Pts',(17.1653078416885,10.75,-18.5011174272147));
#16892=CARTESIAN_POINT('Ctrl Pts',(17.219277234529,9.82273940521341,-18.5438785660551));
#16893=CARTESIAN_POINT('Ctrl Pts',(16.4780203712861,10.75,-17.8656547184465));
#16894=CARTESIAN_POINT('Ctrl Pts',(17.2666005307924,10.75,-18.4405653936073));
#16895=CARTESIAN_POINT('Ctrl Pts',(17.2858341932194,9.77439024390244,-18.4545876051966));
#16896=CARTESIAN_POINT('Origin',(16.4780203712883,9.75,-17.8656547184365));
#16897=CARTESIAN_POINT('Ctrl Pts',(16.478020371287,10.75,-17.8656547184383));
#16898=CARTESIAN_POINT('Ctrl Pts',(17.2666005307932,10.75,-18.4405653935993));
#16899=CARTESIAN_POINT('Ctrl Pts',(17.2858341932202,9.77439024390244,-18.4545876051886));
#16900=CARTESIAN_POINT('Ctrl Pts',(17.0876217955002,10.75,-17.0294907556147));
#16901=CARTESIAN_POINT('Ctrl Pts',(17.8730318351501,10.75,-17.6235351385526));
#16902=CARTESIAN_POINT('Ctrl Pts',(17.8824917699869,9.76550892532975,-17.6365459729653));
#16903=CARTESIAN_POINT('Ctrl Pts',(17.7244639958765,10.75,-16.2146287497473));
#16904=CARTESIAN_POINT('Ctrl Pts',(18.5021835427756,10.75,-16.8319676033442));
#16905=CARTESIAN_POINT('Ctrl Pts',(18.505450860094,9.75743449038534,-16.8395985788126));
#16906=CARTESIAN_POINT('Ctrl Pts',(18.3893975112944,10.75,-15.4217398231068));
#16907=CARTESIAN_POINT('Ctrl Pts',(19.1556224075984,10.75,-16.0643123157362));
#16908=CARTESIAN_POINT('Ctrl Pts',(19.1556224075984,9.75,-16.0643123157362));
#16909=CARTESIAN_POINT('Origin',(18.3893975112944,9.75,-15.4217398231068));
#16910=CARTESIAN_POINT('Origin',(0.,9.75,0.));
#16911=CARTESIAN_POINT('Origin',(-18.3893975112961,9.75,-15.4217398231048));
#16912=CARTESIAN_POINT('Ctrl Pts',(-18.3893975112962,10.75,-15.4217398231047));
#16913=CARTESIAN_POINT('Ctrl Pts',(-19.1556224076002,10.75,-16.0643123157342));
#16914=CARTESIAN_POINT('Ctrl Pts',(-19.1556224076001,9.74999999999998,-16.0643123157342));
#16915=CARTESIAN_POINT('Ctrl Pts',(-17.7244639958755,10.75,-16.2146287497338));
#16916=CARTESIAN_POINT('Ctrl Pts',(-18.5021835427609,10.75,-16.831967603351));
#16917=CARTESIAN_POINT('Ctrl Pts',(-18.5054508600983,9.75743449038528,-16.8395985788073));
#16918=CARTESIAN_POINT('Ctrl Pts',(-17.087621795494,10.75,-17.0294907555989));
#16919=CARTESIAN_POINT('Ctrl Pts',(-17.8730318353239,10.75,-17.6235351386475));
#16920=CARTESIAN_POINT('Ctrl Pts',(-17.882491769997,9.76550892511712,-17.636545972961));
#16921=CARTESIAN_POINT('Ctrl Pts',(-16.4780203712963,10.75,-17.8656547184255));
#16922=CARTESIAN_POINT('Ctrl Pts',(-17.2666005308023,10.75,-18.4405653935868));
#16923=CARTESIAN_POINT('Ctrl Pts',(-17.2858341932293,9.77439024390244,-18.4545876051761));
#16924=CARTESIAN_POINT('Origin',(-16.4780203712963,9.75,-17.8656547184255));
#16925=CARTESIAN_POINT('Ctrl Pts',(-16.4780203712963,10.75,-17.8656547184255));
#16926=CARTESIAN_POINT('Ctrl Pts',(-17.2666005308023,10.75,-18.4405653935868));
#16927=CARTESIAN_POINT('Ctrl Pts',(-17.2858341932293,9.77439024390244,-18.4545876051761));
#16928=CARTESIAN_POINT('Ctrl Pts',(-16.4201864022648,10.75,-17.9449830848021));
#16929=CARTESIAN_POINT('Ctrl Pts',(-17.1646987552868,10.75,-18.5014815360729));
#16930=CARTESIAN_POINT('Ctrl Pts',(-17.218866142633,9.82303803510935,-18.5444300755103));
#16931=CARTESIAN_POINT('Ctrl Pts',(-16.3609340347869,10.75,-18.02263898301));
#16932=CARTESIAN_POINT('Ctrl Pts',(-17.0565699547838,10.75,-18.5602973050011));
#16933=CARTESIAN_POINT('Ctrl Pts',(-17.1454229102227,9.87836276842072,-18.6315395728606));
#16934=CARTESIAN_POINT('Ctrl Pts',(-16.2394647608977,10.75,-18.1745295246669));
#16935=CARTESIAN_POINT('Ctrl Pts',(-16.8540047055406,10.75,-18.6788326359793));
#16936=CARTESIAN_POINT('Ctrl Pts',(-16.9922413943597,9.97582686527399,-18.7950045725024));
#16937=CARTESIAN_POINT('Ctrl Pts',(-16.1773081113176,10.75,-18.2488221735804));
#16938=CARTESIAN_POINT('Ctrl Pts',(-16.7583976671095,10.75,-18.7391027373331));
#16939=CARTESIAN_POINT('Ctrl Pts',(-16.9133187470158,10.0176700000194,-18.8718344001161));
#16940=CARTESIAN_POINT('Ctrl Pts',(-15.9875644144501,10.75,-18.4678954650287));
#16941=CARTESIAN_POINT('Ctrl Pts',(-16.4909861673416,10.75,-18.9187569933661));
#16942=CARTESIAN_POINT('Ctrl Pts',(-16.6765372063045,10.1240114260742,-19.0935506433102));
#16943=CARTESIAN_POINT('Ctrl Pts',(-15.8568225101403,10.75,-18.6090096240717));
#16944=CARTESIAN_POINT('Ctrl Pts',(-16.3229486004107,10.75,-19.0436478681489));
#16945=CARTESIAN_POINT('Ctrl Pts',(-16.5179814662747,10.1729273502797,-19.2306007925839));
#16946=CARTESIAN_POINT('Ctrl Pts',(-15.4560570391986,10.75,-19.022427441684));
#16947=CARTESIAN_POINT('Ctrl Pts',(-15.8403045574767,10.75,-19.4059080219932));
#16948=CARTESIAN_POINT('Ctrl Pts',(-16.0415174065673,10.2970310354252,-19.6286372648663));
#16949=CARTESIAN_POINT('Ctrl Pts',(-15.1775121139771,10.75,-19.2848278240086));
#16950=CARTESIAN_POINT('Ctrl Pts',(-15.5212812150538,10.75,-19.6505377189946));
#16951=CARTESIAN_POINT('Ctrl Pts',(-15.7216572711263,10.348875402469,-19.8754301022878));
#16952=CARTESIAN_POINT('Ctrl Pts',(-14.3174283733606,10.75,-20.0436150917647));
#16953=CARTESIAN_POINT('Ctrl Pts',(-14.5807052024803,10.75,-20.3431259159971));
#16954=CARTESIAN_POINT('Ctrl Pts',(-14.7498205235984,10.4800501520585,-20.5861008531739));
#16955=CARTESIAN_POINT('Ctrl Pts',(-13.7112218641341,10.75,-20.5113338976033));
#16956=CARTESIAN_POINT('Ctrl Pts',(-13.9284252757989,10.7499999999993,-20.7911770990046));
#16957=CARTESIAN_POINT('Ctrl Pts',(-14.0859782414491,10.5295463004092,-21.0183499982884));
#16958=CARTESIAN_POINT('Ctrl Pts',(-12.4444282590142,10.75,-21.3835719658861));
#16959=CARTESIAN_POINT('Ctrl Pts',(-12.5993509724761,10.7500000000007,-21.6142534710497));
#16960=CARTESIAN_POINT('Ctrl Pts',(-12.7203223126449,10.6086489117022,-21.8215270095887));
#16961=CARTESIAN_POINT('Ctrl Pts',(-11.7822109370075,10.75,-21.7877736287786));
#16962=CARTESIAN_POINT('Ctrl Pts',(-11.9106547115054,10.75,-21.9998133945471));
#16963=CARTESIAN_POINT('Ctrl Pts',(-12.0175682524596,10.6355424608076,-22.1915948020202));
#16964=CARTESIAN_POINT('Ctrl Pts',(-10.4276042052731,10.75,-22.5220998589761));
#16965=CARTESIAN_POINT('Ctrl Pts',(-10.517968550615,10.75,-22.6958229564086));
#16966=CARTESIAN_POINT('Ctrl Pts',(-10.5948532243925,10.6772804141949,-22.8609639240628));
#16967=CARTESIAN_POINT('Ctrl Pts',(-9.73251018538841,10.75,-22.8541153700753));
#16968=CARTESIAN_POINT('Ctrl Pts',(-9.80642247244996,10.7500000000007,-23.0117088133774));
#16969=CARTESIAN_POINT('Ctrl Pts',(-9.87204995901313,10.6919698658189,-23.1619487822281));
#16970=CARTESIAN_POINT('Ctrl Pts',(-7.5953935489335,10.75,-23.7477563831789));
#16971=CARTESIAN_POINT('Ctrl Pts',(-7.63899237204751,10.7499999999987,-23.8550327052981));
#16972=CARTESIAN_POINT('Ctrl Pts',(-7.66543048576834,10.7263148678275,-23.9669915332266));
#16973=CARTESIAN_POINT('Ctrl Pts',(-6.11513874037353,10.75,-24.2011081296453));
#16974=CARTESIAN_POINT('Ctrl Pts',(-6.13861428588092,10.7500000000081,-24.2845436650569));
#16975=CARTESIAN_POINT('Ctrl Pts',(-6.15722358267897,10.7363628565299,-24.3678462428209));
#16976=CARTESIAN_POINT('Ctrl Pts',(-3.08771028814254,10.75,-24.8194092303953));
#16977=CARTESIAN_POINT('Ctrl Pts',(-3.09355332608735,10.749999999992,-24.8560196583291));
#16978=CARTESIAN_POINT('Ctrl Pts',(-3.09482729538221,10.7484649507037,-24.8935813777596));
#16979=CARTESIAN_POINT('Ctrl Pts',(-1.54655171301441,10.75,-24.9814490354507));
#16980=CARTESIAN_POINT('Ctrl Pts',(-1.54684319067547,10.75,-24.998560764468));
#16981=CARTESIAN_POINT('Ctrl Pts',(-1.54703957001513,10.75,-25.0156741336263));
#16982=CARTESIAN_POINT('Ctrl Pts',(6.05752864795171E-16,10.75,-25.));
#16983=CARTESIAN_POINT('Ctrl Pts',(6.05752864795171E-16,10.75,-25.));
#16984=CARTESIAN_POINT('Ctrl Pts',(6.05752864795171E-16,10.75,-25.));
#16985=CARTESIAN_POINT('Origin',(0.,-1.42723068592072E-14,-61.5));
#16986=CARTESIAN_POINT('',(-10.7,-1.31037207508767E-15,-61.5));
#16987=CARTESIAN_POINT('Origin',(0.,0.,-61.5));
#16988=CARTESIAN_POINT('Origin',(0.,0.,0.));
#16989=CARTESIAN_POINT('',(-8.35,-1.02258007728804E-15,-63.85));
#16990=CARTESIAN_POINT('Origin',(0.,0.,-63.85));
#16991=CARTESIAN_POINT('',(-8.35,-1.02258007728804E-15,-70.75));
#16992=CARTESIAN_POINT('',(-8.35,-1.02258007728804E-15,0.));
#16993=CARTESIAN_POINT('Origin',(0.,0.,-70.75));
#16994=CARTESIAN_POINT('Ctrl Pts',(-8.35,0.,-78.75));
#16995=CARTESIAN_POINT('Ctrl Pts',(-8.35,-8.35,-78.75));
#16996=CARTESIAN_POINT('Ctrl Pts',(0.,-8.35,-78.75));
#16997=CARTESIAN_POINT('Ctrl Pts',(8.35,-8.35,-78.75));
#16998=CARTESIAN_POINT('Ctrl Pts',(8.35,0.,-78.75));
#16999=CARTESIAN_POINT('Ctrl Pts',(8.35,8.35,-78.75));
#17000=CARTESIAN_POINT('Ctrl Pts',(0.,8.35,-78.75));
#17001=CARTESIAN_POINT('Ctrl Pts',(-8.35,8.35,-78.75));
#17002=CARTESIAN_POINT('Ctrl Pts',(-8.35,0.,-78.75));
#17003=CARTESIAN_POINT('Ctrl Pts',(-10.2459842001317,0.,-74.75));
#17004=CARTESIAN_POINT('Ctrl Pts',(-10.2459842001317,-10.2459842001317,
-74.75));
#17005=CARTESIAN_POINT('Ctrl Pts',(0.,-10.2459842001317,-74.75));
#17006=CARTESIAN_POINT('Ctrl Pts',(10.2459842001317,-10.2459842001317,-74.75));
#17007=CARTESIAN_POINT('Ctrl Pts',(10.2459842001317,0.,-74.75));
#17008=CARTESIAN_POINT('Ctrl Pts',(10.2459842001317,10.2459842001317,-74.75));
#17009=CARTESIAN_POINT('Ctrl Pts',(0.,10.2459842001317,-74.75));
#17010=CARTESIAN_POINT('Ctrl Pts',(-10.2459842001317,10.2459842001317,-74.75));
#17011=CARTESIAN_POINT('Ctrl Pts',(-10.2459842001317,0.,-74.75));
#17012=CARTESIAN_POINT('Ctrl Pts',(-8.35,0.,-70.75));
#17013=CARTESIAN_POINT('Ctrl Pts',(-8.35,-8.35,-70.75));
#17014=CARTESIAN_POINT('Ctrl Pts',(0.,-8.35,-70.75));
#17015=CARTESIAN_POINT('Ctrl Pts',(8.35,-8.35,-70.75));
#17016=CARTESIAN_POINT('Ctrl Pts',(8.35,0.,-70.75));
#17017=CARTESIAN_POINT('Ctrl Pts',(8.35,8.35,-70.75));
#17018=CARTESIAN_POINT('Ctrl Pts',(0.,8.35,-70.75));
#17019=CARTESIAN_POINT('Ctrl Pts',(-8.35,8.35,-70.75));
#17020=CARTESIAN_POINT('Ctrl Pts',(-8.35,0.,-70.75));
#17021=CARTESIAN_POINT('',(-8.35,-1.02258007728804E-15,-78.75));
#17022=CARTESIAN_POINT('Origin',(0.0888888888889092,1.08857493257567E-17,
-74.75));
#17023=CARTESIAN_POINT('Origin',(0.,0.,-78.75));
#17024=CARTESIAN_POINT('',(-1.72045318260168,-8.718775769933,-77.3287673114253));
#17025=CARTESIAN_POINT('',(-3.7964050773568E-16,-8.72047257416007,-77.85));
#17026=CARTESIAN_POINT('Ctrl Pts',(-1.72045318260167,-8.718775769933,-77.3287673114253));
#17027=CARTESIAN_POINT('Ctrl Pts',(-1.65539500148226,-8.71890290462215,
-77.3721715977544));
#17028=CARTESIAN_POINT('Ctrl Pts',(-1.5891103189426,-8.71902546830415,-77.4128415044279));
#17029=CARTESIAN_POINT('Ctrl Pts',(-1.52164394658355,-8.7191425346816,-77.450851661944));
#17030=CARTESIAN_POINT('Ctrl Pts',(-1.45352593448909,-8.71926073177204,
-77.4892289494557));
#17031=CARTESIAN_POINT('Ctrl Pts',(-1.38420266457374,-8.71937332485106,
-77.5248953093588));
#17032=CARTESIAN_POINT('Ctrl Pts',(-1.31368631099614,-8.71947936052059,
-77.557886799054));
#17033=CARTESIAN_POINT('Ctrl Pts',(-1.27115196980953,-8.71954331954735,
-77.5777867400996));
#17034=CARTESIAN_POINT('Ctrl Pts',(-1.22818293533589,-8.71960489278511,
-77.5967126611893));
#17035=CARTESIAN_POINT('Ctrl Pts',(-1.18477749668439,-8.71966387100391,
-77.6146644277036));
#17036=CARTESIAN_POINT('Ctrl Pts',(-1.12217096659324,-8.71974893918303,
-77.6405574458457));
#17037=CARTESIAN_POINT('Ctrl Pts',(-1.05842838941658,-8.71982876080258,
-77.6645122082305));
#17038=CARTESIAN_POINT('Ctrl Pts',(-0.993822322159884,-8.71990251193502,
-77.6863782440239));
#17039=CARTESIAN_POINT('Ctrl Pts',(-0.929270656109259,-8.7199762009657,
-77.7082258676345));
#17040=CARTESIAN_POINT('Ctrl Pts',(-0.863857416050902,-8.72004382972822,
-77.7279880699753));
#17041=CARTESIAN_POINT('Ctrl Pts',(-0.797874747322811,-8.72010457637465,
-77.7455626996584));
#17042=CARTESIAN_POINT('Ctrl Pts',(-0.733027140671185,-8.7201642780313,
-77.7628350030482));
#17043=CARTESIAN_POINT('Ctrl Pts',(-0.667630028539082,-8.72021733231349,
-77.7779943689607));
#17044=CARTESIAN_POINT('Ctrl Pts',(-0.601973102197269,-8.7202629590612,
-77.7909913489241));
#17045=CARTESIAN_POINT('Ctrl Pts',(-0.524757209733025,-8.72031661844249,
-77.8062764599265));
#17046=CARTESIAN_POINT('Ctrl Pts',(-0.447291752022074,-8.72036016052982,
-77.8185591941));
#17047=CARTESIAN_POINT('Ctrl Pts',(-0.369584773909021,-8.72039335911026,
-77.8278900394418));
#17048=CARTESIAN_POINT('Ctrl Pts',(-0.291661027798569,-8.72042665030001,
-77.8372469137028));
#17049=CARTESIAN_POINT('Ctrl Pts',(-0.213493632636301,-8.72044954019479,
-77.8436355249856));
#17050=CARTESIAN_POINT('Ctrl Pts',(-0.135080649621019,-8.72046180068327,
-77.8470555723296));
#17051=CARTESIAN_POINT('Ctrl Pts',(-0.0901346875977141,-8.720468828339,
-77.8490159277725));
#17052=CARTESIAN_POINT('Ctrl Pts',(-0.0451079148060559,-8.72047236367163,
-77.85));
#17053=CARTESIAN_POINT('Ctrl Pts',(-3.7964050773568E-16,-8.72047236372208,
-77.85));
#17054=CARTESIAN_POINT('Ctrl Pts',(-3.7964050773568E-16,-8.72047236372208,
-77.85));
#17055=CARTESIAN_POINT('Ctrl Pts',(0.000299910886524944,-8.72047236372241,
-77.85));
#17056=CARTESIAN_POINT('Ctrl Pts',(0.000599825357673861,-8.72047236356647,
-77.8499999564775));
#17057=CARTESIAN_POINT('Ctrl Pts',(0.000899743413439149,-8.72047236325423,
-77.8499998694293));
#17058=CARTESIAN_POINT('Ctrl Pts',(0.0640429304707948,-8.72047229751748,
-77.8499815427619));
#17059=CARTESIAN_POINT('Ctrl Pts',(0.127461864754973,-8.7204650795781,-77.8480295862201));
#17060=CARTESIAN_POINT('Ctrl Pts',(0.190853933637923,-8.72045096523215,
-77.844119386193));
#17061=CARTESIAN_POINT('Ctrl Pts',(0.254193326196229,-8.72043686261466,
-77.8402124353888));
#17062=CARTESIAN_POINT('Ctrl Pts',(0.317505410088621,-8.72041587504713,
-77.8343504951573));
#17063=CARTESIAN_POINT('Ctrl Pts',(0.380489429511035,-8.72038825768846,
-77.8265610336918));
#17064=CARTESIAN_POINT('Ctrl Pts',(0.443564297220783,-8.72036060049445,
-77.81876033669));
#17065=CARTESIAN_POINT('Ctrl Pts',(0.506309670583462,-8.72032629436986,
-77.8090266361057));
#17066=CARTESIAN_POINT('Ctrl Pts',(0.56843190743774,-8.72028559557932,-77.7974391161444));
#17067=CARTESIAN_POINT('Ctrl Pts',(0.581380258335366,-8.72027711259082,
-77.7950238896154));
#17068=CARTESIAN_POINT('Ctrl Pts',(0.594301580864125,-8.72026835187617,
-77.7925283002156));
#17069=CARTESIAN_POINT('Ctrl Pts',(0.607193291675441,-8.72025931575594,
-77.7899533395341));
#17070=CARTESIAN_POINT('Ctrl Pts',(0.684092206541919,-8.72020541539694,
-77.7745937270569));
#17071=CARTESIAN_POINT('Ctrl Pts',(0.76023810077427,-8.72014184272655,-77.7563546896797));
#17072=CARTESIAN_POINT('Ctrl Pts',(0.835637247932075,-8.72006925722806,
-77.7352487986546));
#17073=CARTESIAN_POINT('Ctrl Pts',(0.910709368037719,-8.71999698655304,
-77.7142344497434));
#17074=CARTESIAN_POINT('Ctrl Pts',(0.985041941757664,-8.71991578106266,
-77.6903778171793));
#17075=CARTESIAN_POINT('Ctrl Pts',(1.05862557413108,-8.71982629169629,-77.6636423757551));
#17076=CARTESIAN_POINT('Ctrl Pts',(1.1017309535722,-8.71977386871893,-77.6479807223419));
#17077=CARTESIAN_POINT('Ctrl Pts',(1.14457897534976,-8.71971860302155,-77.6313302639057));
#17078=CARTESIAN_POINT('Ctrl Pts',(1.18716371754352,-8.71966062545943,-77.6136763622568));
#17079=CARTESIAN_POINT('Ctrl Pts',(1.26405807871352,-8.71955593661147,-77.5817990883903));
#17080=CARTESIAN_POINT('Ctrl Pts',(1.33962433782053,-8.71944296612345,-77.5468383309899));
#17081=CARTESIAN_POINT('Ctrl Pts',(1.41354178114807,-8.7193235640821,-77.5089671315456));
#17082=CARTESIAN_POINT('Ctrl Pts',(1.48753950477095,-8.71920403236052,-77.4710548009292));
#17083=CARTESIAN_POINT('Ctrl Pts',(1.55988439051607,-8.71907805510766,-77.4302259909402));
#17084=CARTESIAN_POINT('Ctrl Pts',(1.63028320823959,-8.71894748844484,-77.3866980602511));
#17085=CARTESIAN_POINT('Ctrl Pts',(1.66176045181976,-8.71888910850635,-77.3672355277663));
#17086=CARTESIAN_POINT('Ctrl Pts',(1.69284905171952,-8.71882981103946,-77.3472339354576));
#17087=CARTESIAN_POINT('Ctrl Pts',(1.72352497634196,-8.71876976196479,-77.3267152842186));
#17088=CARTESIAN_POINT('Ctrl Pts',(1.80027708010235,-8.7186195173392,-77.2753769898296));
#17089=CARTESIAN_POINT('Ctrl Pts',(1.87496173999789,-8.71846358768554,-77.2204528708162));
#17090=CARTESIAN_POINT('Ctrl Pts',(1.94719992345561,-8.71830462487999,-77.1621385652766));
#17091=CARTESIAN_POINT('Ctrl Pts',(2.01930828703512,-8.71814594774791,-77.103929056891));
#17092=CARTESIAN_POINT('Ctrl Pts',(2.0889785347496,-8.71798424835595,-77.0423417416205));
#17093=CARTESIAN_POINT('Ctrl Pts',(2.15585718417934,-8.71782216430884,-76.9776175168602));
#17094=CARTESIAN_POINT('Ctrl Pts',(2.16846973129543,-8.7177915971144,-76.9654112695555));
#17095=CARTESIAN_POINT('Ctrl Pts',(2.18098307120848,-8.71776101623946,-76.9530935832101));
#17096=CARTESIAN_POINT('Ctrl Pts',(2.19339494574377,-8.71773043937514,-76.9406662484244));
#17097=CARTESIAN_POINT('Ctrl Pts',(2.24888782190004,-8.71759373172956,-76.8851042502544));
#17098=CARTESIAN_POINT('Ctrl Pts',(2.30197065297182,-8.71745811411991,-76.8277389943072));
#17099=CARTESIAN_POINT('Ctrl Pts',(2.35269578179276,-8.71732466077813,-76.7686189730444));
#17100=CARTESIAN_POINT('Ctrl Pts',(2.4037590828821,-8.71719031773492,-76.7091048127786));
#17101=CARTESIAN_POINT('Ctrl Pts',(2.45243369256433,-8.71705816791309,-76.6478118562424));
#17102=CARTESIAN_POINT('Ctrl Pts',(2.49873800210765,-8.71692930717307,-76.584750227367));
#17103=CARTESIAN_POINT('Ctrl Pts',(2.52592884079295,-8.716853637508,-76.547719147649));
#17104=CARTESIAN_POINT('Ctrl Pts',(2.55230163167014,-8.71677910201007,-76.5100774807928));
#17105=CARTESIAN_POINT('Ctrl Pts',(2.57785340962773,-8.71670592258005,-76.4718222319597));
#17106=CARTESIAN_POINT('Ctrl Pts',(2.61310530671562,-8.71660496233609,-76.4190442962256));
#17107=CARTESIAN_POINT('Ctrl Pts',(2.64690716808691,-8.71650634668673,-76.3649202782147));
#17108=CARTESIAN_POINT('Ctrl Pts',(2.67906408116098,-8.71641099671277,-76.3096844709854));
#17109=CARTESIAN_POINT('Ctrl Pts',(2.71118233434677,-8.71631576137105,-76.2545150696992));
#17110=CARTESIAN_POINT('Ctrl Pts',(2.74165931100356,-8.71622378385729,-76.1982369517102));
#17111=CARTESIAN_POINT('Ctrl Pts',(2.77034413004262,-8.71613598193422,-76.1411122891911));
#17112=CARTESIAN_POINT('Ctrl Pts',(2.79905294328358,-8.71604810656682,-76.0839398431847));
#17113=CARTESIAN_POINT('Ctrl Pts',(2.82596638926419,-8.71596441377862,-76.0259198799202));
#17114=CARTESIAN_POINT('Ctrl Pts',(2.85098035509833,-8.71588582363734,-75.9673376749462));
#17115=CARTESIAN_POINT('Ctrl Pts',(2.85565776855165,-8.7158711279035,-75.9563832666973));
#17116=CARTESIAN_POINT('Ctrl Pts',(2.86026890187996,-8.71585661058901,-75.9454092510284));
#17117=CARTESIAN_POINT('Ctrl Pts',(2.86481326500262,-8.7158422777096,-75.9344175600966));
#17118=CARTESIAN_POINT('Ctrl Pts',(2.89487646954094,-8.71574745863955,-75.8617021005733));
#17119=CARTESIAN_POINT('Ctrl Pts',(2.92207389877206,-8.71566033761335,-75.7880886511198));
#17120=CARTESIAN_POINT('Ctrl Pts',(2.94643811869778,-8.71558151593588,-75.7135883004088));
#17121=CARTESIAN_POINT('Ctrl Pts',(2.9707918943071,-8.71550272804726,-75.639119886088));
#17122=CARTESIAN_POINT('Ctrl Pts',(2.99231512996288,-8.71543223239345,-75.5637645823351));
#17123=CARTESIAN_POINT('Ctrl Pts',(3.01099152146986,-8.71537062950641,-75.487516140594));
#17124=CARTESIAN_POINT('Ctrl Pts',(3.02176016915483,-8.71533510980836,-75.4435519409075));
#17125=CARTESIAN_POINT('Ctrl Pts',(3.03158143712092,-8.71530254657911,-75.3992905484563));
#17126=CARTESIAN_POINT('Ctrl Pts',(3.0404443852463,-8.71527305493598,-75.354729642257));
#17127=CARTESIAN_POINT('Ctrl Pts',(3.05342506233143,-8.71522986146461,-75.2894657226435));
#17128=CARTESIAN_POINT('Ctrl Pts',(3.06433888891931,-8.71519347811349,-75.2235881046905));
#17129=CARTESIAN_POINT('Ctrl Pts',(3.07311393468772,-8.71516409033977,-75.1573950716788));
#17130=CARTESIAN_POINT('Ctrl Pts',(3.08211546594833,-8.71513394406239,-75.0894935847106));
#17131=CARTESIAN_POINT('Ctrl Pts',(3.08886606565568,-8.71511115913683,-75.0212606998728));
#17132=CARTESIAN_POINT('Ctrl Pts',(3.09334449590245,-8.71509593575412,-74.9530266723119));
#17133=CARTESIAN_POINT('Ctrl Pts',(3.09782292614922,-8.71508071237141,-74.884792644751));
#17134=CARTESIAN_POINT('Ctrl Pts',(3.10002921243779,-8.71507305053155,-74.8165580440902));
#17135=CARTESIAN_POINT('Ctrl Pts',(3.09999970736836,-8.71507315042558,-74.74865303448));
#17136=CARTESIAN_POINT('Ctrl Pts',(3.0999658079665,-8.71507326519731,-74.6706346039406));
#17137=CARTESIAN_POINT('Ctrl Pts',(3.09699103187926,-8.71508334203519,-74.592719406739));
#17138=CARTESIAN_POINT('Ctrl Pts',(3.09107242805617,-8.71510332750266,-74.514901628013));
#17139=CARTESIAN_POINT('Ctrl Pts',(3.08519738465212,-8.7151231658788,-74.4376565814973));
#17140=CARTESIAN_POINT('Ctrl Pts',(3.07642156717969,-8.71515276756792,-74.3605067705524));
#17141=CARTESIAN_POINT('Ctrl Pts',(3.06469171994945,-8.7151920803047,-74.2834545449012));
#17142=CARTESIAN_POINT('Ctrl Pts',(3.05764210342273,-8.71521570718691,-74.2371462995585));
#17143=CARTESIAN_POINT('Ctrl Pts',(3.04952453053919,-8.7152428416877,-74.1908735071733));
#17144=CARTESIAN_POINT('Ctrl Pts',(3.04031890638674,-8.7152734724613,-74.1446398200514));
#17145=CARTESIAN_POINT('Ctrl Pts',(3.02312760546873,-8.71533067475824,-74.0582994247997));
#17146=CARTESIAN_POINT('Ctrl Pts',(3.00236130986795,-8.71539936732086,-73.9731867127046));
#17147=CARTESIAN_POINT('Ctrl Pts',(2.97813906776938,-8.71547848786435,-73.8893678526654));
#17148=CARTESIAN_POINT('Ctrl Pts',(2.95358359569693,-8.71555869688413,-73.8043958806876));
#17149=CARTESIAN_POINT('Ctrl Pts',(2.92547631861943,-8.7156496227778,-73.7207526603851));
#17150=CARTESIAN_POINT('Ctrl Pts',(2.89388813158801,-8.71575015881243,-73.6385093424351));
#17151=CARTESIAN_POINT('Ctrl Pts',(2.88421919183921,-8.7157809322424,-73.6133351947321));
#17152=CARTESIAN_POINT('Ctrl Pts',(2.87422375058271,-8.71581260607772,-73.5882922788232));
#17153=CARTESIAN_POINT('Ctrl Pts',(2.8639029002749,-8.7158451485785,-73.5633828849216));
#17154=CARTESIAN_POINT('Ctrl Pts',(2.83722639600753,-8.71592926181869,-73.4989990858261));
#17155=CARTESIAN_POINT('Ctrl Pts',(2.80825858386043,-8.71601965988724,-73.4352360891271));
#17156=CARTESIAN_POINT('Ctrl Pts',(2.77708668903123,-8.71611528859754,-73.3723971829277));
#17157=CARTESIAN_POINT('Ctrl Pts',(2.7459426515262,-8.71621083184751,-73.3096144338464));
#17158=CARTESIAN_POINT('Ctrl Pts',(2.71259864889984,-8.71631159639449,-73.247754606431));
#17159=CARTESIAN_POINT('Ctrl Pts',(2.67718998623632,-8.71641653087558,-73.1871008421539));
#17160=CARTESIAN_POINT('Ctrl Pts',(2.6453452533964,-8.71651090355912,-73.1325519613478));
#17161=CARTESIAN_POINT('Ctrl Pts',(2.6118313261885,-8.71660864900209,-73.0789785513262));
#17162=CARTESIAN_POINT('Ctrl Pts',(2.57677782571062,-8.71670900242383,-73.0265685285089));
#17163=CARTESIAN_POINT('Ctrl Pts',(2.53302624838245,-8.71683425726091,-72.9611536302875));
#17164=CARTESIAN_POINT('Ctrl Pts',(2.48698488900056,-8.71696313162736,-72.8976977641212));
#17165=CARTESIAN_POINT('Ctrl Pts',(2.43869838176886,-8.7170944992703,-72.8361687109993));
#17166=CARTESIAN_POINT('Ctrl Pts',(2.39024128370483,-8.71722633102043,-72.7744222826108));
#17167=CARTESIAN_POINT('Ctrl Pts',(2.33952268394173,-8.7173606736951,-72.7146156676716));
#17168=CARTESIAN_POINT('Ctrl Pts',(2.28654394533952,-8.71749638906238,-72.6567449304896));
#17169=CARTESIAN_POINT('Ctrl Pts',(2.25591502933889,-8.71757485100191,-72.6232877739998));
#17170=CARTESIAN_POINT('Ctrl Pts',(2.22452990562365,-8.71765377175192,-72.5904782499961));
#17171=CARTESIAN_POINT('Ctrl Pts',(2.19238316845143,-8.71773293136402,-72.5583211816758));
#17172=CARTESIAN_POINT('Ctrl Pts',(2.14794006336032,-8.71784237012106,-72.5138637936951));
#17173=CARTESIAN_POINT('Ctrl Pts',(2.10193823605173,-8.71795248897054,-72.4705578338053));
#17174=CARTESIAN_POINT('Ctrl Pts',(2.05457270333021,-8.71806216059154,-72.4286359598869));
#17175=CARTESIAN_POINT('Ctrl Pts',(2.00725118285122,-8.71817173030522,-72.3867530399415));
#17176=CARTESIAN_POINT('Ctrl Pts',(1.958568832385,-8.71828085362116,-72.3462519807932));
#17177=CARTESIAN_POINT('Ctrl Pts',(1.90875629780346,-8.71838840635804,-72.3073274072042));
#17178=CARTESIAN_POINT('Ctrl Pts',(1.85887614986205,-8.71849610508231,-72.2683499990983));
#17179=CARTESIAN_POINT('Ctrl Pts',(1.8078631442273,-8.71860222896096,-72.2309536442723));
#17180=CARTESIAN_POINT('Ctrl Pts',(1.75597961225169,-8.71870564922871,-72.1952914840717));
#17181=CARTESIAN_POINT('Ctrl Pts',(1.7444829025098,-8.7187285658027,-72.1873892174183));
#17182=CARTESIAN_POINT('Ctrl Pts',(1.73294355506966,-8.71875134962739,-72.1795719277208));
#17183=CARTESIAN_POINT('Ctrl Pts',(1.72136459638604,-8.71877398842172,-72.1718409811828));
#17184=CARTESIAN_POINT('Ctrl Pts',(1.65608855780722,-8.71890161395805,-72.1282579977509));
#17185=CARTESIAN_POINT('Ctrl Pts',(1.58931917610361,-8.71902518049889,-72.0872569224723));
#17186=CARTESIAN_POINT('Ctrl Pts',(1.52106342354734,-8.71914358262926,-72.0488213569728));
#17187=CARTESIAN_POINT('Ctrl Pts',(1.45305348802619,-8.71926155834487,-72.0105242137512));
#17188=CARTESIAN_POINT('Ctrl Pts',(1.38356717504495,-8.71937440678136,-71.9747737795834));
#17189=CARTESIAN_POINT('Ctrl Pts',(1.31258722743462,-8.71948103442396,-71.9415992503962));
#17190=CARTESIAN_POINT('Ctrl Pts',(1.27119052763988,-8.7195432214593,-71.9222513067609));
#17191=CARTESIAN_POINT('Ctrl Pts',(1.22928537930285,-8.7196032925422,-71.903780415527));
#17192=CARTESIAN_POINT('Ctrl Pts',(1.18686599705147,-8.71966103074505,-71.8862002330744));
#17193=CARTESIAN_POINT('Ctrl Pts',(1.11536548171387,-8.71975835208826,-71.8565677387199));
#17194=CARTESIAN_POINT('Ctrl Pts',(1.04272571061629,-8.7198484073864,-71.8296054502696));
#17195=CARTESIAN_POINT('Ctrl Pts',(0.969264783005578,-8.71993024967823,
-71.8054243462894));
#17196=CARTESIAN_POINT('Ctrl Pts',(0.895724679176382,-8.72001218017971,
-71.7812171799052));
#17197=CARTESIAN_POINT('Ctrl Pts',(0.821362159731487,-8.72008587996139,
-71.7597973336574));
#17198=CARTESIAN_POINT('Ctrl Pts',(0.746509800824368,-8.72015039899682,
-71.7412256453378));
#17199=CARTESIAN_POINT('Ctrl Pts',(0.699376616873181,-8.72019102547285,
-71.7295313872725));
#17200=CARTESIAN_POINT('Ctrl Pts',(0.652049454415536,-8.72022801178817,
-71.7189654010855));
#17201=CARTESIAN_POINT('Ctrl Pts',(0.604612671139789,-8.72026112075105,
-71.7095323521048));
#17202=CARTESIAN_POINT('Ctrl Pts',(0.492199602444168,-8.7203395805424,-71.6871784336929));
#17203=CARTESIAN_POINT('Ctrl Pts',(0.378251973714541,-8.72039706472714,
-71.671003936024));
#17204=CARTESIAN_POINT('Ctrl Pts',(0.263380851782798,-8.72043208706923,
-71.6612088890775));
#17205=CARTESIAN_POINT('Ctrl Pts',(0.175897227641158,-8.72045875940742,
-71.65374917082));
#17206=CARTESIAN_POINT('Ctrl Pts',(0.0878785715260265,-8.72047240376249,
-71.6499888373265));
#17207=CARTESIAN_POINT('Ctrl Pts',(-0.000392895601461571,-8.72047236363328,
-71.6500000248979));
#17208=CARTESIAN_POINT('Ctrl Pts',(-0.0788581112235056,-8.72047232796211,
-71.6500099696199));
#17209=CARTESIAN_POINT('Ctrl Pts',(-0.156878976850864,-8.72046160079282,
-71.6529946419127));
#17210=CARTESIAN_POINT('Ctrl Pts',(-0.234458459311995,-8.72044056033218,
-71.6588789685849));
#17211=CARTESIAN_POINT('Ctrl Pts',(-0.312611281100131,-8.72041936437522,
-71.6648067824754));
#17212=CARTESIAN_POINT('Ctrl Pts',(-0.390316953274498,-8.72038770212602,
-71.6736772639242));
#17213=CARTESIAN_POINT('Ctrl Pts',(-0.46758220711631,-8.72034596023869,
-71.6854662867594));
#17214=CARTESIAN_POINT('Ctrl Pts',(-0.513198175170774,-8.72032131660518,
-71.6924263064618));
#17215=CARTESIAN_POINT('Ctrl Pts',(-0.558660646769238,-8.72029315971191,
-71.7004045820686));
#17216=CARTESIAN_POINT('Ctrl Pts',(-0.603969926403656,-8.72026156912362,
-71.70940460962));
#17217=CARTESIAN_POINT('Ctrl Pts',(-0.666812925267637,-8.72021775365536,
-71.7218874547625));
#17218=CARTESIAN_POINT('Ctrl Pts',(-0.729577541050631,-8.72016698756626,
-71.7363842594945));
#17219=CARTESIAN_POINT('Ctrl Pts',(-0.791959476863296,-8.72010995703038,
-71.7528680064091));
#17220=CARTESIAN_POINT('Ctrl Pts',(-0.85426463882863,-8.72005299668235,
-71.7693314666709));
#17221=CARTESIAN_POINT('Ctrl Pts',(-0.916187576992764,-8.71998978729745,
-71.7877768974763));
#17222=CARTESIAN_POINT('Ctrl Pts',(-0.977435294335463,-8.71992101251944,
-71.8081264056069));
#17223=CARTESIAN_POINT('Ctrl Pts',(-1.03872472132528,-8.71985219090586,
-71.8284897717364));
#17224=CARTESIAN_POINT('Ctrl Pts',(-1.09933754194174,-8.71977779631652,
-71.8507596442123));
#17225=CARTESIAN_POINT('Ctrl Pts',(-1.15899751628672,-8.71969851379281,
-71.8748087442326));
#17226=CARTESIAN_POINT('Ctrl Pts',(-1.16832598893221,-8.7196861171255,-71.8785690772557));
#17227=CARTESIAN_POINT('Ctrl Pts',(-1.17763120827332,-8.71967360095478,
-71.8823728154656));
#17228=CARTESIAN_POINT('Ctrl Pts',(-1.18691216784278,-8.71966096789941,
-71.8862193684176));
#17229=CARTESIAN_POINT('Ctrl Pts',(-1.25962167120132,-8.7195619971869,-71.9163542863307));
#17230=CARTESIAN_POINT('Ctrl Pts',(-1.33092427709693,-8.71945601925101,
-71.9491461201246));
#17231=CARTESIAN_POINT('Ctrl Pts',(-1.40083655360198,-8.71934409131941,
-71.9845602609906));
#17232=CARTESIAN_POINT('Ctrl Pts',(-1.4707719340463,-8.71923212639895,-72.0199861051826));
#17233=CARTESIAN_POINT('Ctrl Pts',(-1.53931676946223,-8.71911420754953,
-72.058036343111));
#17234=CARTESIAN_POINT('Ctrl Pts',(-1.60646589924809,-8.71899139304733,
-72.0987234556627));
#17235=CARTESIAN_POINT('Ctrl Pts',(-1.64514751867028,-8.71892064508904,
-72.1221614869244));
#17236=CARTESIAN_POINT('Ctrl Pts',(-1.68336552882153,-8.71884827255814,
-72.1464753830905));
#17237=CARTESIAN_POINT('Ctrl Pts',(-1.72111430332097,-8.71877447775272,
-72.1716738850751));
#17238=CARTESIAN_POINT('Ctrl Pts',(-1.77546294501159,-8.71866823198736,
-72.2079533239088));
#17239=CARTESIAN_POINT('Ctrl Pts',(-1.82884692297603,-8.71855898012913,
-72.2460781855651));
#17240=CARTESIAN_POINT('Ctrl Pts',(-1.88100370177939,-8.71844793038841,
-72.2858926415653));
#17241=CARTESIAN_POINT('Ctrl Pts',(-1.93313773363776,-8.71833692907942,
-72.3256897334325));
#17242=CARTESIAN_POINT('Ctrl Pts',(-1.984045231546,-8.71822413145581,-72.3671746566697));
#17243=CARTESIAN_POINT('Ctrl Pts',(-2.0334946489006,-8.71811074414789,-72.4101496815197));
#17244=CARTESIAN_POINT('Ctrl Pts',(-2.08302250952138,-8.71799717696988,
-72.4531928790902));
#17245=CARTESIAN_POINT('Ctrl Pts',(-2.13108730686939,-8.7178830182352,-72.4977305567866));
#17246=CARTESIAN_POINT('Ctrl Pts',(-2.17749286533221,-8.7177694803256,-72.5435266098529));
#17247=CARTESIAN_POINT('Ctrl Pts',(-2.18235588682236,-8.71775758224027,
-72.5483257588687));
#17248=CARTESIAN_POINT('Ctrl Pts',(-2.18720072261472,-8.7177456909727,-72.5531386962157));
#17249=CARTESIAN_POINT('Ctrl Pts',(-2.19202717238361,-8.71773380791812,
-72.5579651290338));
#17250=CARTESIAN_POINT('Ctrl Pts',(-2.24727143395521,-8.71759779270889,
-72.6132091965836));
#17251=CARTESIAN_POINT('Ctrl Pts',(-2.30034622323894,-8.71746227622743,
-72.670454482637));
#17252=CARTESIAN_POINT('Ctrl Pts',(-2.35125589236409,-8.71732840283244,
-72.7297040492485));
#17253=CARTESIAN_POINT('Ctrl Pts',(-2.40182647150608,-8.71719542111733,
-72.788558976985));
#17254=CARTESIAN_POINT('Ctrl Pts',(-2.45026113238754,-8.71706406067362,
-72.8493921916015));
#17255=CARTESIAN_POINT('Ctrl Pts',(-2.49652311457611,-8.71693544314557,
-72.912237137608));
#17256=CARTESIAN_POINT('Ctrl Pts',(-2.52413192723861,-8.71685868514538,
-72.9497425418081));
#17257=CARTESIAN_POINT('Ctrl Pts',(-2.55096609695345,-8.71678290406618,
-72.9879649889125));
#17258=CARTESIAN_POINT('Ctrl Pts',(-2.57700978828989,-8.7167083383186,-73.0269153964306));
#17259=CARTESIAN_POINT('Ctrl Pts',(-2.63792412174072,-8.71653393436203,
-73.1180176169627));
#17260=CARTESIAN_POINT('Ctrl Pts',(-2.69367621163527,-8.71636874430105,
-73.2118473144967));
#17261=CARTESIAN_POINT('Ctrl Pts',(-2.74421580489452,-8.71621544490872,
-73.3080292596009));
#17262=CARTESIAN_POINT('Ctrl Pts',(-2.78794079145064,-8.71608281594524,
-73.3912423205975));
#17263=CARTESIAN_POINT('Ctrl Pts',(-2.82776422424687,-8.71595908723085,
-73.4762174781629));
#17264=CARTESIAN_POINT('Ctrl Pts',(-2.86363533708147,-8.71584599219185,
-73.5627373263602));
#17265=CARTESIAN_POINT('Ctrl Pts',(-2.89131369256179,-8.715758727414,-73.6294965352409));
#17266=CARTESIAN_POINT('Ctrl Pts',(-2.91676714010597,-8.71567746862,-73.6974992504068));
#17267=CARTESIAN_POINT('Ctrl Pts',(-2.93983939673707,-8.71560303834219,
-73.7664633604219));
#17268=CARTESIAN_POINT('Ctrl Pts',(-2.96289040591261,-8.71552867660791,
-73.8353639607471));
#17269=CARTESIAN_POINT('Ctrl Pts',(-2.98356439031223,-8.71546113081872,
-73.9052237124384));
#17270=CARTESIAN_POINT('Ctrl Pts',(-3.00175318757531,-8.71540122123661,
-73.9757404822145));
#17271=CARTESIAN_POINT('Ctrl Pts',(-3.01622482082387,-8.7153535551107,-74.0318460517753));
#17272=CARTESIAN_POINT('Ctrl Pts',(-3.02912415352737,-8.71531072296457,
-74.0883670360562));
#17273=CARTESIAN_POINT('Ctrl Pts',(-3.04041944202858,-8.71527313793444,
-74.1451449623797));
#17274=CARTESIAN_POINT('Ctrl Pts',(-3.05576944744673,-8.71522206084897,
-74.2223046981938));
#17275=CARTESIAN_POINT('Ctrl Pts',(-3.06811378251743,-8.715180647215,-74.2996825691113));
#17276=CARTESIAN_POINT('Ctrl Pts',(-3.07751063014557,-8.71514903579499,
-74.3772691033185));
#17277=CARTESIAN_POINT('Ctrl Pts',(-3.0869477281149,-8.715117288971,-74.455187970729));
#17278=CARTESIAN_POINT('Ctrl Pts',(-3.09341216521581,-8.71509542851419,
-74.5333180690773));
#17279=CARTESIAN_POINT('Ctrl Pts',(-3.09691174535638,-8.71508359497775,
-74.611661135346));
#17280=CARTESIAN_POINT('Ctrl Pts',(-3.0989402844013,-8.71507673564328,-74.6570728597364));
#17281=CARTESIAN_POINT('Ctrl Pts',(-3.0999716790725,-8.71507324531976,-74.7025562905255));
#17282=CARTESIAN_POINT('Ctrl Pts',(-3.09999942502794,-8.71507315138149,
-74.7481119251981));
#17283=CARTESIAN_POINT('Ctrl Pts',(-3.10003763936464,-8.71507302200089,
-74.810855425439));
#17284=CARTESIAN_POINT('Ctrl Pts',(-3.09816683500873,-8.71507954824019,
-74.8738970593066));
#17285=CARTESIAN_POINT('Ctrl Pts',(-3.09435865722023,-8.71509252803483,
-74.9369344818011));
#17286=CARTESIAN_POINT('Ctrl Pts',(-3.09055434489376,-8.71510549465442,
-74.9999079186372));
#17287=CARTESIAN_POINT('Ctrl Pts',(-3.08481658471838,-8.71512490173472,
-75.0628766666462));
#17288=CARTESIAN_POINT('Ctrl Pts',(-3.07716911332992,-8.71515054782583,
-75.1255399419082));
#17289=CARTESIAN_POINT('Ctrl Pts',(-3.06951203300335,-8.71517622614088,
-75.1882819526766));
#17290=CARTESIAN_POINT('Ctrl Pts',(-3.05994051554409,-8.71520815915505,
-75.2507172406093));
#17291=CARTESIAN_POINT('Ctrl Pts',(-3.04853004779056,-8.71524614465811,
-75.3125518178072));
#17292=CARTESIAN_POINT('Ctrl Pts',(-3.04594441182365,-8.71525475225292,
-75.3265636629177));
#17293=CARTESIAN_POINT('Ctrl Pts',(-3.0432645546154,-8.71526367063402,-75.3405447112827));
#17294=CARTESIAN_POINT('Ctrl Pts',(-3.04049171352755,-8.71527289744857,
-75.3544916376348));
#17295=CARTESIAN_POINT('Ctrl Pts',(-3.02517464325816,-8.71532386602642,
-75.4315339362046));
#17296=CARTESIAN_POINT('Ctrl Pts',(-3.00697437584422,-8.71538409459489,
-75.5077898636854));
#17297=CARTESIAN_POINT('Ctrl Pts',(-2.98591140298778,-8.71545305551348,
-75.5832665200928));
#17298=CARTESIAN_POINT('Ctrl Pts',(-2.9649086222243,-8.71552181936102,-75.6585274852989));
#17299=CARTESIAN_POINT('Ctrl Pts',(-2.94105924077799,-8.71559926572075,
-75.733014372415));
#17300=CARTESIAN_POINT('Ctrl Pts',(-2.91433412241562,-8.71568487146281,
-75.806719746633));
#17301=CARTESIAN_POINT('Ctrl Pts',(-2.8988064503099,-8.71573460961083,-75.8495436124721));
#17302=CARTESIAN_POINT('Ctrl Pts',(-2.8823070876191,-8.71578710218233,-75.8921033293857));
#17303=CARTESIAN_POINT('Ctrl Pts',(-2.86482313746517,-8.71584224657204,
-75.9343936807685));
#17304=CARTESIAN_POINT('Ctrl Pts',(-2.83675354100562,-8.71593077809681,
-76.0022886980269));
#17305=CARTESIAN_POINT('Ctrl Pts',(-2.80623364659306,-8.71602596365631,
-76.0692631955475));
#17306=CARTESIAN_POINT('Ctrl Pts',(-2.77339398152871,-8.71612656968704,
-76.1350219576672));
#17307=CARTESIAN_POINT('Ctrl Pts',(-2.74051886555452,-8.71622728432349,
-76.2008517073547));
#17308=CARTESIAN_POINT('Ctrl Pts',(-2.7053192132796,-8.71633343114044,-76.2654626307996));
#17309=CARTESIAN_POINT('Ctrl Pts',(-2.6679720312962,-8.71644377257514,-76.3285833016415));
#17310=CARTESIAN_POINT('Ctrl Pts',(-2.63928378184157,-8.71652853138252,
-76.3770694645777));
#17311=CARTESIAN_POINT('Ctrl Pts',(-2.60932935209317,-8.71661576524465,
-76.4246767513742));
#17312=CARTESIAN_POINT('Ctrl Pts',(-2.5782058164628,-8.71670491323516,-76.4712945035517));
#17313=CARTESIAN_POINT('Ctrl Pts',(-2.52214838765517,-8.71686548005477,
-76.5552589783755));
#17314=CARTESIAN_POINT('Ctrl Pts',(-2.46186510330967,-8.71703357655273,
-76.6366627857791));
#17315=CARTESIAN_POINT('Ctrl Pts',(-2.39760626728135,-8.7172058063275,-76.7150659498076));
#17316=CARTESIAN_POINT('Ctrl Pts',(-2.33454281768458,-8.71737483216724,
-76.7920106050261));
#17317=CARTESIAN_POINT('Ctrl Pts',(-2.26765065393195,-8.71754783893412,
-76.8660649139989));
#17318=CARTESIAN_POINT('Ctrl Pts',(-2.1972126796686,-8.71772161626889,-76.9368370859082));
#17319=CARTESIAN_POINT('Ctrl Pts',(-2.12477194629744,-8.7179003346052,-77.009621519149));
#17320=CARTESIAN_POINT('Ctrl Pts',(-2.04858089905465,-8.71807986795139,
-77.0789339827324));
#17321=CARTESIAN_POINT('Ctrl Pts',(-1.96899494562744,-8.71825672424842,
-77.1443806932261));
#17322=CARTESIAN_POINT('Ctrl Pts',(-1.88940899220023,-8.71843358054545,
-77.2098274037197));
#17323=CARTESIAN_POINT('Ctrl Pts',(-1.80642841226459,-8.71860775979332,
-77.2714079844154));
#17324=CARTESIAN_POINT('Ctrl Pts',(-1.72045318260168,-8.718775769933,-77.3287673114253));
#17325=CARTESIAN_POINT('',(-1.72045318260168,8.718775769933,-77.3287673114253));
#17326=CARTESIAN_POINT('',(-3.7964050773568E-16,8.72047385811859,-77.85));
#17327=CARTESIAN_POINT('Ctrl Pts',(-1.72045318260166,8.71877576993301,-77.3287673114254));
#17328=CARTESIAN_POINT('Ctrl Pts',(-1.78551125050533,8.71864863546511,-77.2853631006294));
#17329=CARTESIAN_POINT('Ctrl Pts',(-1.84851550918092,8.71851861461283,-77.2397764701245));
#17330=CARTESIAN_POINT('Ctrl Pts',(-1.90951766312105,8.71838686972407,-77.1920774545925));
#17331=CARTESIAN_POINT('Ctrl Pts',(-1.97110904819074,8.71825385228698,-77.1439177054144));
#17332=CARTESIAN_POINT('Ctrl Pts',(-2.03066012128449,8.71811907734696,-77.0936041566429));
#17333=CARTESIAN_POINT('Ctrl Pts',(-2.08819950349703,8.71798374126032,-77.0411618959809));
#17334=CARTESIAN_POINT('Ctrl Pts',(-2.12290656241685,8.7179021081709,-77.0095293590872));
#17335=CARTESIAN_POINT('Ctrl Pts',(-2.15688117527828,8.71782027091635,-76.9771214408884));
#17336=CARTESIAN_POINT('Ctrl Pts',(-2.19012387534448,8.71773849205049,-76.9439365101675));
#17337=CARTESIAN_POINT('Ctrl Pts',(-2.23807228578435,8.71762053633037,-76.8960714247366));
#17338=CARTESIAN_POINT('Ctrl Pts',(-2.28466721546423,8.7175022835572,-76.8464130966564));
#17339=CARTESIAN_POINT('Ctrl Pts',(-2.3296650707744,8.7173849984541,-76.795155411702));
#17340=CARTESIAN_POINT('Ctrl Pts',(-2.37462503718522,8.71726781210689,-76.7439408865215));
#17341=CARTESIAN_POINT('Ctrl Pts',(-2.41799024538773,8.71715159180084,-76.6911300427942));
#17342=CARTESIAN_POINT('Ctrl Pts',(-2.45955419545791,8.71703759906697,-76.6369534068454));
#17343=CARTESIAN_POINT('Ctrl Pts',(-2.50040182112492,8.71692557091482,-76.5837104657535));
#17344=CARTESIAN_POINT('Ctrl Pts',(-2.53950956633579,8.71681569421533,-76.5291488734177));
#17345=CARTESIAN_POINT('Ctrl Pts',(-2.57672055083978,8.71670916639245,-76.4735171025783));
#17346=CARTESIAN_POINT('Ctrl Pts',(-2.62048380112934,8.71658388070496,-76.4080894568509));
#17347=CARTESIAN_POINT('Ctrl Pts',(-2.66157063421398,8.71646333904376,-76.3412785006447));
#17348=CARTESIAN_POINT('Ctrl Pts',(-2.70002458033065,8.71634842363173,-76.2731110483515));
#17349=CARTESIAN_POINT('Ctrl Pts',(-2.73858537466607,8.71623318891549,-76.2047541858263));
#17350=CARTESIAN_POINT('Ctrl Pts',(-2.77449903809121,8.71612361175808,-76.1350326040181));
#17351=CARTESIAN_POINT('Ctrl Pts',(-2.80776603790274,8.71602058175687,-76.063944396236));
#17352=CARTESIAN_POINT('Ctrl Pts',(-2.8269613262682,8.71596113273548,-76.0229260099826));
#17353=CARTESIAN_POINT('Ctrl Pts',(-2.84527460480386,8.71590386350438,-75.9814521402428));
#17354=CARTESIAN_POINT('Ctrl Pts',(-2.86269864862687,8.71584894496138,-75.9395194185678));
#17355=CARTESIAN_POINT('Ctrl Pts',(-2.88692761794546,8.71577257809116,-75.8812099562394));
#17356=CARTESIAN_POINT('Ctrl Pts',(-2.9094770889549,8.71570078483281,-75.8219033957506));
#17357=CARTESIAN_POINT('Ctrl Pts',(-2.93020813456406,8.71563414597153,-75.7618696991879));
#17358=CARTESIAN_POINT('Ctrl Pts',(-2.95092195111498,8.71556756249215,-75.7018858951427));
#17359=CARTESIAN_POINT('Ctrl Pts',(-2.96982017704862,8.71550612484602,-75.6411766139907));
#17360=CARTESIAN_POINT('Ctrl Pts',(-2.98681268740842,8.71545041237147,-75.5800301020663));
#17361=CARTESIAN_POINT('Ctrl Pts',(-3.00382970566113,8.71539461954415,-75.5187953999844));
#17362=CARTESIAN_POINT('Ctrl Pts',(-3.01893539773509,8.7153445684149,-75.4571226823428));
#17363=CARTESIAN_POINT('Ctrl Pts',(-3.03209012160052,8.71530084083237,-75.3953134854414));
#17364=CARTESIAN_POINT('Ctrl Pts',(-3.03483210777939,8.71529172620342,-75.3824299034397));
#17365=CARTESIAN_POINT('Ctrl Pts',(-3.03748950746607,8.7152828863182,-75.3695404189203));
#17366=CARTESIAN_POINT('Ctrl Pts',(-3.04006224424406,8.71527432644609,-75.3566477982502));
#17367=CARTESIAN_POINT('Ctrl Pts',(-3.05540807035026,8.71522326863485,-75.2797460659984));
#17368=CARTESIAN_POINT('Ctrl Pts',(-3.06780605637265,8.71518167516255,-75.2024339736059));
#17369=CARTESIAN_POINT('Ctrl Pts',(-3.07727021873385,8.71514983838311,-75.1247105561547));
#17370=CARTESIAN_POINT('Ctrl Pts',(-3.08669333243792,8.71511813968849,-75.0473242463938));
#17371=CARTESIAN_POINT('Ctrl Pts',(-3.09320807389713,8.7150961132354,-74.9695293973752));
#17372=CARTESIAN_POINT('Ctrl Pts',(-3.09677711036136,8.7150840475902,-74.8913206592895));
#17373=CARTESIAN_POINT('Ctrl Pts',(-3.09886784950679,8.71507697954342,-74.8455060334458));
#17374=CARTESIAN_POINT('Ctrl Pts',(-3.09994676922755,8.7150733296559,-74.7995493518158));
#17375=CARTESIAN_POINT('Ctrl Pts',(-3.09999807972757,8.71507315593626,-74.7534504616245));
#17376=CARTESIAN_POINT('Ctrl Pts',(-3.10009072223195,8.71507284228071,-74.6702176606448));
#17377=CARTESIAN_POINT('Ctrl Pts',(-3.09682687049161,8.71508405787463,-74.5870270480835));
#17378=CARTESIAN_POINT('Ctrl Pts',(-3.09024312842374,8.71510632342949,-74.5042411604237));
#17379=CARTESIAN_POINT('Ctrl Pts',(-3.08365223666089,8.71512861316389,-74.4213653704198));
#17380=CARTESIAN_POINT('Ctrl Pts',(-3.07373433760075,8.71516197687195,-74.3388957004902));
#17381=CARTESIAN_POINT('Ctrl Pts',(-3.06057750882953,8.71520593370195,-74.257186330905));
#17382=CARTESIAN_POINT('Ctrl Pts',(-3.05469194827621,8.7152255972994,-74.2206345560944));
#17383=CARTESIAN_POINT('Ctrl Pts',(-3.04815891436369,8.71524738070808,-74.1842347523213));
#17384=CARTESIAN_POINT('Ctrl Pts',(-3.04098950787876,8.71527124088319,-74.1480175974571));
#17385=CARTESIAN_POINT('Ctrl Pts',(-3.02305629236416,8.71533092360076,-74.0574257130564));
#17386=CARTESIAN_POINT('Ctrl Pts',(-3.0010173356265,8.71540396717694,-73.9673660698357));
#17387=CARTESIAN_POINT('Ctrl Pts',(-2.97490774237264,8.71548918236498,-73.8782638447493));
#17388=CARTESIAN_POINT('Ctrl Pts',(-2.94884511938841,8.71557424425379,-73.7893219115332));
#17389=CARTESIAN_POINT('Ctrl Pts',(-2.9187265192217,8.71567143400121,-73.7013344257932));
#17390=CARTESIAN_POINT('Ctrl Pts',(-2.88463864710567,8.71577956876717,-73.6147203535585));
#17391=CARTESIAN_POINT('Ctrl Pts',(-2.87821859643875,8.71579993468129,-73.5984076095326));
#17392=CARTESIAN_POINT('Ctrl Pts',(-2.87165789742049,8.71582068882947,-73.5821435593562));
#17393=CARTESIAN_POINT('Ctrl Pts',(-2.86495733316071,8.71584182330963,-73.5659309652015));
#17394=CARTESIAN_POINT('Ctrl Pts',(-2.83496309072156,8.71593642918116,-73.4933573041199));
#17395=CARTESIAN_POINT('Ctrl Pts',(-2.80237842122547,8.71603785674922,-73.4223165330266));
#17396=CARTESIAN_POINT('Ctrl Pts',(-2.76726820343563,8.71614516205026,-73.3527789400907));
#17397=CARTESIAN_POINT('Ctrl Pts',(-2.73192387853955,8.71625318283913,-73.2827776859848));
#17398=CARTESIAN_POINT('Ctrl Pts',(-2.69401991232817,8.71636716000513,-73.2142989993937));
#17399=CARTESIAN_POINT('Ctrl Pts',(-2.65357271943122,8.71648613057612,-73.1473297835517));
#17400=CARTESIAN_POINT('Ctrl Pts',(-2.62982116648544,8.71655599292289,-73.1080038684045));
#17401=CARTESIAN_POINT('Ctrl Pts',(-2.60519171261152,8.71662757715425,-73.0691988464413));
#17402=CARTESIAN_POINT('Ctrl Pts',(-2.57968045483705,8.7167006882747,-73.0309163048497));
#17403=CARTESIAN_POINT('Ctrl Pts',(-2.5444843609743,8.71680155456206,-72.9781005660462));
#17404=CARTESIAN_POINT('Ctrl Pts',(-2.50748856662359,8.7169057382801,-72.9261068538568));
#17405=CARTESIAN_POINT('Ctrl Pts',(-2.46883456203953,8.71701213292141,-72.8752051031435));
#17406=CARTESIAN_POINT('Ctrl Pts',(-2.43022702536167,8.71711839966041,-72.8243645439627));
#17407=CARTESIAN_POINT('Ctrl Pts',(-2.38996552511782,8.71722687201015,-72.7746137358733));
#17408=CARTESIAN_POINT('Ctrl Pts',(-2.34823420078443,8.71733644744896,-72.72619266276));
#17409=CARTESIAN_POINT('Ctrl Pts',(-2.30646796846453,8.71744611454693,-72.6777310857281));
#17410=CARTESIAN_POINT('Ctrl Pts',(-2.2632297813738,8.7175568865802,-72.6306018338344));
#17411=CARTESIAN_POINT('Ctrl Pts',(-2.21874306936807,8.71766765825803,-72.5850105792103));
#17412=CARTESIAN_POINT('Ctrl Pts',(-2.21042548426694,8.71768836900098,-72.5764864801456));
#17413=CARTESIAN_POINT('Ctrl Pts',(-2.20206435511428,8.71770907973151,-72.5680160381373));
#17414=CARTESIAN_POINT('Ctrl Pts',(-2.19366127714957,8.71772978322563,-72.5596004471479));
#17415=CARTESIAN_POINT('Ctrl Pts',(-2.13806407215614,8.71786676355723,-72.5039204523483));
#17416=CARTESIAN_POINT('Ctrl Pts',(-2.08053732388198,8.71800360659784,-72.4505417303145));
#17417=CARTESIAN_POINT('Ctrl Pts',(-2.02110377686798,8.71813911894957,-72.3994384664234));
#17418=CARTESIAN_POINT('Ctrl Pts',(-1.96169567378192,8.71827457328749,-72.3483570802063));
#17419=CARTESIAN_POINT('Ctrl Pts',(-1.90038180568892,8.71840869807565,-72.2995486945324));
#17420=CARTESIAN_POINT('Ctrl Pts',(-1.83715014326873,8.71854030144823,-72.2530259610705));
#17421=CARTESIAN_POINT('Ctrl Pts',(-1.80069112902299,8.7186161831988,-72.2262012195231));
#17422=CARTESIAN_POINT('Ctrl Pts',(-1.76359392599721,8.71869122667714,-72.2001371210064));
#17423=CARTESIAN_POINT('Ctrl Pts',(-1.72585219029124,8.71876520340843,-72.1748428752274));
#17424=CARTESIAN_POINT('Ctrl Pts',(-1.67057600678017,8.71887354901836,-72.1377971658741));
#17425=CARTESIAN_POINT('Ctrl Pts',(-1.61393953676665,8.7189794375954,-72.1024241924786));
#17426=CARTESIAN_POINT('Ctrl Pts',(-1.55619057584157,8.71908179680457,-72.0689049081277));
#17427=CARTESIAN_POINT('Ctrl Pts',(-1.49695085761279,8.71918679835978,-72.0345203420962));
#17428=CARTESIAN_POINT('Ctrl Pts',(-1.4365408171687,8.71928808597786,-72.002086896522));
#17429=CARTESIAN_POINT('Ctrl Pts',(-1.37525723990444,8.71938450211639,-71.9717509967445));
#17430=CARTESIAN_POINT('Ctrl Pts',(-1.31397366264018,8.71948091825493,-71.9414150969669));
#17431=CARTESIAN_POINT('Ctrl Pts',(-1.25181708431349,8.71957246291391,-71.9131769381707));
#17432=CARTESIAN_POINT('Ctrl Pts',(-1.18910632066891,8.71965797855096,-71.8871297343147));
#17433=CARTESIAN_POINT('Ctrl Pts',(-1.11705587592624,8.71975623025966,-71.8572032509957));
#17434=CARTESIAN_POINT('Ctrl Pts',(-1.04397150370732,8.71984713239851,-71.8300318288547));
#17435=CARTESIAN_POINT('Ctrl Pts',(-0.969846700918411,8.71992982453554,
-71.8056159597095));
#17436=CARTESIAN_POINT('Ctrl Pts',(-0.896267451190071,8.72001190806457,
-71.7813797895535));
#17437=CARTESIAN_POINT('Ctrl Pts',(-0.821662287246619,8.72008590199707,
-71.7598585810759));
#17438=CARTESIAN_POINT('Ctrl Pts',(-0.746012928529198,8.72015096475974,
-71.7411024094418));
#17439=CARTESIAN_POINT('Ctrl Pts',(-0.700547699498278,8.72019006744951,
-71.7298299591058));
#17440=CARTESIAN_POINT('Ctrl Pts',(-0.654705126074108,8.72022594419686,
-71.7195572105806));
#17441=CARTESIAN_POINT('Ctrl Pts',(-0.608480864241395,8.72025841231196,
-71.7103041208285));
#17442=CARTESIAN_POINT('Ctrl Pts',(-0.522148965568356,8.72031905219915,
-71.6930223563349));
#17443=CARTESIAN_POINT('Ctrl Pts',(-0.435577747650747,8.72036694530415,
-71.6795137228333));
#17444=CARTESIAN_POINT('Ctrl Pts',(-0.348874115493963,8.72040190807551,
-71.6696937081618));
#17445=CARTESIAN_POINT('Ctrl Pts',(-0.260977259244963,8.72043735200805,
-71.6597385494622));
#17446=CARTESIAN_POINT('Ctrl Pts',(-0.172943401919679,8.7204595072609,-71.6535739789158));
#17447=CARTESIAN_POINT('Ctrl Pts',(-0.0848655614443662,8.7204681825997,
-71.651161857005));
#17448=CARTESIAN_POINT('Ctrl Pts',(-0.0579277116901832,8.72047083587744,
-71.6504241302707));
#17449=CARTESIAN_POINT('Ctrl Pts',(-0.0309856732385336,8.72047222825804,
-71.6500377660259));
#17450=CARTESIAN_POINT('Ctrl Pts',(-0.0040419767996967,8.72047235427065,
-71.6500026350941));
#17451=CARTESIAN_POINT('Ctrl Pts',(0.0656511889534763,8.72047268021767,
-71.649911764643));
#17452=CARTESIAN_POINT('Ctrl Pts',(0.135650971586711,8.72046435621686,-71.6521750422896));
#17453=CARTESIAN_POINT('Ctrl Pts',(0.205643835986415,8.72044761722972,-71.656828389384));
#17454=CARTESIAN_POINT('Ctrl Pts',(0.275574141809366,8.72043089320364,-71.6614775773863));
#17455=CARTESIAN_POINT('Ctrl Pts',(0.34549702755091,8.72040576922689,-71.6685125833512));
#17456=CARTESIAN_POINT('Ctrl Pts',(0.415099098091722,8.7203724796315,-71.6779171985828));
#17457=CARTESIAN_POINT('Ctrl Pts',(0.477690824307086,8.72034254297553,-71.686374577755));
#17458=CARTESIAN_POINT('Ctrl Pts',(0.540022838919696,8.7203060027519,-71.6967475564138));
#17459=CARTESIAN_POINT('Ctrl Pts',(0.601871906508907,8.7202630293788,-71.7089886208442));
#17460=CARTESIAN_POINT('Ctrl Pts',(0.679072088375951,8.72020938989241,-71.7242679522408));
#17461=CARTESIAN_POINT('Ctrl Pts',(0.755342636959279,8.72014612775218,-71.7424137714015));
#17462=CARTESIAN_POINT('Ctrl Pts',(0.830696162389788,8.72007401553564,-71.7633724896146));
#17463=CARTESIAN_POINT('Ctrl Pts',(0.90631596771332,8.72000164849316,-71.7844052705237));
#17464=CARTESIAN_POINT('Ctrl Pts',(0.981013023994232,8.71992036871607,-71.8082710473993));
#17465=CARTESIAN_POINT('Ctrl Pts',(1.05479044243209,8.71983095700113,-71.8349670460604));
#17466=CARTESIAN_POINT('Ctrl Pts',(1.09744379364417,8.71977926490672,-71.8504009529517));
#17467=CARTESIAN_POINT('Ctrl Pts',(1.1397895247603,8.71972485478723,-71.8667817755452));
#17468=CARTESIAN_POINT('Ctrl Pts',(1.18182525825237,8.71966787752108,-71.8841163563472));
#17469=CARTESIAN_POINT('Ctrl Pts',(1.23993985422713,8.71958910618709,-71.9080814944812));
#17470=CARTESIAN_POINT('Ctrl Pts',(1.29758981844413,8.71950512323467,-71.9339279864301));
#17471=CARTESIAN_POINT('Ctrl Pts',(1.35448544537096,8.71941691938241,-71.9615651023776));
#17472=CARTESIAN_POINT('Ctrl Pts',(1.41132820424855,8.71932879749014,-71.9891765376097));
#17473=CARTESIAN_POINT('Ctrl Pts',(1.46741757631549,8.71923646253861,-72.0185750874006));
#17474=CARTESIAN_POINT('Ctrl Pts',(1.52248529254967,8.71914090248724,-72.0496225200965));
#17475=CARTESIAN_POINT('Ctrl Pts',(1.57762775617506,8.71904521272529,-72.0807120957167));
#17476=CARTESIAN_POINT('Ctrl Pts',(1.6317453729977,8.71894628910224,-72.1134547768304));
#17477=CARTESIAN_POINT('Ctrl Pts',(1.68459601055329,8.71884512360603,-72.147667146342));
#17478=CARTESIAN_POINT('Ctrl Pts',(1.6963074091596,8.71882270591145,-72.1552484114912));
#17479=CARTESIAN_POINT('Ctrl Pts',(1.70795671337826,8.71880017813187,-72.1629016800187));
#17480=CARTESIAN_POINT('Ctrl Pts',(1.71954149938841,8.7187775510613,-72.1706246818501));
#17481=CARTESIAN_POINT('Ctrl Pts',(1.78484836218897,8.71864999557673,-72.2141615258255));
#17482=CARTESIAN_POINT('Ctrl Pts',(1.84834464661823,8.71851898320049,-72.2600686341301));
#17483=CARTESIAN_POINT('Ctrl Pts',(1.91004281928277,8.71838568792874,-72.3083332683377));
#17484=CARTESIAN_POINT('Ctrl Pts',(1.97151884582345,8.71825287259062,-72.3564241242803));
#17485=CARTESIAN_POINT('Ctrl Pts',(2.03121027972591,8.71811779076666,-72.4068560638889));
#17486=CARTESIAN_POINT('Ctrl Pts',(2.08909679274718,8.71798160381756,-72.4596562287435));
#17487=CARTESIAN_POINT('Ctrl Pts',(2.12285709209413,8.71790217750685,-72.490450092081));
#17488=CARTESIAN_POINT('Ctrl Pts',(2.15600280759306,8.7178223752988,-72.5220501914981));
#17489=CARTESIAN_POINT('Ctrl Pts',(2.18852355201527,8.71774242757821,-72.5544671120035));
#17490=CARTESIAN_POINT('Ctrl Pts',(2.2433386200597,8.71760767236821,-72.6091071805155));
#17491=CARTESIAN_POINT('Ctrl Pts',(2.29612570674144,8.71747318196186,-72.6658244324568));
#17492=CARTESIAN_POINT('Ctrl Pts',(2.34666019741014,8.71734056635167,-72.7243677732888));
#17493=CARTESIAN_POINT('Ctrl Pts',(2.39724915531344,8.71720780780533,-72.782974213478));
#17494=CARTESIAN_POINT('Ctrl Pts',(2.44558033542279,8.7170769280987,-72.8434102611175));
#17495=CARTESIAN_POINT('Ctrl Pts',(2.49146986090751,8.71694954243573,-72.9053922009843));
#17496=CARTESIAN_POINT('Ctrl Pts',(2.52036735992414,8.71686932528309,-72.9444233966097));
#17497=CARTESIAN_POINT('Ctrl Pts',(2.54829748073016,8.71679049367888,-72.9840669932305));
#17498=CARTESIAN_POINT('Ctrl Pts',(2.57522351763586,8.71671345095951,-73.0242468791235));
#17499=CARTESIAN_POINT('Ctrl Pts',(2.63903811929646,8.71653086001733,-73.1194730508029));
#17500=CARTESIAN_POINT('Ctrl Pts',(2.6977347010216,8.71635675547632,-73.2184900268912));
#17501=CARTESIAN_POINT('Ctrl Pts',(2.7508937881556,8.71619515040142,-73.3208102413301));
#17502=CARTESIAN_POINT('Ctrl Pts',(2.79136462501235,8.71607211795346,-73.3987082062682));
#17503=CARTESIAN_POINT('Ctrl Pts',(2.82862636615098,8.71595633021215,-73.4785198992802));
#17504=CARTESIAN_POINT('Ctrl Pts',(2.86250414971471,8.7158495579803,-73.5600126081063));
#17505=CARTESIAN_POINT('Ctrl Pts',(2.89262433742607,8.7157546285213,-73.6324664533329));
#17506=CARTESIAN_POINT('Ctrl Pts',(2.9198272202729,8.71566755898673,-73.7056522605558));
#17507=CARTESIAN_POINT('Ctrl Pts',(2.94418325530203,8.71558882104429,-73.7795439426748));
#17508=CARTESIAN_POINT('Ctrl Pts',(2.96871928819064,8.71550950120659,-73.8539817048351));
#17509=CARTESIAN_POINT('Ctrl Pts',(2.99036654369563,8.71543863656162,-73.9291365337836));
#17510=CARTESIAN_POINT('Ctrl Pts',(3.00914988290531,8.7153767093118,-74.0050053810859));
#17511=CARTESIAN_POINT('Ctrl Pts',(3.02023921888543,8.71534014860916,-74.0497969449696));
#17512=CARTESIAN_POINT('Ctrl Pts',(3.03032941905769,8.71530670303841,-74.0948377738576));
#17513=CARTESIAN_POINT('Ctrl Pts',(3.03941737224908,8.71527647182606,-74.1401294913914));
#17514=CARTESIAN_POINT('Ctrl Pts',(3.05202223556094,8.71523454155954,-74.2029484668691));
#17515=CARTESIAN_POINT('Ctrl Pts',(3.06273741417212,8.71519884659067,-74.2664684112262));
#17516=CARTESIAN_POINT('Ctrl Pts',(3.07147100678526,8.71516962114423,-74.3303979808467));
#17517=CARTESIAN_POINT('Ctrl Pts',(3.08019384996495,8.7151404316689,-74.3942488650183));
#17518=CARTESIAN_POINT('Ctrl Pts',(3.08693987329442,8.71511769580024,-74.4585078864968));
#17519=CARTESIAN_POINT('Ctrl Pts',(3.09166849006865,8.71510164689924,-74.5228745995784));
#17520=CARTESIAN_POINT('Ctrl Pts',(3.09640032601161,8.71508558707239,-74.5872851325169));
#17521=CARTESIAN_POINT('Ctrl Pts',(3.09911198139106,8.71507622332107,-74.6518030104008));
#17522=CARTESIAN_POINT('Ctrl Pts',(3.09981490362319,8.7150737894832,-74.7161242966772));
#17523=CARTESIAN_POINT('Ctrl Pts',(3.09992480125886,8.71507340896738,-74.7261805404008));
#17524=CARTESIAN_POINT('Ctrl Pts',(3.09998570215258,8.71507319784241,-74.7362319816975));
#17525=CARTESIAN_POINT('Ctrl Pts',(3.09999776495605,8.71507315700192,-74.7462774649036));
#17526=CARTESIAN_POINT('Ctrl Pts',(3.10009227788373,8.71507283701379,-74.8249845440814));
#17527=CARTESIAN_POINT('Ctrl Pts',(3.09719331507636,8.71508265594522,-74.9034127826038));
#17528=CARTESIAN_POINT('Ctrl Pts',(3.09133919636591,8.71510242433115,-74.9815641876711));
#17529=CARTESIAN_POINT('Ctrl Pts',(3.08548314057808,8.71512219925826,-75.0597414523644));
#17530=CARTESIAN_POINT('Ctrl Pts',(3.07666991689266,8.71515193022534,-75.1376424855042));
#17531=CARTESIAN_POINT('Ctrl Pts',(3.06488602188168,8.71519142757921,-75.2152673133526));
#17532=CARTESIAN_POINT('Ctrl Pts',(3.05809788687412,8.7152141801046,-75.2599832422439));
#17533=CARTESIAN_POINT('Ctrl Pts',(3.05032302065739,8.71524017346659,-75.3046074173627));
#17534=CARTESIAN_POINT('Ctrl Pts',(3.04155119258465,8.71526937141208,-75.3491379998689));
#17535=CARTESIAN_POINT('Ctrl Pts',(3.02892216945727,8.71531140843399,-75.4132498077707));
#17536=CARTESIAN_POINT('Ctrl Pts',(3.0142188489071,8.71536027865207,-75.4771795507943));
#17537=CARTESIAN_POINT('Ctrl Pts',(2.99748430077214,8.7154153389999,-75.5406249848219));
#17538=CARTESIAN_POINT('Ctrl Pts',(2.98075705308234,8.71547037532765,-75.6040427407844));
#17539=CARTESIAN_POINT('Ctrl Pts',(2.96200046149881,8.71553159638542,-75.6669761251053));
#17540=CARTESIAN_POINT('Ctrl Pts',(2.94130818425555,8.715598359948,-75.7291354172082));
#17541=CARTESIAN_POINT('Ctrl Pts',(2.92058308127345,8.71566522942272,-75.7913933173407));
#17542=CARTESIAN_POINT('Ctrl Pts',(2.89791633652228,8.71573765900119,-75.852874205843));
#17543=CARTESIAN_POINT('Ctrl Pts',(2.87345062347374,8.71581500339693,-75.913306285747));
#17544=CARTESIAN_POINT('Ctrl Pts',(2.87088533059335,8.71582311315557,-75.9196427446116));
#17545=CARTESIAN_POINT('Ctrl Pts',(2.86830030198674,8.71583127694801,-75.9259676939315));
#17546=CARTESIAN_POINT('Ctrl Pts',(2.86569573146446,8.71583949403039,-75.9322808357858));
#17547=CARTESIAN_POINT('Ctrl Pts',(2.83589947953976,8.71593349734293,-76.0045030941273));
#17548=CARTESIAN_POINT('Ctrl Pts',(2.8034223737145,8.71603465697795,-76.0754905992693));
#17549=CARTESIAN_POINT('Ctrl Pts',(2.7682632632438,8.71614215617445,-76.1452485460931));
#17550=CARTESIAN_POINT('Ctrl Pts',(2.73333830122917,8.71624893946059,-76.2145419272516));
#17551=CARTESIAN_POINT('Ctrl Pts',(2.69576654364044,8.71636197815047,-76.2826227303007));
#17552=CARTESIAN_POINT('Ctrl Pts',(2.65550299926957,8.71648047169272,-76.3494698561931));
#17553=CARTESIAN_POINT('Ctrl Pts',(2.63147426775503,8.71655118701492,-76.389363304862));
#17554=CARTESIAN_POINT('Ctrl Pts',(2.60648603157346,8.71662384510397,-76.4288168269235));
#17555=CARTESIAN_POINT('Ctrl Pts',(2.58052213110435,8.7166982758045,-76.4678199937365));
#17556=CARTESIAN_POINT('Ctrl Pts',(2.51978387254882,8.71687239414,-76.5590614631446));
#17557=CARTESIAN_POINT('Ctrl Pts',(2.45454347352631,8.71705377090808,-76.6465825710347));
#17558=CARTESIAN_POINT('Ctrl Pts',(2.38512830596815,8.71723875234124,-76.7301926583213));
#17559=CARTESIAN_POINT('Ctrl Pts',(2.32509433867442,8.71739873422559,-76.8025031550349));
#17560=CARTESIAN_POINT('Ctrl Pts',(2.26193646115044,8.71756141229847,-76.8718888973876));
#17561=CARTESIAN_POINT('Ctrl Pts',(2.19583586053567,8.71772442298748,-76.938219567042));
#17562=CARTESIAN_POINT('Ctrl Pts',(2.14482140248578,8.71785022974081,-76.989411585466));
#17563=CARTESIAN_POINT('Ctrl Pts',(2.09180437250501,8.71797683907039,-77.0390266616564));
#17564=CARTESIAN_POINT('Ctrl Pts',(2.03698524923165,8.71810275138921,-77.086812164983));
#17565=CARTESIAN_POINT('Ctrl Pts',(1.9822166052559,8.71822854776373,-77.1345536658066));
#17566=CARTESIAN_POINT('Ctrl Pts',(1.92564953905691,8.71835364841055,-77.1804685789439));
#17567=CARTESIAN_POINT('Ctrl Pts',(1.8675214937686,8.71847655788148,-77.2243410173847));
#17568=CARTESIAN_POINT('Ctrl Pts',(1.8212762647317,8.7185743416037,-77.2592448396969));
#17569=CARTESIAN_POINT('Ctrl Pts',(1.77404384024149,8.71867073844341,-77.2928565446377));
#17570=CARTESIAN_POINT('Ctrl Pts',(1.72595832697208,8.71876499536582,-77.325085989546));
#17571=CARTESIAN_POINT('Ctrl Pts',(1.66060795844858,8.71889309474955,-77.3688872502346));
#17572=CARTESIAN_POINT('Ctrl Pts',(1.59390205777866,8.71901683731767,-77.4099970252329));
#17573=CARTESIAN_POINT('Ctrl Pts',(1.52587171097307,8.71913520491618,-77.4484654012331));
#17574=CARTESIAN_POINT('Ctrl Pts',(1.45754995827931,8.71925407953864,-77.4870985553332));
#17575=CARTESIAN_POINT('Ctrl Pts',(1.38789172230878,8.71936753304584,-77.5230680523986));
#17576=CARTESIAN_POINT('Ctrl Pts',(1.31689839475672,8.71947453414395,-77.5563817662405));
#17577=CARTESIAN_POINT('Ctrl Pts',(1.27574673754136,8.71953655789551,-77.5756922363912));
#17578=CARTESIAN_POINT('Ctrl Pts',(1.23414598119487,8.71959641363605,-77.5941095315021));
#17579=CARTESIAN_POINT('Ctrl Pts',(1.19209316853417,8.71965390050633,-77.6116278370072));
#17580=CARTESIAN_POINT('Ctrl Pts',(1.13417431668521,8.71973307650698,-77.6357555962935));
#17581=CARTESIAN_POINT('Ctrl Pts',(1.07524714468821,8.71980778376098,-77.6582351681579));
#17582=CARTESIAN_POINT('Ctrl Pts',(1.01557993119606,8.71987734230788,-77.6789242740897));
#17583=CARTESIAN_POINT('Ctrl Pts',(0.955973288844866,8.71994683024247,-77.6995923774864));
#17584=CARTESIAN_POINT('Ctrl Pts',(0.895628553388487,8.72001117991806,-77.7184734566331));
#17585=CARTESIAN_POINT('Ctrl Pts',(0.834832564457375,8.72006971344289,-77.7354739304375));
#17586=CARTESIAN_POINT('Ctrl Pts',(0.773960195248435,8.72012832050558,-77.7524957625738));
#17587=CARTESIAN_POINT('Ctrl Pts',(0.712635912251662,8.72018109679423,-77.7676321462886));
#17588=CARTESIAN_POINT('Ctrl Pts',(0.651160151409611,8.72022736185888,-77.7808398930356));
#17589=CARTESIAN_POINT('Ctrl Pts',(0.637229636273559,8.72023784560361,-77.7838327915936));
#17590=CARTESIAN_POINT('Ctrl Pts',(0.623291377035618,8.7202479950077,-77.786726866896));
#17591=CARTESIAN_POINT('Ctrl Pts',(0.609348919153831,8.72025780215369,-77.7895219845769));
#17592=CARTESIAN_POINT('Ctrl Pts',(0.532331146878382,8.72031197657134,-77.80496214146));
#17593=CARTESIAN_POINT('Ctrl Pts',(0.454932360941475,8.72035618745966,-77.817438170274));
#17594=CARTESIAN_POINT('Ctrl Pts',(0.377153874529794,8.72039009691618,-77.8269717182528));
#17595=CARTESIAN_POINT('Ctrl Pts',(0.299597654310796,8.72042390947025,-77.8364780223816));
#17596=CARTESIAN_POINT('Ctrl Pts',(0.221663122665409,8.72044747938484,-77.8430587096567));
#17597=CARTESIAN_POINT('Ctrl Pts',(0.143345956999472,8.72046047164607,-77.8466840227269));
#17598=CARTESIAN_POINT('Ctrl Pts',(0.0978426785326954,8.7204680203166,-77.8487903761522));
#17599=CARTESIAN_POINT('Ctrl Pts',(0.0522101865630996,8.72047199822613,
-77.849898103416));
#17600=CARTESIAN_POINT('Ctrl Pts',(0.00644834567061791,8.72047233966639,
-77.8499932933537));
#17601=CARTESIAN_POINT('Ctrl Pts',(0.00429897232490631,8.72047235570339,
-77.8499977642996));
#17602=CARTESIAN_POINT('Ctrl Pts',(0.00214952107544824,8.72047236353894,
-77.85));
#17603=CARTESIAN_POINT('Ctrl Pts',(2.44051389952465E-13,8.72047236318302,
-77.85));
#17604=CARTESIAN_POINT('Ctrl Pts',(2.44051389952465E-13,8.72047236318302,
-77.85));
#17605=CARTESIAN_POINT('Ctrl Pts',(-0.0734697129943097,8.72047235101777,
-77.85));
#17606=CARTESIAN_POINT('Ctrl Pts',(-0.147020943399736,8.72046276921705,
-77.8473838153449));
#17607=CARTESIAN_POINT('Ctrl Pts',(-0.220331040979787,8.72044401589269,
-77.8421601239879));
#17608=CARTESIAN_POINT('Ctrl Pts',(-0.293720869844243,8.72042524217241,
-77.8369307513996));
#17609=CARTESIAN_POINT('Ctrl Pts',(-0.36686851812668,8.72039727696793,-77.8290882481745));
#17610=CARTESIAN_POINT('Ctrl Pts',(-0.439455673807259,8.72036051969141,
-77.8186933230218));
#17611=CARTESIAN_POINT('Ctrl Pts',(-0.493101433774696,8.72033335411349,
-77.8110109217155));
#17612=CARTESIAN_POINT('Ctrl Pts',(-0.546441130541466,8.7203013863108,-77.8019354866522));
#17613=CARTESIAN_POINT('Ctrl Pts',(-0.599350660335006,8.7202647775142,-77.7915092940769));
#17614=CARTESIAN_POINT('Ctrl Pts',(-0.698403651448248,8.72019624145237,
-77.77199021));
#17615=CARTESIAN_POINT('Ctrl Pts',(-0.79671492865933,8.72011052590357,-77.7475859612361));
#17616=CARTESIAN_POINT('Ctrl Pts',(-0.893782127518088,8.72001010025117,
-77.7183587230201));
#17617=CARTESIAN_POINT('Ctrl Pts',(-0.989042986979578,8.71991154343618,
-77.6896753792657));
#17618=CARTESIAN_POINT('Ctrl Pts',(-1.08310524287333,8.71979881890891,-77.6563470409888));
#17619=CARTESIAN_POINT('Ctrl Pts',(-1.17549851467908,8.71967426074279,-77.6184844852269));
#17620=CARTESIAN_POINT('Ctrl Pts',(-1.27051973265046,8.7195461597629,-77.5795450030147));
#17621=CARTESIAN_POINT('Ctrl Pts',(-1.36377517836987,8.71940554240117,-77.5358094936397));
#17622=CARTESIAN_POINT('Ctrl Pts',(-1.45476477794649,8.71925494761406,-77.4874549203314));
#17623=CARTESIAN_POINT('Ctrl Pts',(-1.54575437752311,8.71910435282694,-77.439100347023));
#17624=CARTESIAN_POINT('Ctrl Pts',(-1.6344776757099,8.71894378061444,-77.3861268233915));
#17625=CARTESIAN_POINT('Ctrl Pts',(-1.72045318260166,8.71877576993301,-77.3287673114254));
#17626=CARTESIAN_POINT('Origin',(0.,0.,-78.75));
#17627=CARTESIAN_POINT('',(-6.18146853146853,-7.57011565109303E-16,-189.5));
#17628=CARTESIAN_POINT('',(-8.35,-1.02258007728804E-15,-78.75));
#17629=CARTESIAN_POINT('Origin',(0.,0.,-189.5));
#17630=CARTESIAN_POINT('Origin',(0.,0.,-63.85));
#17631=CARTESIAN_POINT('Origin',(-10.7,-1.31037207508767E-15,-63.85));
#17632=CARTESIAN_POINT('Origin',(0.,-11.5419797204109,-74.75));
#17633=CARTESIAN_POINT('',(-3.7964050773568E-16,-11.5419797204109,-77.85));
#17634=CARTESIAN_POINT('Origin',(-6.18146853146853,0.,-189.5));
#17635=CARTESIAN_POINT('',(3.74438030913772,-3.85,-189.5));
#17636=CARTESIAN_POINT('',(-3.74438030913772,-3.85,-189.5));
#17637=CARTESIAN_POINT('',(-3.55,-3.85,-189.5));
#17638=CARTESIAN_POINT('',(3.74438030913772,3.85,-189.5));
#17639=CARTESIAN_POINT('',(3.74438030913772,-3.85,-189.5));
#17640=CARTESIAN_POINT('',(-3.74438030913772,3.85,-189.5));
#17641=CARTESIAN_POINT('',(-3.55,3.85,-189.5));
#17642=CARTESIAN_POINT('',(-3.74438030913772,-3.85,-189.5));
#17643=CARTESIAN_POINT('Origin',(3.55,-3.85,-188.5));
#17644=CARTESIAN_POINT('',(3.55,-3.85,-188.5));
#17645=CARTESIAN_POINT('',(3.55,-3.85,-188.5));
#17646=CARTESIAN_POINT('',(3.55,3.85,-188.5));
#17647=CARTESIAN_POINT('',(3.55,-3.85,-188.5));
#17648=CARTESIAN_POINT('',(3.29150268371209,3.85,-187.170146593374));
#17649=CARTESIAN_POINT('Origin',(-3.55,3.85,-188.5));
#17650=CARTESIAN_POINT('',(-3.55,3.85,-188.5));
#17651=CARTESIAN_POINT('',(-3.55,3.85,-188.5));
#17652=CARTESIAN_POINT('',(-3.55,3.85,-188.5));
#17653=CARTESIAN_POINT('Origin',(-3.55,-3.85,-188.5));
#17654=CARTESIAN_POINT('',(-3.55,-3.85,-188.5));
#17655=CARTESIAN_POINT('',(-3.55,-3.85,-188.5));
#17656=CARTESIAN_POINT('',(-3.55,-3.85,-188.5));
#17657=CARTESIAN_POINT('Origin',(-3.55,-3.85,-188.5));
#17658=CARTESIAN_POINT('',(-3.55,-3.85,-188.5));
#17659=CARTESIAN_POINT('Origin',(0.,0.,-188.5));
#32954=UNCERTAINTY_MEASURE_WITH_UNIT(LENGTH_MEASURE(0.01),#33017,
'DISTANCE_ACCURACY_VALUE',
'Maximum model space distance between geometric entities at asserted c
onnectivities');
#32984=UNCERTAINTY_MEASURE_WITH_UNIT(LENGTH_MEASURE(0.01),#33017,
'DISTANCE_ACCURACY_VALUE',
'Maximum model space distance between geometric entities at asserted c
onnectivities');
#32986=(
GEOMETRIC_REPRESENTATION_CONTEXT(3)
GLOBAL_UNCERTAINTY_ASSIGNED_CONTEXT((#32954))
GLOBAL_UNIT_ASSIGNED_CONTEXT((#33017,#33019,#33020))
REPRESENTATION_CONTEXT('','3D')
);
#33016=(
GEOMETRIC_REPRESENTATION_CONTEXT(3)
GLOBAL_UNCERTAINTY_ASSIGNED_CONTEXT((#32984))
GLOBAL_UNIT_ASSIGNED_CONTEXT((#33017,#33019,#33020))
REPRESENTATION_CONTEXT('','3D')
);
#33017=(
LENGTH_UNIT()
NAMED_UNIT(*)
SI_UNIT(.MILLI.,.METRE.)
);
#33019=(
NAMED_UNIT(*)
PLANE_ANGLE_UNIT()
SI_UNIT($,.RADIAN.)
);
#33020=(
NAMED_UNIT(*)
SI_UNIT($,.STERADIAN.)
SOLID_ANGLE_UNIT()
);
#33022=SHAPE_DEFINITION_REPRESENTATION(#33053,#33125);
#33053=PRODUCT_DEFINITION_SHAPE('',$,#33157);
#33125=SHAPE_REPRESENTATION('',(#10268),#32986);
#33155=PRODUCT_DEFINITION_CONTEXT('part definition',#33250,'design');
#33157=PRODUCT_DEFINITION(
'P_Torque Wrench_Handle_PRT-TQ-1012-01_M_Rev01','PRT-TQ-1012-01',#33188,
#33155);
#33188=PRODUCT_DEFINITION_FORMATION('',$,#33253);
#33250=APPLICATION_CONTEXT(
'Core Data for Automotive Mechanical Design Process');
#33251=PRODUCT_CONTEXT('part definition',#33250,'mechanical');
#33253=PRODUCT('P_Torque Wrench_Handle_PRT-TQ-1012-01_M_Rev01',
'PRT-TQ-1012-01',$,(#33251));
#33284=PRESENTATION_STYLE_ASSIGNMENT((#33291));
#33291=SURFACE_STYLE_USAGE(.BOTH.,#33298);
#33298=SURFACE_SIDE_STYLE('',(#33305));
#33305=SURFACE_STYLE_FILL_AREA(#33312);
#33312=FILL_AREA_STYLE('Opaque(186,91,6)',(#33319));
#33319=FILL_AREA_STYLE_COLOUR('Opaque(186,91,6)',#33326);
#33326=COLOUR_RGB('Opaque(186,91,6)', 0.09019608, 0.27058824, 0.51372549);
ENDSEC;
END-ISO-10303-21;
